ISO-10303-21;
HEADER;
/* Generated by software containing ST-Developer
 * from STEP Tools, Inc. (www.steptools.com) 
 */

FILE_DESCRIPTION(
/* description */ (''),
/* implementation_level */ '2;1');

FILE_NAME(
/* name */ 'Carriage Drive Gear Rack m0.5 x 6 x 216.step',
/* time_stamp */ '2026-10-05T09:57:53+05:00',
/* author */ (''),
/* organization */ (''),
/* preprocessor_version */ 'ST-DEVELOPER v20.2',
/* originating_system */ 'Autodesk Translation Framework v15.15.0.0',
/* authorisation */ '');

FILE_SCHEMA (('AUTOMOTIVE_DESIGN { 1 0 10303 214 3 1 1 }'));
ENDSEC;

DATA;
#10=MECHANICAL_DESIGN_GEOMETRIC_PRESENTATION_REPRESENTATION('',(#558),#113984);
#522=SHAPE_REPRESENTATION_RELATIONSHIP('SRR','None',#114059,#540);
#540=ADVANCED_BREP_SHAPE_REPRESENTATION('',(#576),#113973);
#558=STYLED_ITEM('',(#114296),#576);
#576=MANIFOLD_SOLID_BREP('Carriage Drive Gear Rack m0.5 x 6 x 216',#60399);
#703=CYLINDRICAL_SURFACE('',#62400,2.5);
#704=CYLINDRICAL_SURFACE('',#62406,2.5);
#705=CYLINDRICAL_SURFACE('',#62413,1.45);
#706=CYLINDRICAL_SURFACE('',#62415,1.45);
#926=CONICAL_SURFACE('',#62397,2.65000000000001,0.785398163397467);
#927=CONICAL_SURFACE('',#62403,2.65,0.785398163397448);
#1244=CIRCLE('',#62398,2.80000000000001);
#1245=CIRCLE('',#62399,2.5);
#1246=CIRCLE('',#62401,2.5);
#1247=CIRCLE('',#62404,2.8);
#1248=CIRCLE('',#62405,2.5);
#1249=CIRCLE('',#62407,2.5);
#1250=CIRCLE('',#62410,1.45);
#1251=CIRCLE('',#62412,1.45);
#1252=CIRCLE('',#62414,1.45);
#1253=CIRCLE('',#62416,1.45);
#1841=FACE_BOUND('',#9802,.T.);
#1842=FACE_BOUND('',#9806,.T.);
#1843=FACE_BOUND('',#9808,.T.);
#1844=FACE_BOUND('',#9810,.T.);
#1845=FACE_BOUND('',#9816,.T.);
#1846=FACE_BOUND('',#9817,.T.);
#3186=PLANE('',#62402);
#3187=PLANE('',#62408);
#3188=PLANE('',#62409);
#3189=PLANE('',#62411);
#3190=PLANE('',#62417);
#3191=PLANE('',#62418);
#3192=PLANE('',#62419);
#3193=PLANE('',#62420);
#3194=PLANE('',#62421);
#3195=PLANE('',#62422);
#3196=PLANE('',#62423);
#3197=PLANE('',#62424);
#3198=PLANE('',#62425);
#3199=PLANE('',#62426);
#3200=PLANE('',#62427);
#3201=PLANE('',#62428);
#3202=PLANE('',#62429);
#3203=PLANE('',#62430);
#3204=PLANE('',#62431);
#3205=PLANE('',#62432);
#3206=PLANE('',#62433);
#3207=PLANE('',#62434);
#3208=PLANE('',#62435);
#3209=PLANE('',#62436);
#3210=PLANE('',#62437);
#3211=PLANE('',#62438);
#3212=PLANE('',#62439);
#3213=PLANE('',#62440);
#3214=PLANE('',#62441);
#3215=PLANE('',#62442);
#3216=PLANE('',#62443);
#3217=PLANE('',#62444);
#3218=PLANE('',#62445);
#3219=PLANE('',#62446);
#3220=PLANE('',#62447);
#3221=PLANE('',#62448);
#3222=PLANE('',#62449);
#3223=PLANE('',#62450);
#3224=PLANE('',#62451);
#3225=PLANE('',#62452);
#3226=PLANE('',#62453);
#3227=PLANE('',#62454);
#3228=PLANE('',#62455);
#3229=PLANE('',#62456);
#3230=PLANE('',#62457);
#3231=PLANE('',#62458);
#3232=PLANE('',#62459);
#3233=PLANE('',#62460);
#3234=PLANE('',#62461);
#3235=PLANE('',#62462);
#3236=PLANE('',#62463);
#3237=PLANE('',#62464);
#3238=PLANE('',#62465);
#3239=PLANE('',#62466);
#3240=PLANE('',#62467);
#3241=PLANE('',#62468);
#3242=PLANE('',#62469);
#3243=PLANE('',#62470);
#3244=PLANE('',#62471);
#3245=PLANE('',#62472);
#3246=PLANE('',#62473);
#3247=PLANE('',#62474);
#3248=PLANE('',#62475);
#3249=PLANE('',#62476);
#3250=PLANE('',#62477);
#3251=PLANE('',#62478);
#3252=PLANE('',#62479);
#3253=PLANE('',#62480);
#3254=PLANE('',#62481);
#3255=PLANE('',#62482);
#3256=PLANE('',#62483);
#3257=PLANE('',#62484);
#3258=PLANE('',#62485);
#3259=PLANE('',#62486);
#3260=PLANE('',#62487);
#3261=PLANE('',#62488);
#3262=PLANE('',#62489);
#3263=PLANE('',#62490);
#3264=PLANE('',#62491);
#3265=PLANE('',#62492);
#3266=PLANE('',#62493);
#3267=PLANE('',#62494);
#3268=PLANE('',#62495);
#3269=PLANE('',#62496);
#3270=PLANE('',#62497);
#3271=PLANE('',#62498);
#3272=PLANE('',#62499);
#3273=PLANE('',#62500);
#3274=PLANE('',#62501);
#3275=PLANE('',#62502);
#3276=PLANE('',#62503);
#3277=PLANE('',#62504);
#3278=PLANE('',#62505);
#3279=PLANE('',#62506);
#3280=PLANE('',#62507);
#3281=PLANE('',#62508);
#3282=PLANE('',#62509);
#3283=PLANE('',#62510);
#3284=PLANE('',#62511);
#3285=PLANE('',#62512);
#3286=PLANE('',#62513);
#3287=PLANE('',#62514);
#3288=PLANE('',#62515);
#3289=PLANE('',#62516);
#3290=PLANE('',#62517);
#3291=PLANE('',#62518);
#3292=PLANE('',#62519);
#3293=PLANE('',#62520);
#3294=PLANE('',#62521);
#3295=PLANE('',#62522);
#3296=PLANE('',#62523);
#3297=PLANE('',#62524);
#3298=PLANE('',#62525);
#3299=PLANE('',#62526);
#3300=PLANE('',#62527);
#3301=PLANE('',#62528);
#3302=PLANE('',#62529);
#3303=PLANE('',#62530);
#3304=PLANE('',#62531);
#3305=PLANE('',#62532);
#3306=PLANE('',#62533);
#3307=PLANE('',#62534);
#3308=PLANE('',#62535);
#3309=PLANE('',#62536);
#3310=PLANE('',#62537);
#3311=PLANE('',#62538);
#3312=PLANE('',#62539);
#3313=PLANE('',#62540);
#3314=PLANE('',#62541);
#3315=PLANE('',#62542);
#3316=PLANE('',#62543);
#3317=PLANE('',#62544);
#3318=PLANE('',#62545);
#3319=PLANE('',#62546);
#3320=PLANE('',#62547);
#3321=PLANE('',#62548);
#3322=PLANE('',#62549);
#3323=PLANE('',#62550);
#3324=PLANE('',#62551);
#3325=PLANE('',#62552);
#3326=PLANE('',#62553);
#3327=PLANE('',#62554);
#3328=PLANE('',#62555);
#3329=PLANE('',#62556);
#3330=PLANE('',#62557);
#3331=PLANE('',#62558);
#3332=PLANE('',#62559);
#3333=PLANE('',#62560);
#3334=PLANE('',#62561);
#3335=PLANE('',#62562);
#3336=PLANE('',#62563);
#3337=PLANE('',#62564);
#3338=PLANE('',#62565);
#3339=PLANE('',#62566);
#3340=PLANE('',#62567);
#3341=PLANE('',#62568);
#3342=PLANE('',#62569);
#3343=PLANE('',#62570);
#3344=PLANE('',#62571);
#3345=PLANE('',#62572);
#3346=PLANE('',#62573);
#3347=PLANE('',#62574);
#3348=PLANE('',#62575);
#3349=PLANE('',#62576);
#3350=PLANE('',#62577);
#3351=PLANE('',#62578);
#3352=PLANE('',#62579);
#3353=PLANE('',#62580);
#3354=PLANE('',#62581);
#3355=PLANE('',#62582);
#3356=PLANE('',#62583);
#3357=PLANE('',#62584);
#3358=PLANE('',#62585);
#3359=PLANE('',#62586);
#3360=PLANE('',#62587);
#3361=PLANE('',#62588);
#3362=PLANE('',#62589);
#3363=PLANE('',#62590);
#3364=PLANE('',#62591);
#3365=PLANE('',#62592);
#3366=PLANE('',#62593);
#3367=PLANE('',#62594);
#3368=PLANE('',#62595);
#3369=PLANE('',#62596);
#3370=PLANE('',#62597);
#3371=PLANE('',#62598);
#3372=PLANE('',#62599);
#3373=PLANE('',#62600);
#3374=PLANE('',#62601);
#3375=PLANE('',#62602);
#3376=PLANE('',#62603);
#3377=PLANE('',#62604);
#3378=PLANE('',#62605);
#3379=PLANE('',#62606);
#3380=PLANE('',#62607);
#3381=PLANE('',#62608);
#3382=PLANE('',#62609);
#3383=PLANE('',#62610);
#3384=PLANE('',#62611);
#3385=PLANE('',#62612);
#3386=PLANE('',#62613);
#3387=PLANE('',#62614);
#3388=PLANE('',#62615);
#3389=PLANE('',#62616);
#3390=PLANE('',#62617);
#3391=PLANE('',#62618);
#3392=PLANE('',#62619);
#3393=PLANE('',#62620);
#3394=PLANE('',#62621);
#3395=PLANE('',#62622);
#3396=PLANE('',#62623);
#3397=PLANE('',#62624);
#3398=PLANE('',#62625);
#3399=PLANE('',#62626);
#3400=PLANE('',#62627);
#3401=PLANE('',#62628);
#3402=PLANE('',#62629);
#3403=PLANE('',#62630);
#3404=PLANE('',#62631);
#3405=PLANE('',#62632);
#3406=PLANE('',#62633);
#3407=PLANE('',#62634);
#3408=PLANE('',#62635);
#3409=PLANE('',#62636);
#3410=PLANE('',#62637);
#3411=PLANE('',#62638);
#3412=PLANE('',#62639);
#3413=PLANE('',#62640);
#3414=PLANE('',#62641);
#3415=PLANE('',#62642);
#3416=PLANE('',#62643);
#3417=PLANE('',#62644);
#3418=PLANE('',#62645);
#3419=PLANE('',#62646);
#3420=PLANE('',#62647);
#3421=PLANE('',#62648);
#3422=PLANE('',#62649);
#3423=PLANE('',#62650);
#3424=PLANE('',#62651);
#3425=PLANE('',#62652);
#3426=PLANE('',#62653);
#3427=PLANE('',#62654);
#3428=PLANE('',#62655);
#3429=PLANE('',#62656);
#3430=PLANE('',#62657);
#3431=PLANE('',#62658);
#3432=PLANE('',#62659);
#3433=PLANE('',#62660);
#3434=PLANE('',#62661);
#3435=PLANE('',#62662);
#3436=PLANE('',#62663);
#3437=PLANE('',#62664);
#3438=PLANE('',#62665);
#3439=PLANE('',#62666);
#3440=PLANE('',#62667);
#3441=PLANE('',#62668);
#3442=PLANE('',#62669);
#3443=PLANE('',#62670);
#3444=PLANE('',#62671);
#3445=PLANE('',#62672);
#3446=PLANE('',#62673);
#3447=PLANE('',#62674);
#3448=PLANE('',#62675);
#3449=PLANE('',#62676);
#3450=PLANE('',#62677);
#3451=PLANE('',#62678);
#3452=PLANE('',#62679);
#3453=PLANE('',#62680);
#3454=PLANE('',#62681);
#3455=PLANE('',#62682);
#3456=PLANE('',#62683);
#3457=PLANE('',#62684);
#3458=PLANE('',#62685);
#3459=PLANE('',#62686);
#3460=PLANE('',#62687);
#3461=PLANE('',#62688);
#3462=PLANE('',#62689);
#3463=PLANE('',#62690);
#3464=PLANE('',#62691);
#3465=PLANE('',#62692);
#3466=PLANE('',#62693);
#3467=PLANE('',#62694);
#3468=PLANE('',#62695);
#3469=PLANE('',#62696);
#3470=PLANE('',#62697);
#3471=PLANE('',#62698);
#3472=PLANE('',#62699);
#3473=PLANE('',#62700);
#3474=PLANE('',#62701);
#3475=PLANE('',#62702);
#3476=PLANE('',#62703);
#3477=PLANE('',#62704);
#3478=PLANE('',#62705);
#3479=PLANE('',#62706);
#3480=PLANE('',#62707);
#3481=PLANE('',#62708);
#3482=PLANE('',#62709);
#3483=PLANE('',#62710);
#3484=PLANE('',#62711);
#3485=PLANE('',#62712);
#3486=PLANE('',#62713);
#3487=PLANE('',#62714);
#3488=PLANE('',#62715);
#3489=PLANE('',#62716);
#3490=PLANE('',#62717);
#3491=PLANE('',#62718);
#3492=PLANE('',#62719);
#3493=PLANE('',#62720);
#3494=PLANE('',#62721);
#3495=PLANE('',#62722);
#3496=PLANE('',#62723);
#3497=PLANE('',#62724);
#3498=PLANE('',#62725);
#3499=PLANE('',#62726);
#3500=PLANE('',#62727);
#3501=PLANE('',#62728);
#3502=PLANE('',#62729);
#3503=PLANE('',#62730);
#3504=PLANE('',#62731);
#3505=PLANE('',#62732);
#3506=PLANE('',#62733);
#3507=PLANE('',#62734);
#3508=PLANE('',#62735);
#3509=PLANE('',#62736);
#3510=PLANE('',#62737);
#3511=PLANE('',#62738);
#3512=PLANE('',#62739);
#3513=PLANE('',#62740);
#3514=PLANE('',#62741);
#3515=PLANE('',#62742);
#3516=PLANE('',#62743);
#3517=PLANE('',#62744);
#3518=PLANE('',#62745);
#3519=PLANE('',#62746);
#3520=PLANE('',#62747);
#3521=PLANE('',#62748);
#3522=PLANE('',#62749);
#3523=PLANE('',#62750);
#3524=PLANE('',#62751);
#3525=PLANE('',#62752);
#3526=PLANE('',#62753);
#3527=PLANE('',#62754);
#3528=PLANE('',#62755);
#3529=PLANE('',#62756);
#3530=PLANE('',#62757);
#3531=PLANE('',#62758);
#3532=PLANE('',#62759);
#3533=PLANE('',#62760);
#3534=PLANE('',#62761);
#3535=PLANE('',#62762);
#3536=PLANE('',#62763);
#3537=PLANE('',#62764);
#3538=PLANE('',#62765);
#3539=PLANE('',#62766);
#3540=PLANE('',#62767);
#3541=PLANE('',#62768);
#3542=PLANE('',#62769);
#3543=PLANE('',#62770);
#3544=PLANE('',#62771);
#3545=PLANE('',#62772);
#3546=PLANE('',#62773);
#3547=PLANE('',#62774);
#3548=PLANE('',#62775);
#3549=PLANE('',#62776);
#3550=PLANE('',#62777);
#3551=PLANE('',#62778);
#3552=PLANE('',#62779);
#3553=PLANE('',#62780);
#3554=PLANE('',#62781);
#3555=PLANE('',#62782);
#3556=PLANE('',#62783);
#3557=PLANE('',#62784);
#3558=PLANE('',#62785);
#3559=PLANE('',#62786);
#3560=PLANE('',#62787);
#3561=PLANE('',#62788);
#3562=PLANE('',#62789);
#3563=PLANE('',#62790);
#3564=PLANE('',#62791);
#3565=PLANE('',#62792);
#3566=PLANE('',#62793);
#3567=PLANE('',#62794);
#3568=PLANE('',#62795);
#3569=PLANE('',#62796);
#3570=PLANE('',#62797);
#3571=PLANE('',#62798);
#3572=PLANE('',#62799);
#3573=PLANE('',#62800);
#3574=PLANE('',#62801);
#3575=PLANE('',#62802);
#3576=PLANE('',#62803);
#3577=PLANE('',#62804);
#3578=PLANE('',#62805);
#3579=PLANE('',#62806);
#3580=PLANE('',#62807);
#3581=PLANE('',#62808);
#3582=PLANE('',#62809);
#3583=PLANE('',#62810);
#3584=PLANE('',#62811);
#3585=PLANE('',#62812);
#3586=PLANE('',#62813);
#3587=PLANE('',#62814);
#3588=PLANE('',#62815);
#3589=PLANE('',#62816);
#3590=PLANE('',#62817);
#3591=PLANE('',#62818);
#3592=PLANE('',#62819);
#3593=PLANE('',#62820);
#3594=PLANE('',#62821);
#3595=PLANE('',#62822);
#3596=PLANE('',#62823);
#3597=PLANE('',#62824);
#3598=PLANE('',#62825);
#3599=PLANE('',#62826);
#3600=PLANE('',#62827);
#3601=PLANE('',#62828);
#3602=PLANE('',#62829);
#3603=PLANE('',#62830);
#3604=PLANE('',#62831);
#3605=PLANE('',#62832);
#3606=PLANE('',#62833);
#3607=PLANE('',#62834);
#3608=PLANE('',#62835);
#3609=PLANE('',#62836);
#3610=PLANE('',#62837);
#3611=PLANE('',#62838);
#3612=PLANE('',#62839);
#3613=PLANE('',#62840);
#3614=PLANE('',#62841);
#3615=PLANE('',#62842);
#3616=PLANE('',#62843);
#3617=PLANE('',#62844);
#3618=PLANE('',#62845);
#3619=PLANE('',#62846);
#3620=PLANE('',#62847);
#3621=PLANE('',#62848);
#3622=PLANE('',#62849);
#3623=PLANE('',#62850);
#3624=PLANE('',#62851);
#3625=PLANE('',#62852);
#3626=PLANE('',#62853);
#3627=PLANE('',#62854);
#3628=PLANE('',#62855);
#3629=PLANE('',#62856);
#3630=PLANE('',#62857);
#3631=PLANE('',#62858);
#3632=PLANE('',#62859);
#3633=PLANE('',#62860);
#3634=PLANE('',#62861);
#3635=PLANE('',#62862);
#3636=PLANE('',#62863);
#3637=PLANE('',#62864);
#3638=PLANE('',#62865);
#3639=PLANE('',#62866);
#3640=PLANE('',#62867);
#3641=PLANE('',#62868);
#3642=PLANE('',#62869);
#3643=PLANE('',#62870);
#3644=PLANE('',#62871);
#3645=PLANE('',#62872);
#3646=PLANE('',#62873);
#3647=PLANE('',#62874);
#3648=PLANE('',#62875);
#3649=PLANE('',#62876);
#3650=PLANE('',#62877);
#3651=PLANE('',#62878);
#3652=PLANE('',#62879);
#3653=PLANE('',#62880);
#3654=PLANE('',#62881);
#3655=PLANE('',#62882);
#3656=PLANE('',#62883);
#3657=PLANE('',#62884);
#3658=PLANE('',#62885);
#3659=PLANE('',#62886);
#3660=PLANE('',#62887);
#3661=PLANE('',#62888);
#3662=PLANE('',#62889);
#3663=PLANE('',#62890);
#3664=PLANE('',#62891);
#3665=PLANE('',#62892);
#3666=PLANE('',#62893);
#3667=PLANE('',#62894);
#3668=PLANE('',#62895);
#3669=PLANE('',#62896);
#3670=PLANE('',#62897);
#3671=PLANE('',#62898);
#3672=PLANE('',#62899);
#3673=PLANE('',#62900);
#3674=PLANE('',#62901);
#3675=PLANE('',#62902);
#3676=PLANE('',#62903);
#3677=PLANE('',#62904);
#3678=PLANE('',#62905);
#3679=PLANE('',#62906);
#3680=PLANE('',#62907);
#3681=PLANE('',#62908);
#3682=PLANE('',#62909);
#3683=PLANE('',#62910);
#3684=PLANE('',#62911);
#3685=PLANE('',#62912);
#3686=PLANE('',#62913);
#3687=PLANE('',#62914);
#3688=PLANE('',#62915);
#3689=PLANE('',#62916);
#3690=PLANE('',#62917);
#3691=PLANE('',#62918);
#3692=PLANE('',#62919);
#3693=PLANE('',#62920);
#3694=PLANE('',#62921);
#3695=PLANE('',#62922);
#6233=FACE_OUTER_BOUND('',#9799,.T.);
#6234=FACE_OUTER_BOUND('',#9800,.T.);
#6235=FACE_OUTER_BOUND('',#9801,.T.);
#6236=FACE_OUTER_BOUND('',#9803,.T.);
#6237=FACE_OUTER_BOUND('',#9804,.T.);
#6238=FACE_OUTER_BOUND('',#9805,.T.);
#6239=FACE_OUTER_BOUND('',#9807,.T.);
#6240=FACE_OUTER_BOUND('',#9809,.T.);
#6241=FACE_OUTER_BOUND('',#9811,.T.);
#6242=FACE_OUTER_BOUND('',#9812,.T.);
#6243=FACE_OUTER_BOUND('',#9813,.T.);
#6244=FACE_OUTER_BOUND('',#9814,.T.);
#6245=FACE_OUTER_BOUND('',#9815,.T.);
#6246=FACE_OUTER_BOUND('',#9818,.T.);
#6247=FACE_OUTER_BOUND('',#9819,.T.);
#6248=FACE_OUTER_BOUND('',#9820,.T.);
#6249=FACE_OUTER_BOUND('',#9821,.T.);
#6250=FACE_OUTER_BOUND('',#9822,.T.);
#6251=FACE_OUTER_BOUND('',#9823,.T.);
#6252=FACE_OUTER_BOUND('',#9824,.T.);
#6253=FACE_OUTER_BOUND('',#9825,.T.);
#6254=FACE_OUTER_BOUND('',#9826,.T.);
#6255=FACE_OUTER_BOUND('',#9827,.T.);
#6256=FACE_OUTER_BOUND('',#9828,.T.);
#6257=FACE_OUTER_BOUND('',#9829,.T.);
#6258=FACE_OUTER_BOUND('',#9830,.T.);
#6259=FACE_OUTER_BOUND('',#9831,.T.);
#6260=FACE_OUTER_BOUND('',#9832,.T.);
#6261=FACE_OUTER_BOUND('',#9833,.T.);
#6262=FACE_OUTER_BOUND('',#9834,.T.);
#6263=FACE_OUTER_BOUND('',#9835,.T.);
#6264=FACE_OUTER_BOUND('',#9836,.T.);
#6265=FACE_OUTER_BOUND('',#9837,.T.);
#6266=FACE_OUTER_BOUND('',#9838,.T.);
#6267=FACE_OUTER_BOUND('',#9839,.T.);
#6268=FACE_OUTER_BOUND('',#9840,.T.);
#6269=FACE_OUTER_BOUND('',#9841,.T.);
#6270=FACE_OUTER_BOUND('',#9842,.T.);
#6271=FACE_OUTER_BOUND('',#9843,.T.);
#6272=FACE_OUTER_BOUND('',#9844,.T.);
#6273=FACE_OUTER_BOUND('',#9845,.T.);
#6274=FACE_OUTER_BOUND('',#9846,.T.);
#6275=FACE_OUTER_BOUND('',#9847,.T.);
#6276=FACE_OUTER_BOUND('',#9848,.T.);
#6277=FACE_OUTER_BOUND('',#9849,.T.);
#6278=FACE_OUTER_BOUND('',#9850,.T.);
#6279=FACE_OUTER_BOUND('',#9851,.T.);
#6280=FACE_OUTER_BOUND('',#9852,.T.);
#6281=FACE_OUTER_BOUND('',#9853,.T.);
#6282=FACE_OUTER_BOUND('',#9854,.T.);
#6283=FACE_OUTER_BOUND('',#9855,.T.);
#6284=FACE_OUTER_BOUND('',#9856,.T.);
#6285=FACE_OUTER_BOUND('',#9857,.T.);
#6286=FACE_OUTER_BOUND('',#9858,.T.);
#6287=FACE_OUTER_BOUND('',#9859,.T.);
#6288=FACE_OUTER_BOUND('',#9860,.T.);
#6289=FACE_OUTER_BOUND('',#9861,.T.);
#6290=FACE_OUTER_BOUND('',#9862,.T.);
#6291=FACE_OUTER_BOUND('',#9863,.T.);
#6292=FACE_OUTER_BOUND('',#9864,.T.);
#6293=FACE_OUTER_BOUND('',#9865,.T.);
#6294=FACE_OUTER_BOUND('',#9866,.T.);
#6295=FACE_OUTER_BOUND('',#9867,.T.);
#6296=FACE_OUTER_BOUND('',#9868,.T.);
#6297=FACE_OUTER_BOUND('',#9869,.T.);
#6298=FACE_OUTER_BOUND('',#9870,.T.);
#6299=FACE_OUTER_BOUND('',#9871,.T.);
#6300=FACE_OUTER_BOUND('',#9872,.T.);
#6301=FACE_OUTER_BOUND('',#9873,.T.);
#6302=FACE_OUTER_BOUND('',#9874,.T.);
#6303=FACE_OUTER_BOUND('',#9875,.T.);
#6304=FACE_OUTER_BOUND('',#9876,.T.);
#6305=FACE_OUTER_BOUND('',#9877,.T.);
#6306=FACE_OUTER_BOUND('',#9878,.T.);
#6307=FACE_OUTER_BOUND('',#9879,.T.);
#6308=FACE_OUTER_BOUND('',#9880,.T.);
#6309=FACE_OUTER_BOUND('',#9881,.T.);
#6310=FACE_OUTER_BOUND('',#9882,.T.);
#6311=FACE_OUTER_BOUND('',#9883,.T.);
#6312=FACE_OUTER_BOUND('',#9884,.T.);
#6313=FACE_OUTER_BOUND('',#9885,.T.);
#6314=FACE_OUTER_BOUND('',#9886,.T.);
#6315=FACE_OUTER_BOUND('',#9887,.T.);
#6316=FACE_OUTER_BOUND('',#9888,.T.);
#6317=FACE_OUTER_BOUND('',#9889,.T.);
#6318=FACE_OUTER_BOUND('',#9890,.T.);
#6319=FACE_OUTER_BOUND('',#9891,.T.);
#6320=FACE_OUTER_BOUND('',#9892,.T.);
#6321=FACE_OUTER_BOUND('',#9893,.T.);
#6322=FACE_OUTER_BOUND('',#9894,.T.);
#6323=FACE_OUTER_BOUND('',#9895,.T.);
#6324=FACE_OUTER_BOUND('',#9896,.T.);
#6325=FACE_OUTER_BOUND('',#9897,.T.);
#6326=FACE_OUTER_BOUND('',#9898,.T.);
#6327=FACE_OUTER_BOUND('',#9899,.T.);
#6328=FACE_OUTER_BOUND('',#9900,.T.);
#6329=FACE_OUTER_BOUND('',#9901,.T.);
#6330=FACE_OUTER_BOUND('',#9902,.T.);
#6331=FACE_OUTER_BOUND('',#9903,.T.);
#6332=FACE_OUTER_BOUND('',#9904,.T.);
#6333=FACE_OUTER_BOUND('',#9905,.T.);
#6334=FACE_OUTER_BOUND('',#9906,.T.);
#6335=FACE_OUTER_BOUND('',#9907,.T.);
#6336=FACE_OUTER_BOUND('',#9908,.T.);
#6337=FACE_OUTER_BOUND('',#9909,.T.);
#6338=FACE_OUTER_BOUND('',#9910,.T.);
#6339=FACE_OUTER_BOUND('',#9911,.T.);
#6340=FACE_OUTER_BOUND('',#9912,.T.);
#6341=FACE_OUTER_BOUND('',#9913,.T.);
#6342=FACE_OUTER_BOUND('',#9914,.T.);
#6343=FACE_OUTER_BOUND('',#9915,.T.);
#6344=FACE_OUTER_BOUND('',#9916,.T.);
#6345=FACE_OUTER_BOUND('',#9917,.T.);
#6346=FACE_OUTER_BOUND('',#9918,.T.);
#6347=FACE_OUTER_BOUND('',#9919,.T.);
#6348=FACE_OUTER_BOUND('',#9920,.T.);
#6349=FACE_OUTER_BOUND('',#9921,.T.);
#6350=FACE_OUTER_BOUND('',#9922,.T.);
#6351=FACE_OUTER_BOUND('',#9923,.T.);
#6352=FACE_OUTER_BOUND('',#9924,.T.);
#6353=FACE_OUTER_BOUND('',#9925,.T.);
#6354=FACE_OUTER_BOUND('',#9926,.T.);
#6355=FACE_OUTER_BOUND('',#9927,.T.);
#6356=FACE_OUTER_BOUND('',#9928,.T.);
#6357=FACE_OUTER_BOUND('',#9929,.T.);
#6358=FACE_OUTER_BOUND('',#9930,.T.);
#6359=FACE_OUTER_BOUND('',#9931,.T.);
#6360=FACE_OUTER_BOUND('',#9932,.T.);
#6361=FACE_OUTER_BOUND('',#9933,.T.);
#6362=FACE_OUTER_BOUND('',#9934,.T.);
#6363=FACE_OUTER_BOUND('',#9935,.T.);
#6364=FACE_OUTER_BOUND('',#9936,.T.);
#6365=FACE_OUTER_BOUND('',#9937,.T.);
#6366=FACE_OUTER_BOUND('',#9938,.T.);
#6367=FACE_OUTER_BOUND('',#9939,.T.);
#6368=FACE_OUTER_BOUND('',#9940,.T.);
#6369=FACE_OUTER_BOUND('',#9941,.T.);
#6370=FACE_OUTER_BOUND('',#9942,.T.);
#6371=FACE_OUTER_BOUND('',#9943,.T.);
#6372=FACE_OUTER_BOUND('',#9944,.T.);
#6373=FACE_OUTER_BOUND('',#9945,.T.);
#6374=FACE_OUTER_BOUND('',#9946,.T.);
#6375=FACE_OUTER_BOUND('',#9947,.T.);
#6376=FACE_OUTER_BOUND('',#9948,.T.);
#6377=FACE_OUTER_BOUND('',#9949,.T.);
#6378=FACE_OUTER_BOUND('',#9950,.T.);
#6379=FACE_OUTER_BOUND('',#9951,.T.);
#6380=FACE_OUTER_BOUND('',#9952,.T.);
#6381=FACE_OUTER_BOUND('',#9953,.T.);
#6382=FACE_OUTER_BOUND('',#9954,.T.);
#6383=FACE_OUTER_BOUND('',#9955,.T.);
#6384=FACE_OUTER_BOUND('',#9956,.T.);
#6385=FACE_OUTER_BOUND('',#9957,.T.);
#6386=FACE_OUTER_BOUND('',#9958,.T.);
#6387=FACE_OUTER_BOUND('',#9959,.T.);
#6388=FACE_OUTER_BOUND('',#9960,.T.);
#6389=FACE_OUTER_BOUND('',#9961,.T.);
#6390=FACE_OUTER_BOUND('',#9962,.T.);
#6391=FACE_OUTER_BOUND('',#9963,.T.);
#6392=FACE_OUTER_BOUND('',#9964,.T.);
#6393=FACE_OUTER_BOUND('',#9965,.T.);
#6394=FACE_OUTER_BOUND('',#9966,.T.);
#6395=FACE_OUTER_BOUND('',#9967,.T.);
#6396=FACE_OUTER_BOUND('',#9968,.T.);
#6397=FACE_OUTER_BOUND('',#9969,.T.);
#6398=FACE_OUTER_BOUND('',#9970,.T.);
#6399=FACE_OUTER_BOUND('',#9971,.T.);
#6400=FACE_OUTER_BOUND('',#9972,.T.);
#6401=FACE_OUTER_BOUND('',#9973,.T.);
#6402=FACE_OUTER_BOUND('',#9974,.T.);
#6403=FACE_OUTER_BOUND('',#9975,.T.);
#6404=FACE_OUTER_BOUND('',#9976,.T.);
#6405=FACE_OUTER_BOUND('',#9977,.T.);
#6406=FACE_OUTER_BOUND('',#9978,.T.);
#6407=FACE_OUTER_BOUND('',#9979,.T.);
#6408=FACE_OUTER_BOUND('',#9980,.T.);
#6409=FACE_OUTER_BOUND('',#9981,.T.);
#6410=FACE_OUTER_BOUND('',#9982,.T.);
#6411=FACE_OUTER_BOUND('',#9983,.T.);
#6412=FACE_OUTER_BOUND('',#9984,.T.);
#6413=FACE_OUTER_BOUND('',#9985,.T.);
#6414=FACE_OUTER_BOUND('',#9986,.T.);
#6415=FACE_OUTER_BOUND('',#9987,.T.);
#6416=FACE_OUTER_BOUND('',#9988,.T.);
#6417=FACE_OUTER_BOUND('',#9989,.T.);
#6418=FACE_OUTER_BOUND('',#9990,.T.);
#6419=FACE_OUTER_BOUND('',#9991,.T.);
#6420=FACE_OUTER_BOUND('',#9992,.T.);
#6421=FACE_OUTER_BOUND('',#9993,.T.);
#6422=FACE_OUTER_BOUND('',#9994,.T.);
#6423=FACE_OUTER_BOUND('',#9995,.T.);
#6424=FACE_OUTER_BOUND('',#9996,.T.);
#6425=FACE_OUTER_BOUND('',#9997,.T.);
#6426=FACE_OUTER_BOUND('',#9998,.T.);
#6427=FACE_OUTER_BOUND('',#9999,.T.);
#6428=FACE_OUTER_BOUND('',#10000,.T.);
#6429=FACE_OUTER_BOUND('',#10001,.T.);
#6430=FACE_OUTER_BOUND('',#10002,.T.);
#6431=FACE_OUTER_BOUND('',#10003,.T.);
#6432=FACE_OUTER_BOUND('',#10004,.T.);
#6433=FACE_OUTER_BOUND('',#10005,.T.);
#6434=FACE_OUTER_BOUND('',#10006,.T.);
#6435=FACE_OUTER_BOUND('',#10007,.T.);
#6436=FACE_OUTER_BOUND('',#10008,.T.);
#6437=FACE_OUTER_BOUND('',#10009,.T.);
#6438=FACE_OUTER_BOUND('',#10010,.T.);
#6439=FACE_OUTER_BOUND('',#10011,.T.);
#6440=FACE_OUTER_BOUND('',#10012,.T.);
#6441=FACE_OUTER_BOUND('',#10013,.T.);
#6442=FACE_OUTER_BOUND('',#10014,.T.);
#6443=FACE_OUTER_BOUND('',#10015,.T.);
#6444=FACE_OUTER_BOUND('',#10016,.T.);
#6445=FACE_OUTER_BOUND('',#10017,.T.);
#6446=FACE_OUTER_BOUND('',#10018,.T.);
#6447=FACE_OUTER_BOUND('',#10019,.T.);
#6448=FACE_OUTER_BOUND('',#10020,.T.);
#6449=FACE_OUTER_BOUND('',#10021,.T.);
#6450=FACE_OUTER_BOUND('',#10022,.T.);
#6451=FACE_OUTER_BOUND('',#10023,.T.);
#6452=FACE_OUTER_BOUND('',#10024,.T.);
#6453=FACE_OUTER_BOUND('',#10025,.T.);
#6454=FACE_OUTER_BOUND('',#10026,.T.);
#6455=FACE_OUTER_BOUND('',#10027,.T.);
#6456=FACE_OUTER_BOUND('',#10028,.T.);
#6457=FACE_OUTER_BOUND('',#10029,.T.);
#6458=FACE_OUTER_BOUND('',#10030,.T.);
#6459=FACE_OUTER_BOUND('',#10031,.T.);
#6460=FACE_OUTER_BOUND('',#10032,.T.);
#6461=FACE_OUTER_BOUND('',#10033,.T.);
#6462=FACE_OUTER_BOUND('',#10034,.T.);
#6463=FACE_OUTER_BOUND('',#10035,.T.);
#6464=FACE_OUTER_BOUND('',#10036,.T.);
#6465=FACE_OUTER_BOUND('',#10037,.T.);
#6466=FACE_OUTER_BOUND('',#10038,.T.);
#6467=FACE_OUTER_BOUND('',#10039,.T.);
#6468=FACE_OUTER_BOUND('',#10040,.T.);
#6469=FACE_OUTER_BOUND('',#10041,.T.);
#6470=FACE_OUTER_BOUND('',#10042,.T.);
#6471=FACE_OUTER_BOUND('',#10043,.T.);
#6472=FACE_OUTER_BOUND('',#10044,.T.);
#6473=FACE_OUTER_BOUND('',#10045,.T.);
#6474=FACE_OUTER_BOUND('',#10046,.T.);
#6475=FACE_OUTER_BOUND('',#10047,.T.);
#6476=FACE_OUTER_BOUND('',#10048,.T.);
#6477=FACE_OUTER_BOUND('',#10049,.T.);
#6478=FACE_OUTER_BOUND('',#10050,.T.);
#6479=FACE_OUTER_BOUND('',#10051,.T.);
#6480=FACE_OUTER_BOUND('',#10052,.T.);
#6481=FACE_OUTER_BOUND('',#10053,.T.);
#6482=FACE_OUTER_BOUND('',#10054,.T.);
#6483=FACE_OUTER_BOUND('',#10055,.T.);
#6484=FACE_OUTER_BOUND('',#10056,.T.);
#6485=FACE_OUTER_BOUND('',#10057,.T.);
#6486=FACE_OUTER_BOUND('',#10058,.T.);
#6487=FACE_OUTER_BOUND('',#10059,.T.);
#6488=FACE_OUTER_BOUND('',#10060,.T.);
#6489=FACE_OUTER_BOUND('',#10061,.T.);
#6490=FACE_OUTER_BOUND('',#10062,.T.);
#6491=FACE_OUTER_BOUND('',#10063,.T.);
#6492=FACE_OUTER_BOUND('',#10064,.T.);
#6493=FACE_OUTER_BOUND('',#10065,.T.);
#6494=FACE_OUTER_BOUND('',#10066,.T.);
#6495=FACE_OUTER_BOUND('',#10067,.T.);
#6496=FACE_OUTER_BOUND('',#10068,.T.);
#6497=FACE_OUTER_BOUND('',#10069,.T.);
#6498=FACE_OUTER_BOUND('',#10070,.T.);
#6499=FACE_OUTER_BOUND('',#10071,.T.);
#6500=FACE_OUTER_BOUND('',#10072,.T.);
#6501=FACE_OUTER_BOUND('',#10073,.T.);
#6502=FACE_OUTER_BOUND('',#10074,.T.);
#6503=FACE_OUTER_BOUND('',#10075,.T.);
#6504=FACE_OUTER_BOUND('',#10076,.T.);
#6505=FACE_OUTER_BOUND('',#10077,.T.);
#6506=FACE_OUTER_BOUND('',#10078,.T.);
#6507=FACE_OUTER_BOUND('',#10079,.T.);
#6508=FACE_OUTER_BOUND('',#10080,.T.);
#6509=FACE_OUTER_BOUND('',#10081,.T.);
#6510=FACE_OUTER_BOUND('',#10082,.T.);
#6511=FACE_OUTER_BOUND('',#10083,.T.);
#6512=FACE_OUTER_BOUND('',#10084,.T.);
#6513=FACE_OUTER_BOUND('',#10085,.T.);
#6514=FACE_OUTER_BOUND('',#10086,.T.);
#6515=FACE_OUTER_BOUND('',#10087,.T.);
#6516=FACE_OUTER_BOUND('',#10088,.T.);
#6517=FACE_OUTER_BOUND('',#10089,.T.);
#6518=FACE_OUTER_BOUND('',#10090,.T.);
#6519=FACE_OUTER_BOUND('',#10091,.T.);
#6520=FACE_OUTER_BOUND('',#10092,.T.);
#6521=FACE_OUTER_BOUND('',#10093,.T.);
#6522=FACE_OUTER_BOUND('',#10094,.T.);
#6523=FACE_OUTER_BOUND('',#10095,.T.);
#6524=FACE_OUTER_BOUND('',#10096,.T.);
#6525=FACE_OUTER_BOUND('',#10097,.T.);
#6526=FACE_OUTER_BOUND('',#10098,.T.);
#6527=FACE_OUTER_BOUND('',#10099,.T.);
#6528=FACE_OUTER_BOUND('',#10100,.T.);
#6529=FACE_OUTER_BOUND('',#10101,.T.);
#6530=FACE_OUTER_BOUND('',#10102,.T.);
#6531=FACE_OUTER_BOUND('',#10103,.T.);
#6532=FACE_OUTER_BOUND('',#10104,.T.);
#6533=FACE_OUTER_BOUND('',#10105,.T.);
#6534=FACE_OUTER_BOUND('',#10106,.T.);
#6535=FACE_OUTER_BOUND('',#10107,.T.);
#6536=FACE_OUTER_BOUND('',#10108,.T.);
#6537=FACE_OUTER_BOUND('',#10109,.T.);
#6538=FACE_OUTER_BOUND('',#10110,.T.);
#6539=FACE_OUTER_BOUND('',#10111,.T.);
#6540=FACE_OUTER_BOUND('',#10112,.T.);
#6541=FACE_OUTER_BOUND('',#10113,.T.);
#6542=FACE_OUTER_BOUND('',#10114,.T.);
#6543=FACE_OUTER_BOUND('',#10115,.T.);
#6544=FACE_OUTER_BOUND('',#10116,.T.);
#6545=FACE_OUTER_BOUND('',#10117,.T.);
#6546=FACE_OUTER_BOUND('',#10118,.T.);
#6547=FACE_OUTER_BOUND('',#10119,.T.);
#6548=FACE_OUTER_BOUND('',#10120,.T.);
#6549=FACE_OUTER_BOUND('',#10121,.T.);
#6550=FACE_OUTER_BOUND('',#10122,.T.);
#6551=FACE_OUTER_BOUND('',#10123,.T.);
#6552=FACE_OUTER_BOUND('',#10124,.T.);
#6553=FACE_OUTER_BOUND('',#10125,.T.);
#6554=FACE_OUTER_BOUND('',#10126,.T.);
#6555=FACE_OUTER_BOUND('',#10127,.T.);
#6556=FACE_OUTER_BOUND('',#10128,.T.);
#6557=FACE_OUTER_BOUND('',#10129,.T.);
#6558=FACE_OUTER_BOUND('',#10130,.T.);
#6559=FACE_OUTER_BOUND('',#10131,.T.);
#6560=FACE_OUTER_BOUND('',#10132,.T.);
#6561=FACE_OUTER_BOUND('',#10133,.T.);
#6562=FACE_OUTER_BOUND('',#10134,.T.);
#6563=FACE_OUTER_BOUND('',#10135,.T.);
#6564=FACE_OUTER_BOUND('',#10136,.T.);
#6565=FACE_OUTER_BOUND('',#10137,.T.);
#6566=FACE_OUTER_BOUND('',#10138,.T.);
#6567=FACE_OUTER_BOUND('',#10139,.T.);
#6568=FACE_OUTER_BOUND('',#10140,.T.);
#6569=FACE_OUTER_BOUND('',#10141,.T.);
#6570=FACE_OUTER_BOUND('',#10142,.T.);
#6571=FACE_OUTER_BOUND('',#10143,.T.);
#6572=FACE_OUTER_BOUND('',#10144,.T.);
#6573=FACE_OUTER_BOUND('',#10145,.T.);
#6574=FACE_OUTER_BOUND('',#10146,.T.);
#6575=FACE_OUTER_BOUND('',#10147,.T.);
#6576=FACE_OUTER_BOUND('',#10148,.T.);
#6577=FACE_OUTER_BOUND('',#10149,.T.);
#6578=FACE_OUTER_BOUND('',#10150,.T.);
#6579=FACE_OUTER_BOUND('',#10151,.T.);
#6580=FACE_OUTER_BOUND('',#10152,.T.);
#6581=FACE_OUTER_BOUND('',#10153,.T.);
#6582=FACE_OUTER_BOUND('',#10154,.T.);
#6583=FACE_OUTER_BOUND('',#10155,.T.);
#6584=FACE_OUTER_BOUND('',#10156,.T.);
#6585=FACE_OUTER_BOUND('',#10157,.T.);
#6586=FACE_OUTER_BOUND('',#10158,.T.);
#6587=FACE_OUTER_BOUND('',#10159,.T.);
#6588=FACE_OUTER_BOUND('',#10160,.T.);
#6589=FACE_OUTER_BOUND('',#10161,.T.);
#6590=FACE_OUTER_BOUND('',#10162,.T.);
#6591=FACE_OUTER_BOUND('',#10163,.T.);
#6592=FACE_OUTER_BOUND('',#10164,.T.);
#6593=FACE_OUTER_BOUND('',#10165,.T.);
#6594=FACE_OUTER_BOUND('',#10166,.T.);
#6595=FACE_OUTER_BOUND('',#10167,.T.);
#6596=FACE_OUTER_BOUND('',#10168,.T.);
#6597=FACE_OUTER_BOUND('',#10169,.T.);
#6598=FACE_OUTER_BOUND('',#10170,.T.);
#6599=FACE_OUTER_BOUND('',#10171,.T.);
#6600=FACE_OUTER_BOUND('',#10172,.T.);
#6601=FACE_OUTER_BOUND('',#10173,.T.);
#6602=FACE_OUTER_BOUND('',#10174,.T.);
#6603=FACE_OUTER_BOUND('',#10175,.T.);
#6604=FACE_OUTER_BOUND('',#10176,.T.);
#6605=FACE_OUTER_BOUND('',#10177,.T.);
#6606=FACE_OUTER_BOUND('',#10178,.T.);
#6607=FACE_OUTER_BOUND('',#10179,.T.);
#6608=FACE_OUTER_BOUND('',#10180,.T.);
#6609=FACE_OUTER_BOUND('',#10181,.T.);
#6610=FACE_OUTER_BOUND('',#10182,.T.);
#6611=FACE_OUTER_BOUND('',#10183,.T.);
#6612=FACE_OUTER_BOUND('',#10184,.T.);
#6613=FACE_OUTER_BOUND('',#10185,.T.);
#6614=FACE_OUTER_BOUND('',#10186,.T.);
#6615=FACE_OUTER_BOUND('',#10187,.T.);
#6616=FACE_OUTER_BOUND('',#10188,.T.);
#6617=FACE_OUTER_BOUND('',#10189,.T.);
#6618=FACE_OUTER_BOUND('',#10190,.T.);
#6619=FACE_OUTER_BOUND('',#10191,.T.);
#6620=FACE_OUTER_BOUND('',#10192,.T.);
#6621=FACE_OUTER_BOUND('',#10193,.T.);
#6622=FACE_OUTER_BOUND('',#10194,.T.);
#6623=FACE_OUTER_BOUND('',#10195,.T.);
#6624=FACE_OUTER_BOUND('',#10196,.T.);
#6625=FACE_OUTER_BOUND('',#10197,.T.);
#6626=FACE_OUTER_BOUND('',#10198,.T.);
#6627=FACE_OUTER_BOUND('',#10199,.T.);
#6628=FACE_OUTER_BOUND('',#10200,.T.);
#6629=FACE_OUTER_BOUND('',#10201,.T.);
#6630=FACE_OUTER_BOUND('',#10202,.T.);
#6631=FACE_OUTER_BOUND('',#10203,.T.);
#6632=FACE_OUTER_BOUND('',#10204,.T.);
#6633=FACE_OUTER_BOUND('',#10205,.T.);
#6634=FACE_OUTER_BOUND('',#10206,.T.);
#6635=FACE_OUTER_BOUND('',#10207,.T.);
#6636=FACE_OUTER_BOUND('',#10208,.T.);
#6637=FACE_OUTER_BOUND('',#10209,.T.);
#6638=FACE_OUTER_BOUND('',#10210,.T.);
#6639=FACE_OUTER_BOUND('',#10211,.T.);
#6640=FACE_OUTER_BOUND('',#10212,.T.);
#6641=FACE_OUTER_BOUND('',#10213,.T.);
#6642=FACE_OUTER_BOUND('',#10214,.T.);
#6643=FACE_OUTER_BOUND('',#10215,.T.);
#6644=FACE_OUTER_BOUND('',#10216,.T.);
#6645=FACE_OUTER_BOUND('',#10217,.T.);
#6646=FACE_OUTER_BOUND('',#10218,.T.);
#6647=FACE_OUTER_BOUND('',#10219,.T.);
#6648=FACE_OUTER_BOUND('',#10220,.T.);
#6649=FACE_OUTER_BOUND('',#10221,.T.);
#6650=FACE_OUTER_BOUND('',#10222,.T.);
#6651=FACE_OUTER_BOUND('',#10223,.T.);
#6652=FACE_OUTER_BOUND('',#10224,.T.);
#6653=FACE_OUTER_BOUND('',#10225,.T.);
#6654=FACE_OUTER_BOUND('',#10226,.T.);
#6655=FACE_OUTER_BOUND('',#10227,.T.);
#6656=FACE_OUTER_BOUND('',#10228,.T.);
#6657=FACE_OUTER_BOUND('',#10229,.T.);
#6658=FACE_OUTER_BOUND('',#10230,.T.);
#6659=FACE_OUTER_BOUND('',#10231,.T.);
#6660=FACE_OUTER_BOUND('',#10232,.T.);
#6661=FACE_OUTER_BOUND('',#10233,.T.);
#6662=FACE_OUTER_BOUND('',#10234,.T.);
#6663=FACE_OUTER_BOUND('',#10235,.T.);
#6664=FACE_OUTER_BOUND('',#10236,.T.);
#6665=FACE_OUTER_BOUND('',#10237,.T.);
#6666=FACE_OUTER_BOUND('',#10238,.T.);
#6667=FACE_OUTER_BOUND('',#10239,.T.);
#6668=FACE_OUTER_BOUND('',#10240,.T.);
#6669=FACE_OUTER_BOUND('',#10241,.T.);
#6670=FACE_OUTER_BOUND('',#10242,.T.);
#6671=FACE_OUTER_BOUND('',#10243,.T.);
#6672=FACE_OUTER_BOUND('',#10244,.T.);
#6673=FACE_OUTER_BOUND('',#10245,.T.);
#6674=FACE_OUTER_BOUND('',#10246,.T.);
#6675=FACE_OUTER_BOUND('',#10247,.T.);
#6676=FACE_OUTER_BOUND('',#10248,.T.);
#6677=FACE_OUTER_BOUND('',#10249,.T.);
#6678=FACE_OUTER_BOUND('',#10250,.T.);
#6679=FACE_OUTER_BOUND('',#10251,.T.);
#6680=FACE_OUTER_BOUND('',#10252,.T.);
#6681=FACE_OUTER_BOUND('',#10253,.T.);
#6682=FACE_OUTER_BOUND('',#10254,.T.);
#6683=FACE_OUTER_BOUND('',#10255,.T.);
#6684=FACE_OUTER_BOUND('',#10256,.T.);
#6685=FACE_OUTER_BOUND('',#10257,.T.);
#6686=FACE_OUTER_BOUND('',#10258,.T.);
#6687=FACE_OUTER_BOUND('',#10259,.T.);
#6688=FACE_OUTER_BOUND('',#10260,.T.);
#6689=FACE_OUTER_BOUND('',#10261,.T.);
#6690=FACE_OUTER_BOUND('',#10262,.T.);
#6691=FACE_OUTER_BOUND('',#10263,.T.);
#6692=FACE_OUTER_BOUND('',#10264,.T.);
#6693=FACE_OUTER_BOUND('',#10265,.T.);
#6694=FACE_OUTER_BOUND('',#10266,.T.);
#6695=FACE_OUTER_BOUND('',#10267,.T.);
#6696=FACE_OUTER_BOUND('',#10268,.T.);
#6697=FACE_OUTER_BOUND('',#10269,.T.);
#6698=FACE_OUTER_BOUND('',#10270,.T.);
#6699=FACE_OUTER_BOUND('',#10271,.T.);
#6700=FACE_OUTER_BOUND('',#10272,.T.);
#6701=FACE_OUTER_BOUND('',#10273,.T.);
#6702=FACE_OUTER_BOUND('',#10274,.T.);
#6703=FACE_OUTER_BOUND('',#10275,.T.);
#6704=FACE_OUTER_BOUND('',#10276,.T.);
#6705=FACE_OUTER_BOUND('',#10277,.T.);
#6706=FACE_OUTER_BOUND('',#10278,.T.);
#6707=FACE_OUTER_BOUND('',#10279,.T.);
#6708=FACE_OUTER_BOUND('',#10280,.T.);
#6709=FACE_OUTER_BOUND('',#10281,.T.);
#6710=FACE_OUTER_BOUND('',#10282,.T.);
#6711=FACE_OUTER_BOUND('',#10283,.T.);
#6712=FACE_OUTER_BOUND('',#10284,.T.);
#6713=FACE_OUTER_BOUND('',#10285,.T.);
#6714=FACE_OUTER_BOUND('',#10286,.T.);
#6715=FACE_OUTER_BOUND('',#10287,.T.);
#6716=FACE_OUTER_BOUND('',#10288,.T.);
#6717=FACE_OUTER_BOUND('',#10289,.T.);
#6718=FACE_OUTER_BOUND('',#10290,.T.);
#6719=FACE_OUTER_BOUND('',#10291,.T.);
#6720=FACE_OUTER_BOUND('',#10292,.T.);
#6721=FACE_OUTER_BOUND('',#10293,.T.);
#6722=FACE_OUTER_BOUND('',#10294,.T.);
#6723=FACE_OUTER_BOUND('',#10295,.T.);
#6724=FACE_OUTER_BOUND('',#10296,.T.);
#6725=FACE_OUTER_BOUND('',#10297,.T.);
#6726=FACE_OUTER_BOUND('',#10298,.T.);
#6727=FACE_OUTER_BOUND('',#10299,.T.);
#6728=FACE_OUTER_BOUND('',#10300,.T.);
#6729=FACE_OUTER_BOUND('',#10301,.T.);
#6730=FACE_OUTER_BOUND('',#10302,.T.);
#6731=FACE_OUTER_BOUND('',#10303,.T.);
#6732=FACE_OUTER_BOUND('',#10304,.T.);
#6733=FACE_OUTER_BOUND('',#10305,.T.);
#6734=FACE_OUTER_BOUND('',#10306,.T.);
#6735=FACE_OUTER_BOUND('',#10307,.T.);
#6736=FACE_OUTER_BOUND('',#10308,.T.);
#6737=FACE_OUTER_BOUND('',#10309,.T.);
#6738=FACE_OUTER_BOUND('',#10310,.T.);
#6739=FACE_OUTER_BOUND('',#10311,.T.);
#6740=FACE_OUTER_BOUND('',#10312,.T.);
#6741=FACE_OUTER_BOUND('',#10313,.T.);
#6742=FACE_OUTER_BOUND('',#10314,.T.);
#6743=FACE_OUTER_BOUND('',#10315,.T.);
#6744=FACE_OUTER_BOUND('',#10316,.T.);
#6745=FACE_OUTER_BOUND('',#10317,.T.);
#6746=FACE_OUTER_BOUND('',#10318,.T.);
#6747=FACE_OUTER_BOUND('',#10319,.T.);
#6748=FACE_OUTER_BOUND('',#10320,.T.);
#9799=EDGE_LOOP('',(#50433,#50434,#50435,#50436));
#9800=EDGE_LOOP('',(#50437,#50438,#50439,#50440));
#9801=EDGE_LOOP('',(#50441,#50442,#50443,#50444));
#9802=EDGE_LOOP('',(#50445));
#9803=EDGE_LOOP('',(#50446,#50447,#50448,#50449));
#9804=EDGE_LOOP('',(#50450,#50451,#50452,#50453));
#9805=EDGE_LOOP('',(#50454,#50455,#50456,#50457));
#9806=EDGE_LOOP('',(#50458));
#9807=EDGE_LOOP('',(#50459));
#9808=EDGE_LOOP('',(#50460));
#9809=EDGE_LOOP('',(#50461));
#9810=EDGE_LOOP('',(#50462));
#9811=EDGE_LOOP('',(#50463,#50464,#50465,#50466));
#9812=EDGE_LOOP('',(#50467,#50468,#50469,#50470));
#9813=EDGE_LOOP('',(#50471,#50472,#50473,#50474));
#9814=EDGE_LOOP('',(#50475,#50476,#50477,#50478,#50479,#50480));
#9815=EDGE_LOOP('',(#50481,#50482,#50483,#50484));
#9816=EDGE_LOOP('',(#50485));
#9817=EDGE_LOOP('',(#50486));
#9818=EDGE_LOOP('',(#50487,#50488,#50489,#50490));
#9819=EDGE_LOOP('',(#50491,#50492,#50493,#50494));
#9820=EDGE_LOOP('',(#50495,#50496,#50497,#50498));
#9821=EDGE_LOOP('',(#50499,#50500,#50501,#50502));
#9822=EDGE_LOOP('',(#50503,#50504,#50505,#50506));
#9823=EDGE_LOOP('',(#50507,#50508,#50509,#50510));
#9824=EDGE_LOOP('',(#50511,#50512,#50513,#50514));
#9825=EDGE_LOOP('',(#50515,#50516,#50517,#50518));
#9826=EDGE_LOOP('',(#50519,#50520,#50521,#50522));
#9827=EDGE_LOOP('',(#50523,#50524,#50525,#50526));
#9828=EDGE_LOOP('',(#50527,#50528,#50529,#50530));
#9829=EDGE_LOOP('',(#50531,#50532,#50533,#50534));
#9830=EDGE_LOOP('',(#50535,#50536,#50537,#50538));
#9831=EDGE_LOOP('',(#50539,#50540,#50541,#50542));
#9832=EDGE_LOOP('',(#50543,#50544,#50545,#50546));
#9833=EDGE_LOOP('',(#50547,#50548,#50549,#50550));
#9834=EDGE_LOOP('',(#50551,#50552,#50553,#50554));
#9835=EDGE_LOOP('',(#50555,#50556,#50557,#50558));
#9836=EDGE_LOOP('',(#50559,#50560,#50561,#50562));
#9837=EDGE_LOOP('',(#50563,#50564,#50565,#50566));
#9838=EDGE_LOOP('',(#50567,#50568,#50569,#50570));
#9839=EDGE_LOOP('',(#50571,#50572,#50573,#50574));
#9840=EDGE_LOOP('',(#50575,#50576,#50577,#50578));
#9841=EDGE_LOOP('',(#50579,#50580,#50581,#50582));
#9842=EDGE_LOOP('',(#50583,#50584,#50585,#50586));
#9843=EDGE_LOOP('',(#50587,#50588,#50589,#50590));
#9844=EDGE_LOOP('',(#50591,#50592,#50593,#50594));
#9845=EDGE_LOOP('',(#50595,#50596,#50597,#50598));
#9846=EDGE_LOOP('',(#50599,#50600,#50601,#50602));
#9847=EDGE_LOOP('',(#50603,#50604,#50605,#50606));
#9848=EDGE_LOOP('',(#50607,#50608,#50609,#50610));
#9849=EDGE_LOOP('',(#50611,#50612,#50613,#50614));
#9850=EDGE_LOOP('',(#50615,#50616,#50617,#50618));
#9851=EDGE_LOOP('',(#50619,#50620,#50621,#50622));
#9852=EDGE_LOOP('',(#50623,#50624,#50625,#50626));
#9853=EDGE_LOOP('',(#50627,#50628,#50629,#50630));
#9854=EDGE_LOOP('',(#50631,#50632,#50633,#50634));
#9855=EDGE_LOOP('',(#50635,#50636,#50637,#50638));
#9856=EDGE_LOOP('',(#50639,#50640,#50641,#50642));
#9857=EDGE_LOOP('',(#50643,#50644,#50645,#50646));
#9858=EDGE_LOOP('',(#50647,#50648,#50649,#50650));
#9859=EDGE_LOOP('',(#50651,#50652,#50653,#50654));
#9860=EDGE_LOOP('',(#50655,#50656,#50657,#50658));
#9861=EDGE_LOOP('',(#50659,#50660,#50661,#50662));
#9862=EDGE_LOOP('',(#50663,#50664,#50665,#50666));
#9863=EDGE_LOOP('',(#50667,#50668,#50669,#50670));
#9864=EDGE_LOOP('',(#50671,#50672,#50673,#50674));
#9865=EDGE_LOOP('',(#50675,#50676,#50677,#50678));
#9866=EDGE_LOOP('',(#50679,#50680,#50681,#50682));
#9867=EDGE_LOOP('',(#50683,#50684,#50685,#50686));
#9868=EDGE_LOOP('',(#50687,#50688,#50689,#50690));
#9869=EDGE_LOOP('',(#50691,#50692,#50693,#50694));
#9870=EDGE_LOOP('',(#50695,#50696,#50697,#50698));
#9871=EDGE_LOOP('',(#50699,#50700,#50701,#50702));
#9872=EDGE_LOOP('',(#50703,#50704,#50705,#50706));
#9873=EDGE_LOOP('',(#50707,#50708,#50709,#50710));
#9874=EDGE_LOOP('',(#50711,#50712,#50713,#50714));
#9875=EDGE_LOOP('',(#50715,#50716,#50717,#50718));
#9876=EDGE_LOOP('',(#50719,#50720,#50721,#50722));
#9877=EDGE_LOOP('',(#50723,#50724,#50725,#50726));
#9878=EDGE_LOOP('',(#50727,#50728,#50729,#50730));
#9879=EDGE_LOOP('',(#50731,#50732,#50733,#50734));
#9880=EDGE_LOOP('',(#50735,#50736,#50737,#50738));
#9881=EDGE_LOOP('',(#50739,#50740,#50741,#50742));
#9882=EDGE_LOOP('',(#50743,#50744,#50745,#50746));
#9883=EDGE_LOOP('',(#50747,#50748,#50749,#50750));
#9884=EDGE_LOOP('',(#50751,#50752,#50753,#50754));
#9885=EDGE_LOOP('',(#50755,#50756,#50757,#50758));
#9886=EDGE_LOOP('',(#50759,#50760,#50761,#50762));
#9887=EDGE_LOOP('',(#50763,#50764,#50765,#50766));
#9888=EDGE_LOOP('',(#50767,#50768,#50769,#50770));
#9889=EDGE_LOOP('',(#50771,#50772,#50773,#50774));
#9890=EDGE_LOOP('',(#50775,#50776,#50777,#50778));
#9891=EDGE_LOOP('',(#50779,#50780,#50781,#50782));
#9892=EDGE_LOOP('',(#50783,#50784,#50785,#50786));
#9893=EDGE_LOOP('',(#50787,#50788,#50789,#50790));
#9894=EDGE_LOOP('',(#50791,#50792,#50793,#50794));
#9895=EDGE_LOOP('',(#50795,#50796,#50797,#50798));
#9896=EDGE_LOOP('',(#50799,#50800,#50801,#50802));
#9897=EDGE_LOOP('',(#50803,#50804,#50805,#50806));
#9898=EDGE_LOOP('',(#50807,#50808,#50809,#50810));
#9899=EDGE_LOOP('',(#50811,#50812,#50813,#50814));
#9900=EDGE_LOOP('',(#50815,#50816,#50817,#50818));
#9901=EDGE_LOOP('',(#50819,#50820,#50821,#50822));
#9902=EDGE_LOOP('',(#50823,#50824,#50825,#50826));
#9903=EDGE_LOOP('',(#50827,#50828,#50829,#50830));
#9904=EDGE_LOOP('',(#50831,#50832,#50833,#50834));
#9905=EDGE_LOOP('',(#50835,#50836,#50837,#50838));
#9906=EDGE_LOOP('',(#50839,#50840,#50841,#50842));
#9907=EDGE_LOOP('',(#50843,#50844,#50845,#50846));
#9908=EDGE_LOOP('',(#50847,#50848,#50849,#50850));
#9909=EDGE_LOOP('',(#50851,#50852,#50853,#50854));
#9910=EDGE_LOOP('',(#50855,#50856,#50857,#50858));
#9911=EDGE_LOOP('',(#50859,#50860,#50861,#50862));
#9912=EDGE_LOOP('',(#50863,#50864,#50865,#50866));
#9913=EDGE_LOOP('',(#50867,#50868,#50869,#50870));
#9914=EDGE_LOOP('',(#50871,#50872,#50873,#50874));
#9915=EDGE_LOOP('',(#50875,#50876,#50877,#50878));
#9916=EDGE_LOOP('',(#50879,#50880,#50881,#50882));
#9917=EDGE_LOOP('',(#50883,#50884,#50885,#50886));
#9918=EDGE_LOOP('',(#50887,#50888,#50889,#50890));
#9919=EDGE_LOOP('',(#50891,#50892,#50893,#50894));
#9920=EDGE_LOOP('',(#50895,#50896,#50897,#50898));
#9921=EDGE_LOOP('',(#50899,#50900,#50901,#50902));
#9922=EDGE_LOOP('',(#50903,#50904,#50905,#50906));
#9923=EDGE_LOOP('',(#50907,#50908,#50909,#50910));
#9924=EDGE_LOOP('',(#50911,#50912,#50913,#50914));
#9925=EDGE_LOOP('',(#50915,#50916,#50917,#50918));
#9926=EDGE_LOOP('',(#50919,#50920,#50921,#50922));
#9927=EDGE_LOOP('',(#50923,#50924,#50925,#50926));
#9928=EDGE_LOOP('',(#50927,#50928,#50929,#50930));
#9929=EDGE_LOOP('',(#50931,#50932,#50933,#50934));
#9930=EDGE_LOOP('',(#50935,#50936,#50937,#50938));
#9931=EDGE_LOOP('',(#50939,#50940,#50941,#50942));
#9932=EDGE_LOOP('',(#50943,#50944,#50945,#50946));
#9933=EDGE_LOOP('',(#50947,#50948,#50949,#50950));
#9934=EDGE_LOOP('',(#50951,#50952,#50953,#50954));
#9935=EDGE_LOOP('',(#50955,#50956,#50957,#50958));
#9936=EDGE_LOOP('',(#50959,#50960,#50961,#50962));
#9937=EDGE_LOOP('',(#50963,#50964,#50965,#50966));
#9938=EDGE_LOOP('',(#50967,#50968,#50969,#50970));
#9939=EDGE_LOOP('',(#50971,#50972,#50973,#50974));
#9940=EDGE_LOOP('',(#50975,#50976,#50977,#50978));
#9941=EDGE_LOOP('',(#50979,#50980,#50981,#50982));
#9942=EDGE_LOOP('',(#50983,#50984,#50985,#50986));
#9943=EDGE_LOOP('',(#50987,#50988,#50989,#50990));
#9944=EDGE_LOOP('',(#50991,#50992,#50993,#50994));
#9945=EDGE_LOOP('',(#50995,#50996,#50997,#50998));
#9946=EDGE_LOOP('',(#50999,#51000,#51001,#51002));
#9947=EDGE_LOOP('',(#51003,#51004,#51005,#51006));
#9948=EDGE_LOOP('',(#51007,#51008,#51009,#51010));
#9949=EDGE_LOOP('',(#51011,#51012,#51013,#51014));
#9950=EDGE_LOOP('',(#51015,#51016,#51017,#51018));
#9951=EDGE_LOOP('',(#51019,#51020,#51021,#51022));
#9952=EDGE_LOOP('',(#51023,#51024,#51025,#51026));
#9953=EDGE_LOOP('',(#51027,#51028,#51029,#51030));
#9954=EDGE_LOOP('',(#51031,#51032,#51033,#51034));
#9955=EDGE_LOOP('',(#51035,#51036,#51037,#51038));
#9956=EDGE_LOOP('',(#51039,#51040,#51041,#51042));
#9957=EDGE_LOOP('',(#51043,#51044,#51045,#51046));
#9958=EDGE_LOOP('',(#51047,#51048,#51049,#51050));
#9959=EDGE_LOOP('',(#51051,#51052,#51053,#51054));
#9960=EDGE_LOOP('',(#51055,#51056,#51057,#51058));
#9961=EDGE_LOOP('',(#51059,#51060,#51061,#51062));
#9962=EDGE_LOOP('',(#51063,#51064,#51065,#51066));
#9963=EDGE_LOOP('',(#51067,#51068,#51069,#51070));
#9964=EDGE_LOOP('',(#51071,#51072,#51073,#51074));
#9965=EDGE_LOOP('',(#51075,#51076,#51077,#51078));
#9966=EDGE_LOOP('',(#51079,#51080,#51081,#51082));
#9967=EDGE_LOOP('',(#51083,#51084,#51085,#51086));
#9968=EDGE_LOOP('',(#51087,#51088,#51089,#51090));
#9969=EDGE_LOOP('',(#51091,#51092,#51093,#51094));
#9970=EDGE_LOOP('',(#51095,#51096,#51097,#51098));
#9971=EDGE_LOOP('',(#51099,#51100,#51101,#51102));
#9972=EDGE_LOOP('',(#51103,#51104,#51105,#51106));
#9973=EDGE_LOOP('',(#51107,#51108,#51109,#51110));
#9974=EDGE_LOOP('',(#51111,#51112,#51113,#51114));
#9975=EDGE_LOOP('',(#51115,#51116,#51117,#51118));
#9976=EDGE_LOOP('',(#51119,#51120,#51121,#51122));
#9977=EDGE_LOOP('',(#51123,#51124,#51125,#51126));
#9978=EDGE_LOOP('',(#51127,#51128,#51129,#51130));
#9979=EDGE_LOOP('',(#51131,#51132,#51133,#51134));
#9980=EDGE_LOOP('',(#51135,#51136,#51137,#51138));
#9981=EDGE_LOOP('',(#51139,#51140,#51141,#51142));
#9982=EDGE_LOOP('',(#51143,#51144,#51145,#51146));
#9983=EDGE_LOOP('',(#51147,#51148,#51149,#51150));
#9984=EDGE_LOOP('',(#51151,#51152,#51153,#51154));
#9985=EDGE_LOOP('',(#51155,#51156,#51157,#51158));
#9986=EDGE_LOOP('',(#51159,#51160,#51161,#51162));
#9987=EDGE_LOOP('',(#51163,#51164,#51165,#51166));
#9988=EDGE_LOOP('',(#51167,#51168,#51169,#51170));
#9989=EDGE_LOOP('',(#51171,#51172,#51173,#51174));
#9990=EDGE_LOOP('',(#51175,#51176,#51177,#51178));
#9991=EDGE_LOOP('',(#51179,#51180,#51181,#51182));
#9992=EDGE_LOOP('',(#51183,#51184,#51185,#51186));
#9993=EDGE_LOOP('',(#51187,#51188,#51189,#51190));
#9994=EDGE_LOOP('',(#51191,#51192,#51193,#51194));
#9995=EDGE_LOOP('',(#51195,#51196,#51197,#51198));
#9996=EDGE_LOOP('',(#51199,#51200,#51201,#51202));
#9997=EDGE_LOOP('',(#51203,#51204,#51205,#51206));
#9998=EDGE_LOOP('',(#51207,#51208,#51209,#51210));
#9999=EDGE_LOOP('',(#51211,#51212,#51213,#51214));
#10000=EDGE_LOOP('',(#51215,#51216,#51217,#51218));
#10001=EDGE_LOOP('',(#51219,#51220,#51221,#51222));
#10002=EDGE_LOOP('',(#51223,#51224,#51225,#51226));
#10003=EDGE_LOOP('',(#51227,#51228,#51229,#51230));
#10004=EDGE_LOOP('',(#51231,#51232,#51233,#51234));
#10005=EDGE_LOOP('',(#51235,#51236,#51237,#51238));
#10006=EDGE_LOOP('',(#51239,#51240,#51241,#51242));
#10007=EDGE_LOOP('',(#51243,#51244,#51245,#51246));
#10008=EDGE_LOOP('',(#51247,#51248,#51249,#51250));
#10009=EDGE_LOOP('',(#51251,#51252,#51253,#51254));
#10010=EDGE_LOOP('',(#51255,#51256,#51257,#51258));
#10011=EDGE_LOOP('',(#51259,#51260,#51261,#51262));
#10012=EDGE_LOOP('',(#51263,#51264,#51265,#51266));
#10013=EDGE_LOOP('',(#51267,#51268,#51269,#51270));
#10014=EDGE_LOOP('',(#51271,#51272,#51273,#51274));
#10015=EDGE_LOOP('',(#51275,#51276,#51277,#51278));
#10016=EDGE_LOOP('',(#51279,#51280,#51281,#51282));
#10017=EDGE_LOOP('',(#51283,#51284,#51285,#51286));
#10018=EDGE_LOOP('',(#51287,#51288,#51289,#51290));
#10019=EDGE_LOOP('',(#51291,#51292,#51293,#51294));
#10020=EDGE_LOOP('',(#51295,#51296,#51297,#51298));
#10021=EDGE_LOOP('',(#51299,#51300,#51301,#51302));
#10022=EDGE_LOOP('',(#51303,#51304,#51305,#51306));
#10023=EDGE_LOOP('',(#51307,#51308,#51309,#51310));
#10024=EDGE_LOOP('',(#51311,#51312,#51313,#51314));
#10025=EDGE_LOOP('',(#51315,#51316,#51317,#51318));
#10026=EDGE_LOOP('',(#51319,#51320,#51321,#51322));
#10027=EDGE_LOOP('',(#51323,#51324,#51325,#51326));
#10028=EDGE_LOOP('',(#51327,#51328,#51329,#51330));
#10029=EDGE_LOOP('',(#51331,#51332,#51333,#51334));
#10030=EDGE_LOOP('',(#51335,#51336,#51337,#51338));
#10031=EDGE_LOOP('',(#51339,#51340,#51341,#51342));
#10032=EDGE_LOOP('',(#51343,#51344,#51345,#51346));
#10033=EDGE_LOOP('',(#51347,#51348,#51349,#51350));
#10034=EDGE_LOOP('',(#51351,#51352,#51353,#51354));
#10035=EDGE_LOOP('',(#51355,#51356,#51357,#51358));
#10036=EDGE_LOOP('',(#51359,#51360,#51361,#51362));
#10037=EDGE_LOOP('',(#51363,#51364,#51365,#51366));
#10038=EDGE_LOOP('',(#51367,#51368,#51369,#51370));
#10039=EDGE_LOOP('',(#51371,#51372,#51373,#51374));
#10040=EDGE_LOOP('',(#51375,#51376,#51377,#51378));
#10041=EDGE_LOOP('',(#51379,#51380,#51381,#51382));
#10042=EDGE_LOOP('',(#51383,#51384,#51385,#51386));
#10043=EDGE_LOOP('',(#51387,#51388,#51389,#51390));
#10044=EDGE_LOOP('',(#51391,#51392,#51393,#51394));
#10045=EDGE_LOOP('',(#51395,#51396,#51397,#51398));
#10046=EDGE_LOOP('',(#51399,#51400,#51401,#51402));
#10047=EDGE_LOOP('',(#51403,#51404,#51405,#51406));
#10048=EDGE_LOOP('',(#51407,#51408,#51409,#51410));
#10049=EDGE_LOOP('',(#51411,#51412,#51413,#51414));
#10050=EDGE_LOOP('',(#51415,#51416,#51417,#51418));
#10051=EDGE_LOOP('',(#51419,#51420,#51421,#51422));
#10052=EDGE_LOOP('',(#51423,#51424,#51425,#51426));
#10053=EDGE_LOOP('',(#51427,#51428,#51429,#51430));
#10054=EDGE_LOOP('',(#51431,#51432,#51433,#51434));
#10055=EDGE_LOOP('',(#51435,#51436,#51437,#51438));
#10056=EDGE_LOOP('',(#51439,#51440,#51441,#51442));
#10057=EDGE_LOOP('',(#51443,#51444,#51445,#51446));
#10058=EDGE_LOOP('',(#51447,#51448,#51449,#51450));
#10059=EDGE_LOOP('',(#51451,#51452,#51453,#51454));
#10060=EDGE_LOOP('',(#51455,#51456,#51457,#51458));
#10061=EDGE_LOOP('',(#51459,#51460,#51461,#51462));
#10062=EDGE_LOOP('',(#51463,#51464,#51465,#51466));
#10063=EDGE_LOOP('',(#51467,#51468,#51469,#51470));
#10064=EDGE_LOOP('',(#51471,#51472,#51473,#51474));
#10065=EDGE_LOOP('',(#51475,#51476,#51477,#51478));
#10066=EDGE_LOOP('',(#51479,#51480,#51481,#51482));
#10067=EDGE_LOOP('',(#51483,#51484,#51485,#51486));
#10068=EDGE_LOOP('',(#51487,#51488,#51489,#51490));
#10069=EDGE_LOOP('',(#51491,#51492,#51493,#51494));
#10070=EDGE_LOOP('',(#51495,#51496,#51497,#51498));
#10071=EDGE_LOOP('',(#51499,#51500,#51501,#51502));
#10072=EDGE_LOOP('',(#51503,#51504,#51505,#51506));
#10073=EDGE_LOOP('',(#51507,#51508,#51509,#51510));
#10074=EDGE_LOOP('',(#51511,#51512,#51513,#51514));
#10075=EDGE_LOOP('',(#51515,#51516,#51517,#51518));
#10076=EDGE_LOOP('',(#51519,#51520,#51521,#51522));
#10077=EDGE_LOOP('',(#51523,#51524,#51525,#51526));
#10078=EDGE_LOOP('',(#51527,#51528,#51529,#51530));
#10079=EDGE_LOOP('',(#51531,#51532,#51533,#51534));
#10080=EDGE_LOOP('',(#51535,#51536,#51537,#51538));
#10081=EDGE_LOOP('',(#51539,#51540,#51541,#51542));
#10082=EDGE_LOOP('',(#51543,#51544,#51545,#51546));
#10083=EDGE_LOOP('',(#51547,#51548,#51549,#51550));
#10084=EDGE_LOOP('',(#51551,#51552,#51553,#51554));
#10085=EDGE_LOOP('',(#51555,#51556,#51557,#51558));
#10086=EDGE_LOOP('',(#51559,#51560,#51561,#51562));
#10087=EDGE_LOOP('',(#51563,#51564,#51565,#51566));
#10088=EDGE_LOOP('',(#51567,#51568,#51569,#51570));
#10089=EDGE_LOOP('',(#51571,#51572,#51573,#51574));
#10090=EDGE_LOOP('',(#51575,#51576,#51577,#51578));
#10091=EDGE_LOOP('',(#51579,#51580,#51581,#51582));
#10092=EDGE_LOOP('',(#51583,#51584,#51585,#51586));
#10093=EDGE_LOOP('',(#51587,#51588,#51589,#51590));
#10094=EDGE_LOOP('',(#51591,#51592,#51593,#51594));
#10095=EDGE_LOOP('',(#51595,#51596,#51597,#51598));
#10096=EDGE_LOOP('',(#51599,#51600,#51601,#51602));
#10097=EDGE_LOOP('',(#51603,#51604,#51605,#51606));
#10098=EDGE_LOOP('',(#51607,#51608,#51609,#51610));
#10099=EDGE_LOOP('',(#51611,#51612,#51613,#51614));
#10100=EDGE_LOOP('',(#51615,#51616,#51617,#51618));
#10101=EDGE_LOOP('',(#51619,#51620,#51621,#51622));
#10102=EDGE_LOOP('',(#51623,#51624,#51625,#51626));
#10103=EDGE_LOOP('',(#51627,#51628,#51629,#51630));
#10104=EDGE_LOOP('',(#51631,#51632,#51633,#51634));
#10105=EDGE_LOOP('',(#51635,#51636,#51637,#51638));
#10106=EDGE_LOOP('',(#51639,#51640,#51641,#51642));
#10107=EDGE_LOOP('',(#51643,#51644,#51645,#51646));
#10108=EDGE_LOOP('',(#51647,#51648,#51649,#51650));
#10109=EDGE_LOOP('',(#51651,#51652,#51653,#51654));
#10110=EDGE_LOOP('',(#51655,#51656,#51657,#51658));
#10111=EDGE_LOOP('',(#51659,#51660,#51661,#51662));
#10112=EDGE_LOOP('',(#51663,#51664,#51665,#51666));
#10113=EDGE_LOOP('',(#51667,#51668,#51669,#51670));
#10114=EDGE_LOOP('',(#51671,#51672,#51673,#51674));
#10115=EDGE_LOOP('',(#51675,#51676,#51677,#51678));
#10116=EDGE_LOOP('',(#51679,#51680,#51681,#51682));
#10117=EDGE_LOOP('',(#51683,#51684,#51685,#51686));
#10118=EDGE_LOOP('',(#51687,#51688,#51689,#51690));
#10119=EDGE_LOOP('',(#51691,#51692,#51693,#51694));
#10120=EDGE_LOOP('',(#51695,#51696,#51697,#51698));
#10121=EDGE_LOOP('',(#51699,#51700,#51701,#51702));
#10122=EDGE_LOOP('',(#51703,#51704,#51705,#51706));
#10123=EDGE_LOOP('',(#51707,#51708,#51709,#51710));
#10124=EDGE_LOOP('',(#51711,#51712,#51713,#51714));
#10125=EDGE_LOOP('',(#51715,#51716,#51717,#51718));
#10126=EDGE_LOOP('',(#51719,#51720,#51721,#51722));
#10127=EDGE_LOOP('',(#51723,#51724,#51725,#51726));
#10128=EDGE_LOOP('',(#51727,#51728,#51729,#51730));
#10129=EDGE_LOOP('',(#51731,#51732,#51733,#51734));
#10130=EDGE_LOOP('',(#51735,#51736,#51737,#51738));
#10131=EDGE_LOOP('',(#51739,#51740,#51741,#51742));
#10132=EDGE_LOOP('',(#51743,#51744,#51745,#51746));
#10133=EDGE_LOOP('',(#51747,#51748,#51749,#51750));
#10134=EDGE_LOOP('',(#51751,#51752,#51753,#51754));
#10135=EDGE_LOOP('',(#51755,#51756,#51757,#51758));
#10136=EDGE_LOOP('',(#51759,#51760,#51761,#51762));
#10137=EDGE_LOOP('',(#51763,#51764,#51765,#51766));
#10138=EDGE_LOOP('',(#51767,#51768,#51769,#51770));
#10139=EDGE_LOOP('',(#51771,#51772,#51773,#51774));
#10140=EDGE_LOOP('',(#51775,#51776,#51777,#51778));
#10141=EDGE_LOOP('',(#51779,#51780,#51781,#51782));
#10142=EDGE_LOOP('',(#51783,#51784,#51785,#51786));
#10143=EDGE_LOOP('',(#51787,#51788,#51789,#51790));
#10144=EDGE_LOOP('',(#51791,#51792,#51793,#51794));
#10145=EDGE_LOOP('',(#51795,#51796,#51797,#51798));
#10146=EDGE_LOOP('',(#51799,#51800,#51801,#51802));
#10147=EDGE_LOOP('',(#51803,#51804,#51805,#51806));
#10148=EDGE_LOOP('',(#51807,#51808,#51809,#51810));
#10149=EDGE_LOOP('',(#51811,#51812,#51813,#51814));
#10150=EDGE_LOOP('',(#51815,#51816,#51817,#51818));
#10151=EDGE_LOOP('',(#51819,#51820,#51821,#51822));
#10152=EDGE_LOOP('',(#51823,#51824,#51825,#51826));
#10153=EDGE_LOOP('',(#51827,#51828,#51829,#51830));
#10154=EDGE_LOOP('',(#51831,#51832,#51833,#51834));
#10155=EDGE_LOOP('',(#51835,#51836,#51837,#51838));
#10156=EDGE_LOOP('',(#51839,#51840,#51841,#51842));
#10157=EDGE_LOOP('',(#51843,#51844,#51845,#51846));
#10158=EDGE_LOOP('',(#51847,#51848,#51849,#51850));
#10159=EDGE_LOOP('',(#51851,#51852,#51853,#51854));
#10160=EDGE_LOOP('',(#51855,#51856,#51857,#51858));
#10161=EDGE_LOOP('',(#51859,#51860,#51861,#51862));
#10162=EDGE_LOOP('',(#51863,#51864,#51865,#51866));
#10163=EDGE_LOOP('',(#51867,#51868,#51869,#51870));
#10164=EDGE_LOOP('',(#51871,#51872,#51873,#51874));
#10165=EDGE_LOOP('',(#51875,#51876,#51877,#51878));
#10166=EDGE_LOOP('',(#51879,#51880,#51881,#51882));
#10167=EDGE_LOOP('',(#51883,#51884,#51885,#51886));
#10168=EDGE_LOOP('',(#51887,#51888,#51889,#51890));
#10169=EDGE_LOOP('',(#51891,#51892,#51893,#51894));
#10170=EDGE_LOOP('',(#51895,#51896,#51897,#51898));
#10171=EDGE_LOOP('',(#51899,#51900,#51901,#51902));
#10172=EDGE_LOOP('',(#51903,#51904,#51905,#51906));
#10173=EDGE_LOOP('',(#51907,#51908,#51909,#51910));
#10174=EDGE_LOOP('',(#51911,#51912,#51913,#51914));
#10175=EDGE_LOOP('',(#51915,#51916,#51917,#51918));
#10176=EDGE_LOOP('',(#51919,#51920,#51921,#51922));
#10177=EDGE_LOOP('',(#51923,#51924,#51925,#51926));
#10178=EDGE_LOOP('',(#51927,#51928,#51929,#51930));
#10179=EDGE_LOOP('',(#51931,#51932,#51933,#51934));
#10180=EDGE_LOOP('',(#51935,#51936,#51937,#51938));
#10181=EDGE_LOOP('',(#51939,#51940,#51941,#51942));
#10182=EDGE_LOOP('',(#51943,#51944,#51945,#51946));
#10183=EDGE_LOOP('',(#51947,#51948,#51949,#51950));
#10184=EDGE_LOOP('',(#51951,#51952,#51953,#51954));
#10185=EDGE_LOOP('',(#51955,#51956,#51957,#51958));
#10186=EDGE_LOOP('',(#51959,#51960,#51961,#51962));
#10187=EDGE_LOOP('',(#51963,#51964,#51965,#51966));
#10188=EDGE_LOOP('',(#51967,#51968,#51969,#51970));
#10189=EDGE_LOOP('',(#51971,#51972,#51973,#51974));
#10190=EDGE_LOOP('',(#51975,#51976,#51977,#51978));
#10191=EDGE_LOOP('',(#51979,#51980,#51981,#51982));
#10192=EDGE_LOOP('',(#51983,#51984,#51985,#51986));
#10193=EDGE_LOOP('',(#51987,#51988,#51989,#51990));
#10194=EDGE_LOOP('',(#51991,#51992,#51993,#51994));
#10195=EDGE_LOOP('',(#51995,#51996,#51997,#51998));
#10196=EDGE_LOOP('',(#51999,#52000,#52001,#52002));
#10197=EDGE_LOOP('',(#52003,#52004,#52005,#52006));
#10198=EDGE_LOOP('',(#52007,#52008,#52009,#52010));
#10199=EDGE_LOOP('',(#52011,#52012,#52013,#52014));
#10200=EDGE_LOOP('',(#52015,#52016,#52017,#52018));
#10201=EDGE_LOOP('',(#52019,#52020,#52021,#52022));
#10202=EDGE_LOOP('',(#52023,#52024,#52025,#52026));
#10203=EDGE_LOOP('',(#52027,#52028,#52029,#52030));
#10204=EDGE_LOOP('',(#52031,#52032,#52033,#52034));
#10205=EDGE_LOOP('',(#52035,#52036,#52037,#52038));
#10206=EDGE_LOOP('',(#52039,#52040,#52041,#52042));
#10207=EDGE_LOOP('',(#52043,#52044,#52045,#52046));
#10208=EDGE_LOOP('',(#52047,#52048,#52049,#52050));
#10209=EDGE_LOOP('',(#52051,#52052,#52053,#52054));
#10210=EDGE_LOOP('',(#52055,#52056,#52057,#52058));
#10211=EDGE_LOOP('',(#52059,#52060,#52061,#52062));
#10212=EDGE_LOOP('',(#52063,#52064,#52065,#52066));
#10213=EDGE_LOOP('',(#52067,#52068,#52069,#52070));
#10214=EDGE_LOOP('',(#52071,#52072,#52073,#52074));
#10215=EDGE_LOOP('',(#52075,#52076,#52077,#52078));
#10216=EDGE_LOOP('',(#52079,#52080,#52081,#52082));
#10217=EDGE_LOOP('',(#52083,#52084,#52085,#52086));
#10218=EDGE_LOOP('',(#52087,#52088,#52089,#52090));
#10219=EDGE_LOOP('',(#52091,#52092,#52093,#52094));
#10220=EDGE_LOOP('',(#52095,#52096,#52097,#52098));
#10221=EDGE_LOOP('',(#52099,#52100,#52101,#52102));
#10222=EDGE_LOOP('',(#52103,#52104,#52105,#52106));
#10223=EDGE_LOOP('',(#52107,#52108,#52109,#52110));
#10224=EDGE_LOOP('',(#52111,#52112,#52113,#52114));
#10225=EDGE_LOOP('',(#52115,#52116,#52117,#52118));
#10226=EDGE_LOOP('',(#52119,#52120,#52121,#52122));
#10227=EDGE_LOOP('',(#52123,#52124,#52125,#52126));
#10228=EDGE_LOOP('',(#52127,#52128,#52129,#52130));
#10229=EDGE_LOOP('',(#52131,#52132,#52133,#52134));
#10230=EDGE_LOOP('',(#52135,#52136,#52137,#52138));
#10231=EDGE_LOOP('',(#52139,#52140,#52141,#52142));
#10232=EDGE_LOOP('',(#52143,#52144,#52145,#52146));
#10233=EDGE_LOOP('',(#52147,#52148,#52149,#52150));
#10234=EDGE_LOOP('',(#52151,#52152,#52153,#52154));
#10235=EDGE_LOOP('',(#52155,#52156,#52157,#52158));
#10236=EDGE_LOOP('',(#52159,#52160,#52161,#52162));
#10237=EDGE_LOOP('',(#52163,#52164,#52165,#52166));
#10238=EDGE_LOOP('',(#52167,#52168,#52169,#52170));
#10239=EDGE_LOOP('',(#52171,#52172,#52173,#52174));
#10240=EDGE_LOOP('',(#52175,#52176,#52177,#52178));
#10241=EDGE_LOOP('',(#52179,#52180,#52181,#52182));
#10242=EDGE_LOOP('',(#52183,#52184,#52185,#52186));
#10243=EDGE_LOOP('',(#52187,#52188,#52189,#52190));
#10244=EDGE_LOOP('',(#52191,#52192,#52193,#52194));
#10245=EDGE_LOOP('',(#52195,#52196,#52197,#52198));
#10246=EDGE_LOOP('',(#52199,#52200,#52201,#52202));
#10247=EDGE_LOOP('',(#52203,#52204,#52205,#52206));
#10248=EDGE_LOOP('',(#52207,#52208,#52209,#52210));
#10249=EDGE_LOOP('',(#52211,#52212,#52213,#52214));
#10250=EDGE_LOOP('',(#52215,#52216,#52217,#52218));
#10251=EDGE_LOOP('',(#52219,#52220,#52221,#52222));
#10252=EDGE_LOOP('',(#52223,#52224,#52225,#52226));
#10253=EDGE_LOOP('',(#52227,#52228,#52229,#52230));
#10254=EDGE_LOOP('',(#52231,#52232,#52233,#52234));
#10255=EDGE_LOOP('',(#52235,#52236,#52237,#52238));
#10256=EDGE_LOOP('',(#52239,#52240,#52241,#52242));
#10257=EDGE_LOOP('',(#52243,#52244,#52245,#52246));
#10258=EDGE_LOOP('',(#52247,#52248,#52249,#52250));
#10259=EDGE_LOOP('',(#52251,#52252,#52253,#52254));
#10260=EDGE_LOOP('',(#52255,#52256,#52257,#52258));
#10261=EDGE_LOOP('',(#52259,#52260,#52261,#52262));
#10262=EDGE_LOOP('',(#52263,#52264,#52265,#52266));
#10263=EDGE_LOOP('',(#52267,#52268,#52269,#52270));
#10264=EDGE_LOOP('',(#52271,#52272,#52273,#52274));
#10265=EDGE_LOOP('',(#52275,#52276,#52277,#52278));
#10266=EDGE_LOOP('',(#52279,#52280,#52281,#52282));
#10267=EDGE_LOOP('',(#52283,#52284,#52285,#52286));
#10268=EDGE_LOOP('',(#52287,#52288,#52289,#52290));
#10269=EDGE_LOOP('',(#52291,#52292,#52293,#52294));
#10270=EDGE_LOOP('',(#52295,#52296,#52297,#52298));
#10271=EDGE_LOOP('',(#52299,#52300,#52301,#52302));
#10272=EDGE_LOOP('',(#52303,#52304,#52305,#52306));
#10273=EDGE_LOOP('',(#52307,#52308,#52309,#52310));
#10274=EDGE_LOOP('',(#52311,#52312,#52313,#52314));
#10275=EDGE_LOOP('',(#52315,#52316,#52317,#52318));
#10276=EDGE_LOOP('',(#52319,#52320,#52321,#52322));
#10277=EDGE_LOOP('',(#52323,#52324,#52325,#52326));
#10278=EDGE_LOOP('',(#52327,#52328,#52329,#52330));
#10279=EDGE_LOOP('',(#52331,#52332,#52333,#52334));
#10280=EDGE_LOOP('',(#52335,#52336,#52337,#52338));
#10281=EDGE_LOOP('',(#52339,#52340,#52341,#52342));
#10282=EDGE_LOOP('',(#52343,#52344,#52345,#52346));
#10283=EDGE_LOOP('',(#52347,#52348,#52349,#52350));
#10284=EDGE_LOOP('',(#52351,#52352,#52353,#52354));
#10285=EDGE_LOOP('',(#52355,#52356,#52357,#52358));
#10286=EDGE_LOOP('',(#52359,#52360,#52361,#52362));
#10287=EDGE_LOOP('',(#52363,#52364,#52365,#52366));
#10288=EDGE_LOOP('',(#52367,#52368,#52369,#52370));
#10289=EDGE_LOOP('',(#52371,#52372,#52373,#52374));
#10290=EDGE_LOOP('',(#52375,#52376,#52377,#52378));
#10291=EDGE_LOOP('',(#52379,#52380,#52381,#52382));
#10292=EDGE_LOOP('',(#52383,#52384,#52385,#52386));
#10293=EDGE_LOOP('',(#52387,#52388,#52389,#52390));
#10294=EDGE_LOOP('',(#52391,#52392,#52393,#52394));
#10295=EDGE_LOOP('',(#52395,#52396,#52397,#52398));
#10296=EDGE_LOOP('',(#52399,#52400,#52401,#52402));
#10297=EDGE_LOOP('',(#52403,#52404,#52405,#52406));
#10298=EDGE_LOOP('',(#52407,#52408,#52409,#52410));
#10299=EDGE_LOOP('',(#52411,#52412,#52413,#52414));
#10300=EDGE_LOOP('',(#52415,#52416,#52417,#52418));
#10301=EDGE_LOOP('',(#52419,#52420,#52421,#52422));
#10302=EDGE_LOOP('',(#52423,#52424,#52425,#52426));
#10303=EDGE_LOOP('',(#52427,#52428,#52429,#52430));
#10304=EDGE_LOOP('',(#52431,#52432,#52433,#52434));
#10305=EDGE_LOOP('',(#52435,#52436,#52437,#52438));
#10306=EDGE_LOOP('',(#52439,#52440,#52441,#52442));
#10307=EDGE_LOOP('',(#52443,#52444,#52445,#52446));
#10308=EDGE_LOOP('',(#52447,#52448,#52449,#52450));
#10309=EDGE_LOOP('',(#52451,#52452,#52453,#52454));
#10310=EDGE_LOOP('',(#52455,#52456,#52457,#52458));
#10311=EDGE_LOOP('',(#52459,#52460,#52461,#52462));
#10312=EDGE_LOOP('',(#52463,#52464,#52465,#52466));
#10313=EDGE_LOOP('',(#52467,#52468,#52469,#52470));
#10314=EDGE_LOOP('',(#52471,#52472,#52473,#52474));
#10315=EDGE_LOOP('',(#52475,#52476,#52477,#52478));
#10316=EDGE_LOOP('',(#52479,#52480,#52481,#52482));
#10317=EDGE_LOOP('',(#52483,#52484,#52485,#52486));
#10318=EDGE_LOOP('',(#52487,#52488,#52489,#52490,#52491,#52492));
#10319=EDGE_LOOP('',(#52493,#52494,#52495,#52496,#52497,#52498,#52499,#52500,
#52501,#52502,#52503,#52504,#52505,#52506,#52507,#52508,#52509,#52510,#52511,
#52512,#52513,#52514,#52515,#52516,#52517,#52518,#52519,#52520,#52521,#52522,
#52523,#52524,#52525,#52526,#52527,#52528,#52529,#52530,#52531,#52532,#52533,
#52534,#52535,#52536,#52537,#52538,#52539,#52540,#52541,#52542,#52543,#52544,
#52545,#52546,#52547,#52548,#52549,#52550,#52551,#52552,#52553,#52554,#52555,
#52556,#52557,#52558,#52559,#52560,#52561,#52562,#52563,#52564,#52565,#52566,
#52567,#52568,#52569,#52570,#52571,#52572,#52573,#52574,#52575,#52576,#52577,
#52578,#52579,#52580,#52581,#52582,#52583,#52584,#52585,#52586,#52587,#52588,
#52589,#52590,#52591,#52592,#52593,#52594,#52595,#52596,#52597,#52598,#52599,
#52600,#52601,#52602,#52603,#52604,#52605,#52606,#52607,#52608,#52609,#52610,
#52611,#52612,#52613,#52614,#52615,#52616,#52617,#52618,#52619,#52620,#52621,
#52622,#52623,#52624,#52625,#52626,#52627,#52628,#52629,#52630,#52631,#52632,
#52633,#52634,#52635,#52636,#52637,#52638,#52639,#52640,#52641,#52642,#52643,
#52644,#52645,#52646,#52647,#52648,#52649,#52650,#52651,#52652,#52653,#52654,
#52655,#52656,#52657,#52658,#52659,#52660,#52661,#52662,#52663,#52664,#52665,
#52666,#52667,#52668,#52669,#52670,#52671,#52672,#52673,#52674,#52675,#52676,
#52677,#52678,#52679,#52680,#52681,#52682,#52683,#52684,#52685,#52686,#52687,
#52688,#52689,#52690,#52691,#52692,#52693,#52694,#52695,#52696,#52697,#52698,
#52699,#52700,#52701,#52702,#52703,#52704,#52705,#52706,#52707,#52708,#52709,
#52710,#52711,#52712,#52713,#52714,#52715,#52716,#52717,#52718,#52719,#52720,
#52721,#52722,#52723,#52724,#52725,#52726,#52727,#52728,#52729,#52730,#52731,
#52732,#52733,#52734,#52735,#52736,#52737,#52738,#52739,#52740,#52741,#52742,
#52743,#52744,#52745,#52746,#52747,#52748,#52749,#52750,#52751,#52752,#52753,
#52754,#52755,#52756,#52757,#52758,#52759,#52760,#52761,#52762,#52763,#52764,
#52765,#52766,#52767,#52768,#52769,#52770,#52771,#52772,#52773,#52774,#52775,
#52776,#52777,#52778,#52779,#52780,#52781,#52782,#52783,#52784,#52785,#52786,
#52787,#52788,#52789,#52790,#52791,#52792,#52793,#52794,#52795,#52796,#52797,
#52798,#52799,#52800,#52801,#52802,#52803,#52804,#52805,#52806,#52807,#52808,
#52809,#52810,#52811,#52812,#52813,#52814,#52815,#52816,#52817,#52818,#52819,
#52820,#52821,#52822,#52823,#52824,#52825,#52826,#52827,#52828,#52829,#52830,
#52831,#52832,#52833,#52834,#52835,#52836,#52837,#52838,#52839,#52840,#52841,
#52842,#52843,#52844,#52845,#52846,#52847,#52848,#52849,#52850,#52851,#52852,
#52853,#52854,#52855,#52856,#52857,#52858,#52859,#52860,#52861,#52862,#52863,
#52864,#52865,#52866,#52867,#52868,#52869,#52870,#52871,#52872,#52873,#52874,
#52875,#52876,#52877,#52878,#52879,#52880,#52881,#52882,#52883,#52884,#52885,
#52886,#52887,#52888,#52889,#52890,#52891,#52892,#52893,#52894,#52895,#52896,
#52897,#52898,#52899,#52900,#52901,#52902,#52903,#52904,#52905,#52906,#52907,
#52908,#52909,#52910,#52911,#52912,#52913,#52914,#52915,#52916,#52917,#52918,
#52919,#52920,#52921,#52922,#52923,#52924,#52925,#52926,#52927,#52928,#52929,
#52930,#52931,#52932,#52933,#52934,#52935,#52936,#52937,#52938,#52939,#52940,
#52941,#52942,#52943,#52944,#52945,#52946,#52947,#52948,#52949,#52950,#52951,
#52952,#52953,#52954,#52955,#52956,#52957,#52958,#52959,#52960,#52961,#52962,
#52963,#52964,#52965,#52966,#52967,#52968,#52969,#52970,#52971,#52972,#52973,
#52974,#52975,#52976,#52977,#52978,#52979,#52980,#52981,#52982,#52983,#52984,
#52985,#52986,#52987,#52988,#52989,#52990,#52991,#52992,#52993,#52994,#52995,
#52996));
#10320=EDGE_LOOP('',(#52997,#52998,#52999,#53000,#53001,#53002,#53003,#53004,
#53005,#53006,#53007,#53008,#53009,#53010,#53011,#53012,#53013,#53014,#53015,
#53016,#53017,#53018,#53019,#53020,#53021,#53022,#53023,#53024,#53025,#53026,
#53027,#53028,#53029,#53030,#53031,#53032,#53033,#53034,#53035,#53036,#53037,
#53038,#53039,#53040,#53041,#53042,#53043,#53044,#53045,#53046,#53047,#53048,
#53049,#53050,#53051,#53052,#53053,#53054,#53055,#53056,#53057,#53058,#53059,
#53060,#53061,#53062,#53063,#53064,#53065,#53066,#53067,#53068,#53069,#53070,
#53071,#53072,#53073,#53074,#53075,#53076,#53077,#53078,#53079,#53080,#53081,
#53082,#53083,#53084,#53085,#53086,#53087,#53088,#53089,#53090,#53091,#53092,
#53093,#53094,#53095,#53096,#53097,#53098,#53099,#53100,#53101,#53102,#53103,
#53104,#53105,#53106,#53107,#53108,#53109,#53110,#53111,#53112,#53113,#53114,
#53115,#53116,#53117,#53118,#53119,#53120,#53121,#53122,#53123,#53124,#53125,
#53126,#53127,#53128,#53129,#53130,#53131,#53132,#53133,#53134,#53135,#53136,
#53137,#53138,#53139,#53140,#53141,#53142,#53143,#53144,#53145,#53146,#53147,
#53148,#53149,#53150,#53151,#53152,#53153,#53154,#53155,#53156,#53157,#53158,
#53159,#53160,#53161,#53162,#53163,#53164,#53165,#53166,#53167,#53168,#53169,
#53170,#53171,#53172,#53173,#53174,#53175,#53176,#53177,#53178,#53179,#53180,
#53181,#53182,#53183,#53184,#53185,#53186,#53187,#53188,#53189,#53190,#53191,
#53192,#53193,#53194,#53195,#53196,#53197,#53198,#53199,#53200,#53201,#53202,
#53203,#53204,#53205,#53206,#53207,#53208,#53209,#53210,#53211,#53212,#53213,
#53214,#53215,#53216,#53217,#53218,#53219,#53220,#53221,#53222,#53223,#53224,
#53225,#53226,#53227,#53228,#53229,#53230,#53231,#53232,#53233,#53234,#53235,
#53236,#53237,#53238,#53239,#53240,#53241,#53242,#53243,#53244,#53245,#53246,
#53247,#53248,#53249,#53250,#53251,#53252,#53253,#53254,#53255,#53256,#53257,
#53258,#53259,#53260,#53261,#53262,#53263,#53264,#53265,#53266,#53267,#53268,
#53269,#53270,#53271,#53272,#53273,#53274,#53275,#53276,#53277,#53278,#53279,
#53280,#53281,#53282,#53283,#53284,#53285,#53286,#53287,#53288,#53289,#53290,
#53291,#53292,#53293,#53294,#53295,#53296,#53297,#53298,#53299,#53300,#53301,
#53302,#53303,#53304,#53305,#53306,#53307,#53308,#53309,#53310,#53311,#53312,
#53313,#53314,#53315,#53316,#53317,#53318,#53319,#53320,#53321,#53322,#53323,
#53324,#53325,#53326,#53327,#53328,#53329,#53330,#53331,#53332,#53333,#53334,
#53335,#53336,#53337,#53338,#53339,#53340,#53341,#53342,#53343,#53344,#53345,
#53346,#53347,#53348,#53349,#53350,#53351,#53352,#53353,#53354,#53355,#53356,
#53357,#53358,#53359,#53360,#53361,#53362,#53363,#53364,#53365,#53366,#53367,
#53368,#53369,#53370,#53371,#53372,#53373,#53374,#53375,#53376,#53377,#53378,
#53379,#53380,#53381,#53382,#53383,#53384,#53385,#53386,#53387,#53388,#53389,
#53390,#53391,#53392,#53393,#53394,#53395,#53396,#53397,#53398,#53399,#53400,
#53401,#53402,#53403,#53404,#53405,#53406,#53407,#53408,#53409,#53410,#53411,
#53412,#53413,#53414,#53415,#53416,#53417,#53418,#53419,#53420,#53421,#53422,
#53423,#53424,#53425,#53426,#53427,#53428,#53429,#53430,#53431,#53432,#53433,
#53434,#53435,#53436,#53437,#53438,#53439,#53440,#53441,#53442,#53443,#53444,
#53445,#53446,#53447,#53448,#53449,#53450,#53451,#53452,#53453,#53454,#53455,
#53456,#53457,#53458,#53459,#53460,#53461,#53462,#53463,#53464,#53465,#53466,
#53467,#53468,#53469,#53470,#53471,#53472,#53473,#53474,#53475,#53476,#53477,
#53478,#53479,#53480,#53481,#53482,#53483,#53484,#53485,#53486,#53487,#53488,
#53489,#53490,#53491,#53492,#53493,#53494,#53495,#53496,#53497,#53498,#53499,
#53500));
#14637=LINE('',#98950,#20671);
#14638=LINE('',#98954,#20672);
#14639=LINE('',#98959,#20673);
#14640=LINE('',#98961,#20674);
#14641=LINE('',#98963,#20675);
#14642=LINE('',#98964,#20676);
#14643=LINE('',#98969,#20677);
#14644=LINE('',#98973,#20678);
#14645=LINE('',#98978,#20679);
#14646=LINE('',#98980,#20680);
#14647=LINE('',#98982,#20681);
#14648=LINE('',#98983,#20682);
#14649=LINE('',#98992,#20683);
#14650=LINE('',#98996,#20684);
#14651=LINE('',#99001,#20685);
#14652=LINE('',#99003,#20686);
#14653=LINE('',#99005,#20687);
#14654=LINE('',#99006,#20688);
#14655=LINE('',#99009,#20689);
#14656=LINE('',#99011,#20690);
#14657=LINE('',#99012,#20691);
#14658=LINE('',#99013,#20692);
#14659=LINE('',#99016,#20693);
#14660=LINE('',#99017,#20694);
#14661=LINE('',#99020,#20695);
#14662=LINE('',#99021,#20696);
#14663=LINE('',#99024,#20697);
#14664=LINE('',#99026,#20698);
#14665=LINE('',#99027,#20699);
#14666=LINE('',#99030,#20700);
#14667=LINE('',#99032,#20701);
#14668=LINE('',#99033,#20702);
#14669=LINE('',#99036,#20703);
#14670=LINE('',#99038,#20704);
#14671=LINE('',#99039,#20705);
#14672=LINE('',#99042,#20706);
#14673=LINE('',#99044,#20707);
#14674=LINE('',#99045,#20708);
#14675=LINE('',#99048,#20709);
#14676=LINE('',#99050,#20710);
#14677=LINE('',#99051,#20711);
#14678=LINE('',#99054,#20712);
#14679=LINE('',#99056,#20713);
#14680=LINE('',#99057,#20714);
#14681=LINE('',#99060,#20715);
#14682=LINE('',#99062,#20716);
#14683=LINE('',#99063,#20717);
#14684=LINE('',#99066,#20718);
#14685=LINE('',#99068,#20719);
#14686=LINE('',#99069,#20720);
#14687=LINE('',#99072,#20721);
#14688=LINE('',#99074,#20722);
#14689=LINE('',#99075,#20723);
#14690=LINE('',#99078,#20724);
#14691=LINE('',#99080,#20725);
#14692=LINE('',#99081,#20726);
#14693=LINE('',#99084,#20727);
#14694=LINE('',#99086,#20728);
#14695=LINE('',#99087,#20729);
#14696=LINE('',#99090,#20730);
#14697=LINE('',#99092,#20731);
#14698=LINE('',#99093,#20732);
#14699=LINE('',#99096,#20733);
#14700=LINE('',#99098,#20734);
#14701=LINE('',#99099,#20735);
#14702=LINE('',#99102,#20736);
#14703=LINE('',#99104,#20737);
#14704=LINE('',#99105,#20738);
#14705=LINE('',#99108,#20739);
#14706=LINE('',#99110,#20740);
#14707=LINE('',#99111,#20741);
#14708=LINE('',#99114,#20742);
#14709=LINE('',#99116,#20743);
#14710=LINE('',#99117,#20744);
#14711=LINE('',#99120,#20745);
#14712=LINE('',#99122,#20746);
#14713=LINE('',#99123,#20747);
#14714=LINE('',#99126,#20748);
#14715=LINE('',#99128,#20749);
#14716=LINE('',#99129,#20750);
#14717=LINE('',#99132,#20751);
#14718=LINE('',#99134,#20752);
#14719=LINE('',#99135,#20753);
#14720=LINE('',#99138,#20754);
#14721=LINE('',#99140,#20755);
#14722=LINE('',#99141,#20756);
#14723=LINE('',#99144,#20757);
#14724=LINE('',#99146,#20758);
#14725=LINE('',#99147,#20759);
#14726=LINE('',#99150,#20760);
#14727=LINE('',#99152,#20761);
#14728=LINE('',#99153,#20762);
#14729=LINE('',#99156,#20763);
#14730=LINE('',#99158,#20764);
#14731=LINE('',#99159,#20765);
#14732=LINE('',#99162,#20766);
#14733=LINE('',#99164,#20767);
#14734=LINE('',#99165,#20768);
#14735=LINE('',#99168,#20769);
#14736=LINE('',#99170,#20770);
#14737=LINE('',#99171,#20771);
#14738=LINE('',#99174,#20772);
#14739=LINE('',#99176,#20773);
#14740=LINE('',#99177,#20774);
#14741=LINE('',#99180,#20775);
#14742=LINE('',#99182,#20776);
#14743=LINE('',#99183,#20777);
#14744=LINE('',#99186,#20778);
#14745=LINE('',#99188,#20779);
#14746=LINE('',#99189,#20780);
#14747=LINE('',#99192,#20781);
#14748=LINE('',#99194,#20782);
#14749=LINE('',#99195,#20783);
#14750=LINE('',#99198,#20784);
#14751=LINE('',#99200,#20785);
#14752=LINE('',#99201,#20786);
#14753=LINE('',#99204,#20787);
#14754=LINE('',#99206,#20788);
#14755=LINE('',#99207,#20789);
#14756=LINE('',#99210,#20790);
#14757=LINE('',#99212,#20791);
#14758=LINE('',#99213,#20792);
#14759=LINE('',#99216,#20793);
#14760=LINE('',#99218,#20794);
#14761=LINE('',#99219,#20795);
#14762=LINE('',#99222,#20796);
#14763=LINE('',#99224,#20797);
#14764=LINE('',#99225,#20798);
#14765=LINE('',#99228,#20799);
#14766=LINE('',#99230,#20800);
#14767=LINE('',#99231,#20801);
#14768=LINE('',#99234,#20802);
#14769=LINE('',#99236,#20803);
#14770=LINE('',#99237,#20804);
#14771=LINE('',#99240,#20805);
#14772=LINE('',#99242,#20806);
#14773=LINE('',#99243,#20807);
#14774=LINE('',#99246,#20808);
#14775=LINE('',#99248,#20809);
#14776=LINE('',#99249,#20810);
#14777=LINE('',#99252,#20811);
#14778=LINE('',#99254,#20812);
#14779=LINE('',#99255,#20813);
#14780=LINE('',#99258,#20814);
#14781=LINE('',#99260,#20815);
#14782=LINE('',#99261,#20816);
#14783=LINE('',#99264,#20817);
#14784=LINE('',#99266,#20818);
#14785=LINE('',#99267,#20819);
#14786=LINE('',#99270,#20820);
#14787=LINE('',#99272,#20821);
#14788=LINE('',#99273,#20822);
#14789=LINE('',#99276,#20823);
#14790=LINE('',#99278,#20824);
#14791=LINE('',#99279,#20825);
#14792=LINE('',#99282,#20826);
#14793=LINE('',#99284,#20827);
#14794=LINE('',#99285,#20828);
#14795=LINE('',#99288,#20829);
#14796=LINE('',#99290,#20830);
#14797=LINE('',#99291,#20831);
#14798=LINE('',#99294,#20832);
#14799=LINE('',#99296,#20833);
#14800=LINE('',#99297,#20834);
#14801=LINE('',#99300,#20835);
#14802=LINE('',#99302,#20836);
#14803=LINE('',#99303,#20837);
#14804=LINE('',#99306,#20838);
#14805=LINE('',#99308,#20839);
#14806=LINE('',#99309,#20840);
#14807=LINE('',#99312,#20841);
#14808=LINE('',#99314,#20842);
#14809=LINE('',#99315,#20843);
#14810=LINE('',#99318,#20844);
#14811=LINE('',#99320,#20845);
#14812=LINE('',#99321,#20846);
#14813=LINE('',#99324,#20847);
#14814=LINE('',#99326,#20848);
#14815=LINE('',#99327,#20849);
#14816=LINE('',#99330,#20850);
#14817=LINE('',#99332,#20851);
#14818=LINE('',#99333,#20852);
#14819=LINE('',#99336,#20853);
#14820=LINE('',#99338,#20854);
#14821=LINE('',#99339,#20855);
#14822=LINE('',#99342,#20856);
#14823=LINE('',#99344,#20857);
#14824=LINE('',#99345,#20858);
#14825=LINE('',#99348,#20859);
#14826=LINE('',#99350,#20860);
#14827=LINE('',#99351,#20861);
#14828=LINE('',#99354,#20862);
#14829=LINE('',#99356,#20863);
#14830=LINE('',#99357,#20864);
#14831=LINE('',#99360,#20865);
#14832=LINE('',#99362,#20866);
#14833=LINE('',#99363,#20867);
#14834=LINE('',#99366,#20868);
#14835=LINE('',#99368,#20869);
#14836=LINE('',#99369,#20870);
#14837=LINE('',#99372,#20871);
#14838=LINE('',#99374,#20872);
#14839=LINE('',#99375,#20873);
#14840=LINE('',#99378,#20874);
#14841=LINE('',#99380,#20875);
#14842=LINE('',#99381,#20876);
#14843=LINE('',#99384,#20877);
#14844=LINE('',#99386,#20878);
#14845=LINE('',#99387,#20879);
#14846=LINE('',#99390,#20880);
#14847=LINE('',#99392,#20881);
#14848=LINE('',#99393,#20882);
#14849=LINE('',#99396,#20883);
#14850=LINE('',#99398,#20884);
#14851=LINE('',#99399,#20885);
#14852=LINE('',#99402,#20886);
#14853=LINE('',#99404,#20887);
#14854=LINE('',#99405,#20888);
#14855=LINE('',#99408,#20889);
#14856=LINE('',#99410,#20890);
#14857=LINE('',#99411,#20891);
#14858=LINE('',#99414,#20892);
#14859=LINE('',#99416,#20893);
#14860=LINE('',#99417,#20894);
#14861=LINE('',#99420,#20895);
#14862=LINE('',#99422,#20896);
#14863=LINE('',#99423,#20897);
#14864=LINE('',#99426,#20898);
#14865=LINE('',#99428,#20899);
#14866=LINE('',#99429,#20900);
#14867=LINE('',#99432,#20901);
#14868=LINE('',#99434,#20902);
#14869=LINE('',#99435,#20903);
#14870=LINE('',#99438,#20904);
#14871=LINE('',#99440,#20905);
#14872=LINE('',#99441,#20906);
#14873=LINE('',#99444,#20907);
#14874=LINE('',#99446,#20908);
#14875=LINE('',#99447,#20909);
#14876=LINE('',#99450,#20910);
#14877=LINE('',#99452,#20911);
#14878=LINE('',#99453,#20912);
#14879=LINE('',#99456,#20913);
#14880=LINE('',#99458,#20914);
#14881=LINE('',#99459,#20915);
#14882=LINE('',#99462,#20916);
#14883=LINE('',#99464,#20917);
#14884=LINE('',#99465,#20918);
#14885=LINE('',#99468,#20919);
#14886=LINE('',#99470,#20920);
#14887=LINE('',#99471,#20921);
#14888=LINE('',#99474,#20922);
#14889=LINE('',#99476,#20923);
#14890=LINE('',#99477,#20924);
#14891=LINE('',#99480,#20925);
#14892=LINE('',#99482,#20926);
#14893=LINE('',#99483,#20927);
#14894=LINE('',#99486,#20928);
#14895=LINE('',#99488,#20929);
#14896=LINE('',#99489,#20930);
#14897=LINE('',#99492,#20931);
#14898=LINE('',#99494,#20932);
#14899=LINE('',#99495,#20933);
#14900=LINE('',#99498,#20934);
#14901=LINE('',#99500,#20935);
#14902=LINE('',#99501,#20936);
#14903=LINE('',#99504,#20937);
#14904=LINE('',#99506,#20938);
#14905=LINE('',#99507,#20939);
#14906=LINE('',#99510,#20940);
#14907=LINE('',#99512,#20941);
#14908=LINE('',#99513,#20942);
#14909=LINE('',#99516,#20943);
#14910=LINE('',#99518,#20944);
#14911=LINE('',#99519,#20945);
#14912=LINE('',#99522,#20946);
#14913=LINE('',#99524,#20947);
#14914=LINE('',#99525,#20948);
#14915=LINE('',#99528,#20949);
#14916=LINE('',#99530,#20950);
#14917=LINE('',#99531,#20951);
#14918=LINE('',#99534,#20952);
#14919=LINE('',#99536,#20953);
#14920=LINE('',#99537,#20954);
#14921=LINE('',#99540,#20955);
#14922=LINE('',#99542,#20956);
#14923=LINE('',#99543,#20957);
#14924=LINE('',#99546,#20958);
#14925=LINE('',#99548,#20959);
#14926=LINE('',#99549,#20960);
#14927=LINE('',#99552,#20961);
#14928=LINE('',#99554,#20962);
#14929=LINE('',#99555,#20963);
#14930=LINE('',#99558,#20964);
#14931=LINE('',#99560,#20965);
#14932=LINE('',#99561,#20966);
#14933=LINE('',#99564,#20967);
#14934=LINE('',#99566,#20968);
#14935=LINE('',#99567,#20969);
#14936=LINE('',#99570,#20970);
#14937=LINE('',#99572,#20971);
#14938=LINE('',#99573,#20972);
#14939=LINE('',#99576,#20973);
#14940=LINE('',#99578,#20974);
#14941=LINE('',#99579,#20975);
#14942=LINE('',#99582,#20976);
#14943=LINE('',#99584,#20977);
#14944=LINE('',#99585,#20978);
#14945=LINE('',#99588,#20979);
#14946=LINE('',#99590,#20980);
#14947=LINE('',#99591,#20981);
#14948=LINE('',#99594,#20982);
#14949=LINE('',#99596,#20983);
#14950=LINE('',#99597,#20984);
#14951=LINE('',#99600,#20985);
#14952=LINE('',#99602,#20986);
#14953=LINE('',#99603,#20987);
#14954=LINE('',#99606,#20988);
#14955=LINE('',#99608,#20989);
#14956=LINE('',#99609,#20990);
#14957=LINE('',#99612,#20991);
#14958=LINE('',#99614,#20992);
#14959=LINE('',#99615,#20993);
#14960=LINE('',#99618,#20994);
#14961=LINE('',#99620,#20995);
#14962=LINE('',#99621,#20996);
#14963=LINE('',#99624,#20997);
#14964=LINE('',#99626,#20998);
#14965=LINE('',#99627,#20999);
#14966=LINE('',#99630,#21000);
#14967=LINE('',#99632,#21001);
#14968=LINE('',#99633,#21002);
#14969=LINE('',#99636,#21003);
#14970=LINE('',#99638,#21004);
#14971=LINE('',#99639,#21005);
#14972=LINE('',#99642,#21006);
#14973=LINE('',#99644,#21007);
#14974=LINE('',#99645,#21008);
#14975=LINE('',#99648,#21009);
#14976=LINE('',#99650,#21010);
#14977=LINE('',#99651,#21011);
#14978=LINE('',#99654,#21012);
#14979=LINE('',#99656,#21013);
#14980=LINE('',#99657,#21014);
#14981=LINE('',#99660,#21015);
#14982=LINE('',#99662,#21016);
#14983=LINE('',#99663,#21017);
#14984=LINE('',#99666,#21018);
#14985=LINE('',#99668,#21019);
#14986=LINE('',#99669,#21020);
#14987=LINE('',#99672,#21021);
#14988=LINE('',#99674,#21022);
#14989=LINE('',#99675,#21023);
#14990=LINE('',#99678,#21024);
#14991=LINE('',#99680,#21025);
#14992=LINE('',#99681,#21026);
#14993=LINE('',#99684,#21027);
#14994=LINE('',#99686,#21028);
#14995=LINE('',#99687,#21029);
#14996=LINE('',#99690,#21030);
#14997=LINE('',#99692,#21031);
#14998=LINE('',#99693,#21032);
#14999=LINE('',#99696,#21033);
#15000=LINE('',#99698,#21034);
#15001=LINE('',#99699,#21035);
#15002=LINE('',#99702,#21036);
#15003=LINE('',#99704,#21037);
#15004=LINE('',#99705,#21038);
#15005=LINE('',#99708,#21039);
#15006=LINE('',#99710,#21040);
#15007=LINE('',#99711,#21041);
#15008=LINE('',#99714,#21042);
#15009=LINE('',#99716,#21043);
#15010=LINE('',#99717,#21044);
#15011=LINE('',#99720,#21045);
#15012=LINE('',#99722,#21046);
#15013=LINE('',#99723,#21047);
#15014=LINE('',#99726,#21048);
#15015=LINE('',#99728,#21049);
#15016=LINE('',#99729,#21050);
#15017=LINE('',#99732,#21051);
#15018=LINE('',#99734,#21052);
#15019=LINE('',#99735,#21053);
#15020=LINE('',#99738,#21054);
#15021=LINE('',#99740,#21055);
#15022=LINE('',#99741,#21056);
#15023=LINE('',#99744,#21057);
#15024=LINE('',#99746,#21058);
#15025=LINE('',#99747,#21059);
#15026=LINE('',#99750,#21060);
#15027=LINE('',#99752,#21061);
#15028=LINE('',#99753,#21062);
#15029=LINE('',#99756,#21063);
#15030=LINE('',#99758,#21064);
#15031=LINE('',#99759,#21065);
#15032=LINE('',#99762,#21066);
#15033=LINE('',#99764,#21067);
#15034=LINE('',#99765,#21068);
#15035=LINE('',#99768,#21069);
#15036=LINE('',#99770,#21070);
#15037=LINE('',#99771,#21071);
#15038=LINE('',#99774,#21072);
#15039=LINE('',#99776,#21073);
#15040=LINE('',#99777,#21074);
#15041=LINE('',#99780,#21075);
#15042=LINE('',#99782,#21076);
#15043=LINE('',#99783,#21077);
#15044=LINE('',#99786,#21078);
#15045=LINE('',#99788,#21079);
#15046=LINE('',#99789,#21080);
#15047=LINE('',#99792,#21081);
#15048=LINE('',#99794,#21082);
#15049=LINE('',#99795,#21083);
#15050=LINE('',#99798,#21084);
#15051=LINE('',#99800,#21085);
#15052=LINE('',#99801,#21086);
#15053=LINE('',#99804,#21087);
#15054=LINE('',#99806,#21088);
#15055=LINE('',#99807,#21089);
#15056=LINE('',#99810,#21090);
#15057=LINE('',#99812,#21091);
#15058=LINE('',#99813,#21092);
#15059=LINE('',#99816,#21093);
#15060=LINE('',#99818,#21094);
#15061=LINE('',#99819,#21095);
#15062=LINE('',#99822,#21096);
#15063=LINE('',#99824,#21097);
#15064=LINE('',#99825,#21098);
#15065=LINE('',#99828,#21099);
#15066=LINE('',#99830,#21100);
#15067=LINE('',#99831,#21101);
#15068=LINE('',#99834,#21102);
#15069=LINE('',#99836,#21103);
#15070=LINE('',#99837,#21104);
#15071=LINE('',#99840,#21105);
#15072=LINE('',#99842,#21106);
#15073=LINE('',#99843,#21107);
#15074=LINE('',#99846,#21108);
#15075=LINE('',#99848,#21109);
#15076=LINE('',#99849,#21110);
#15077=LINE('',#99852,#21111);
#15078=LINE('',#99854,#21112);
#15079=LINE('',#99855,#21113);
#15080=LINE('',#99858,#21114);
#15081=LINE('',#99860,#21115);
#15082=LINE('',#99861,#21116);
#15083=LINE('',#99864,#21117);
#15084=LINE('',#99866,#21118);
#15085=LINE('',#99867,#21119);
#15086=LINE('',#99870,#21120);
#15087=LINE('',#99872,#21121);
#15088=LINE('',#99873,#21122);
#15089=LINE('',#99876,#21123);
#15090=LINE('',#99878,#21124);
#15091=LINE('',#99879,#21125);
#15092=LINE('',#99882,#21126);
#15093=LINE('',#99884,#21127);
#15094=LINE('',#99885,#21128);
#15095=LINE('',#99888,#21129);
#15096=LINE('',#99890,#21130);
#15097=LINE('',#99891,#21131);
#15098=LINE('',#99894,#21132);
#15099=LINE('',#99896,#21133);
#15100=LINE('',#99897,#21134);
#15101=LINE('',#99900,#21135);
#15102=LINE('',#99902,#21136);
#15103=LINE('',#99903,#21137);
#15104=LINE('',#99906,#21138);
#15105=LINE('',#99908,#21139);
#15106=LINE('',#99909,#21140);
#15107=LINE('',#99912,#21141);
#15108=LINE('',#99914,#21142);
#15109=LINE('',#99915,#21143);
#15110=LINE('',#99918,#21144);
#15111=LINE('',#99920,#21145);
#15112=LINE('',#99921,#21146);
#15113=LINE('',#99924,#21147);
#15114=LINE('',#99926,#21148);
#15115=LINE('',#99927,#21149);
#15116=LINE('',#99930,#21150);
#15117=LINE('',#99932,#21151);
#15118=LINE('',#99933,#21152);
#15119=LINE('',#99936,#21153);
#15120=LINE('',#99938,#21154);
#15121=LINE('',#99939,#21155);
#15122=LINE('',#99942,#21156);
#15123=LINE('',#99944,#21157);
#15124=LINE('',#99945,#21158);
#15125=LINE('',#99948,#21159);
#15126=LINE('',#99950,#21160);
#15127=LINE('',#99951,#21161);
#15128=LINE('',#99954,#21162);
#15129=LINE('',#99956,#21163);
#15130=LINE('',#99957,#21164);
#15131=LINE('',#99960,#21165);
#15132=LINE('',#99962,#21166);
#15133=LINE('',#99963,#21167);
#15134=LINE('',#99966,#21168);
#15135=LINE('',#99968,#21169);
#15136=LINE('',#99969,#21170);
#15137=LINE('',#99972,#21171);
#15138=LINE('',#99974,#21172);
#15139=LINE('',#99975,#21173);
#15140=LINE('',#99978,#21174);
#15141=LINE('',#99980,#21175);
#15142=LINE('',#99981,#21176);
#15143=LINE('',#99984,#21177);
#15144=LINE('',#99986,#21178);
#15145=LINE('',#99987,#21179);
#15146=LINE('',#99990,#21180);
#15147=LINE('',#99992,#21181);
#15148=LINE('',#99993,#21182);
#15149=LINE('',#99996,#21183);
#15150=LINE('',#99998,#21184);
#15151=LINE('',#99999,#21185);
#15152=LINE('',#100002,#21186);
#15153=LINE('',#100004,#21187);
#15154=LINE('',#100005,#21188);
#15155=LINE('',#100008,#21189);
#15156=LINE('',#100010,#21190);
#15157=LINE('',#100011,#21191);
#15158=LINE('',#100014,#21192);
#15159=LINE('',#100016,#21193);
#15160=LINE('',#100017,#21194);
#15161=LINE('',#100020,#21195);
#15162=LINE('',#100022,#21196);
#15163=LINE('',#100023,#21197);
#15164=LINE('',#100026,#21198);
#15165=LINE('',#100028,#21199);
#15166=LINE('',#100029,#21200);
#15167=LINE('',#100032,#21201);
#15168=LINE('',#100034,#21202);
#15169=LINE('',#100035,#21203);
#15170=LINE('',#100038,#21204);
#15171=LINE('',#100040,#21205);
#15172=LINE('',#100041,#21206);
#15173=LINE('',#100044,#21207);
#15174=LINE('',#100046,#21208);
#15175=LINE('',#100047,#21209);
#15176=LINE('',#100050,#21210);
#15177=LINE('',#100052,#21211);
#15178=LINE('',#100053,#21212);
#15179=LINE('',#100056,#21213);
#15180=LINE('',#100058,#21214);
#15181=LINE('',#100059,#21215);
#15182=LINE('',#100062,#21216);
#15183=LINE('',#100064,#21217);
#15184=LINE('',#100065,#21218);
#15185=LINE('',#100068,#21219);
#15186=LINE('',#100070,#21220);
#15187=LINE('',#100071,#21221);
#15188=LINE('',#100074,#21222);
#15189=LINE('',#100076,#21223);
#15190=LINE('',#100077,#21224);
#15191=LINE('',#100080,#21225);
#15192=LINE('',#100082,#21226);
#15193=LINE('',#100083,#21227);
#15194=LINE('',#100086,#21228);
#15195=LINE('',#100088,#21229);
#15196=LINE('',#100089,#21230);
#15197=LINE('',#100092,#21231);
#15198=LINE('',#100094,#21232);
#15199=LINE('',#100095,#21233);
#15200=LINE('',#100098,#21234);
#15201=LINE('',#100100,#21235);
#15202=LINE('',#100101,#21236);
#15203=LINE('',#100104,#21237);
#15204=LINE('',#100106,#21238);
#15205=LINE('',#100107,#21239);
#15206=LINE('',#100110,#21240);
#15207=LINE('',#100112,#21241);
#15208=LINE('',#100113,#21242);
#15209=LINE('',#100116,#21243);
#15210=LINE('',#100118,#21244);
#15211=LINE('',#100119,#21245);
#15212=LINE('',#100122,#21246);
#15213=LINE('',#100124,#21247);
#15214=LINE('',#100125,#21248);
#15215=LINE('',#100128,#21249);
#15216=LINE('',#100130,#21250);
#15217=LINE('',#100131,#21251);
#15218=LINE('',#100134,#21252);
#15219=LINE('',#100136,#21253);
#15220=LINE('',#100137,#21254);
#15221=LINE('',#100140,#21255);
#15222=LINE('',#100142,#21256);
#15223=LINE('',#100143,#21257);
#15224=LINE('',#100146,#21258);
#15225=LINE('',#100148,#21259);
#15226=LINE('',#100149,#21260);
#15227=LINE('',#100152,#21261);
#15228=LINE('',#100154,#21262);
#15229=LINE('',#100155,#21263);
#15230=LINE('',#100158,#21264);
#15231=LINE('',#100160,#21265);
#15232=LINE('',#100161,#21266);
#15233=LINE('',#100164,#21267);
#15234=LINE('',#100166,#21268);
#15235=LINE('',#100167,#21269);
#15236=LINE('',#100170,#21270);
#15237=LINE('',#100172,#21271);
#15238=LINE('',#100173,#21272);
#15239=LINE('',#100176,#21273);
#15240=LINE('',#100178,#21274);
#15241=LINE('',#100179,#21275);
#15242=LINE('',#100182,#21276);
#15243=LINE('',#100184,#21277);
#15244=LINE('',#100185,#21278);
#15245=LINE('',#100188,#21279);
#15246=LINE('',#100190,#21280);
#15247=LINE('',#100191,#21281);
#15248=LINE('',#100194,#21282);
#15249=LINE('',#100196,#21283);
#15250=LINE('',#100197,#21284);
#15251=LINE('',#100200,#21285);
#15252=LINE('',#100202,#21286);
#15253=LINE('',#100203,#21287);
#15254=LINE('',#100206,#21288);
#15255=LINE('',#100208,#21289);
#15256=LINE('',#100209,#21290);
#15257=LINE('',#100212,#21291);
#15258=LINE('',#100214,#21292);
#15259=LINE('',#100215,#21293);
#15260=LINE('',#100218,#21294);
#15261=LINE('',#100220,#21295);
#15262=LINE('',#100221,#21296);
#15263=LINE('',#100224,#21297);
#15264=LINE('',#100226,#21298);
#15265=LINE('',#100227,#21299);
#15266=LINE('',#100230,#21300);
#15267=LINE('',#100232,#21301);
#15268=LINE('',#100233,#21302);
#15269=LINE('',#100236,#21303);
#15270=LINE('',#100238,#21304);
#15271=LINE('',#100239,#21305);
#15272=LINE('',#100242,#21306);
#15273=LINE('',#100244,#21307);
#15274=LINE('',#100245,#21308);
#15275=LINE('',#100248,#21309);
#15276=LINE('',#100250,#21310);
#15277=LINE('',#100251,#21311);
#15278=LINE('',#100254,#21312);
#15279=LINE('',#100256,#21313);
#15280=LINE('',#100257,#21314);
#15281=LINE('',#100260,#21315);
#15282=LINE('',#100262,#21316);
#15283=LINE('',#100263,#21317);
#15284=LINE('',#100266,#21318);
#15285=LINE('',#100268,#21319);
#15286=LINE('',#100269,#21320);
#15287=LINE('',#100272,#21321);
#15288=LINE('',#100274,#21322);
#15289=LINE('',#100275,#21323);
#15290=LINE('',#100278,#21324);
#15291=LINE('',#100280,#21325);
#15292=LINE('',#100281,#21326);
#15293=LINE('',#100284,#21327);
#15294=LINE('',#100286,#21328);
#15295=LINE('',#100287,#21329);
#15296=LINE('',#100290,#21330);
#15297=LINE('',#100292,#21331);
#15298=LINE('',#100293,#21332);
#15299=LINE('',#100296,#21333);
#15300=LINE('',#100298,#21334);
#15301=LINE('',#100299,#21335);
#15302=LINE('',#100302,#21336);
#15303=LINE('',#100304,#21337);
#15304=LINE('',#100305,#21338);
#15305=LINE('',#100308,#21339);
#15306=LINE('',#100310,#21340);
#15307=LINE('',#100311,#21341);
#15308=LINE('',#100314,#21342);
#15309=LINE('',#100316,#21343);
#15310=LINE('',#100317,#21344);
#15311=LINE('',#100320,#21345);
#15312=LINE('',#100322,#21346);
#15313=LINE('',#100323,#21347);
#15314=LINE('',#100326,#21348);
#15315=LINE('',#100328,#21349);
#15316=LINE('',#100329,#21350);
#15317=LINE('',#100332,#21351);
#15318=LINE('',#100334,#21352);
#15319=LINE('',#100335,#21353);
#15320=LINE('',#100338,#21354);
#15321=LINE('',#100340,#21355);
#15322=LINE('',#100341,#21356);
#15323=LINE('',#100344,#21357);
#15324=LINE('',#100346,#21358);
#15325=LINE('',#100347,#21359);
#15326=LINE('',#100350,#21360);
#15327=LINE('',#100352,#21361);
#15328=LINE('',#100353,#21362);
#15329=LINE('',#100356,#21363);
#15330=LINE('',#100358,#21364);
#15331=LINE('',#100359,#21365);
#15332=LINE('',#100362,#21366);
#15333=LINE('',#100364,#21367);
#15334=LINE('',#100365,#21368);
#15335=LINE('',#100368,#21369);
#15336=LINE('',#100370,#21370);
#15337=LINE('',#100371,#21371);
#15338=LINE('',#100374,#21372);
#15339=LINE('',#100376,#21373);
#15340=LINE('',#100377,#21374);
#15341=LINE('',#100380,#21375);
#15342=LINE('',#100382,#21376);
#15343=LINE('',#100383,#21377);
#15344=LINE('',#100386,#21378);
#15345=LINE('',#100388,#21379);
#15346=LINE('',#100389,#21380);
#15347=LINE('',#100392,#21381);
#15348=LINE('',#100394,#21382);
#15349=LINE('',#100395,#21383);
#15350=LINE('',#100398,#21384);
#15351=LINE('',#100400,#21385);
#15352=LINE('',#100401,#21386);
#15353=LINE('',#100404,#21387);
#15354=LINE('',#100406,#21388);
#15355=LINE('',#100407,#21389);
#15356=LINE('',#100410,#21390);
#15357=LINE('',#100412,#21391);
#15358=LINE('',#100413,#21392);
#15359=LINE('',#100416,#21393);
#15360=LINE('',#100418,#21394);
#15361=LINE('',#100419,#21395);
#15362=LINE('',#100422,#21396);
#15363=LINE('',#100424,#21397);
#15364=LINE('',#100425,#21398);
#15365=LINE('',#100428,#21399);
#15366=LINE('',#100430,#21400);
#15367=LINE('',#100431,#21401);
#15368=LINE('',#100434,#21402);
#15369=LINE('',#100436,#21403);
#15370=LINE('',#100437,#21404);
#15371=LINE('',#100440,#21405);
#15372=LINE('',#100442,#21406);
#15373=LINE('',#100443,#21407);
#15374=LINE('',#100446,#21408);
#15375=LINE('',#100448,#21409);
#15376=LINE('',#100449,#21410);
#15377=LINE('',#100452,#21411);
#15378=LINE('',#100454,#21412);
#15379=LINE('',#100455,#21413);
#15380=LINE('',#100458,#21414);
#15381=LINE('',#100460,#21415);
#15382=LINE('',#100461,#21416);
#15383=LINE('',#100464,#21417);
#15384=LINE('',#100466,#21418);
#15385=LINE('',#100467,#21419);
#15386=LINE('',#100470,#21420);
#15387=LINE('',#100472,#21421);
#15388=LINE('',#100473,#21422);
#15389=LINE('',#100476,#21423);
#15390=LINE('',#100478,#21424);
#15391=LINE('',#100479,#21425);
#15392=LINE('',#100482,#21426);
#15393=LINE('',#100484,#21427);
#15394=LINE('',#100485,#21428);
#15395=LINE('',#100488,#21429);
#15396=LINE('',#100490,#21430);
#15397=LINE('',#100491,#21431);
#15398=LINE('',#100494,#21432);
#15399=LINE('',#100496,#21433);
#15400=LINE('',#100497,#21434);
#15401=LINE('',#100500,#21435);
#15402=LINE('',#100502,#21436);
#15403=LINE('',#100503,#21437);
#15404=LINE('',#100506,#21438);
#15405=LINE('',#100508,#21439);
#15406=LINE('',#100509,#21440);
#15407=LINE('',#100512,#21441);
#15408=LINE('',#100514,#21442);
#15409=LINE('',#100515,#21443);
#15410=LINE('',#100518,#21444);
#15411=LINE('',#100520,#21445);
#15412=LINE('',#100521,#21446);
#15413=LINE('',#100524,#21447);
#15414=LINE('',#100526,#21448);
#15415=LINE('',#100527,#21449);
#15416=LINE('',#100530,#21450);
#15417=LINE('',#100532,#21451);
#15418=LINE('',#100533,#21452);
#15419=LINE('',#100536,#21453);
#15420=LINE('',#100538,#21454);
#15421=LINE('',#100539,#21455);
#15422=LINE('',#100542,#21456);
#15423=LINE('',#100544,#21457);
#15424=LINE('',#100545,#21458);
#15425=LINE('',#100548,#21459);
#15426=LINE('',#100550,#21460);
#15427=LINE('',#100551,#21461);
#15428=LINE('',#100554,#21462);
#15429=LINE('',#100556,#21463);
#15430=LINE('',#100557,#21464);
#15431=LINE('',#100560,#21465);
#15432=LINE('',#100562,#21466);
#15433=LINE('',#100563,#21467);
#15434=LINE('',#100566,#21468);
#15435=LINE('',#100568,#21469);
#15436=LINE('',#100569,#21470);
#15437=LINE('',#100572,#21471);
#15438=LINE('',#100574,#21472);
#15439=LINE('',#100575,#21473);
#15440=LINE('',#100578,#21474);
#15441=LINE('',#100580,#21475);
#15442=LINE('',#100581,#21476);
#15443=LINE('',#100584,#21477);
#15444=LINE('',#100586,#21478);
#15445=LINE('',#100587,#21479);
#15446=LINE('',#100590,#21480);
#15447=LINE('',#100592,#21481);
#15448=LINE('',#100593,#21482);
#15449=LINE('',#100596,#21483);
#15450=LINE('',#100598,#21484);
#15451=LINE('',#100599,#21485);
#15452=LINE('',#100602,#21486);
#15453=LINE('',#100604,#21487);
#15454=LINE('',#100605,#21488);
#15455=LINE('',#100608,#21489);
#15456=LINE('',#100610,#21490);
#15457=LINE('',#100611,#21491);
#15458=LINE('',#100614,#21492);
#15459=LINE('',#100616,#21493);
#15460=LINE('',#100617,#21494);
#15461=LINE('',#100620,#21495);
#15462=LINE('',#100622,#21496);
#15463=LINE('',#100623,#21497);
#15464=LINE('',#100626,#21498);
#15465=LINE('',#100628,#21499);
#15466=LINE('',#100629,#21500);
#15467=LINE('',#100632,#21501);
#15468=LINE('',#100634,#21502);
#15469=LINE('',#100635,#21503);
#15470=LINE('',#100638,#21504);
#15471=LINE('',#100640,#21505);
#15472=LINE('',#100641,#21506);
#15473=LINE('',#100644,#21507);
#15474=LINE('',#100646,#21508);
#15475=LINE('',#100647,#21509);
#15476=LINE('',#100650,#21510);
#15477=LINE('',#100652,#21511);
#15478=LINE('',#100653,#21512);
#15479=LINE('',#100656,#21513);
#15480=LINE('',#100658,#21514);
#15481=LINE('',#100659,#21515);
#15482=LINE('',#100662,#21516);
#15483=LINE('',#100664,#21517);
#15484=LINE('',#100665,#21518);
#15485=LINE('',#100668,#21519);
#15486=LINE('',#100670,#21520);
#15487=LINE('',#100671,#21521);
#15488=LINE('',#100674,#21522);
#15489=LINE('',#100676,#21523);
#15490=LINE('',#100677,#21524);
#15491=LINE('',#100680,#21525);
#15492=LINE('',#100682,#21526);
#15493=LINE('',#100683,#21527);
#15494=LINE('',#100686,#21528);
#15495=LINE('',#100688,#21529);
#15496=LINE('',#100689,#21530);
#15497=LINE('',#100692,#21531);
#15498=LINE('',#100694,#21532);
#15499=LINE('',#100695,#21533);
#15500=LINE('',#100698,#21534);
#15501=LINE('',#100700,#21535);
#15502=LINE('',#100701,#21536);
#15503=LINE('',#100704,#21537);
#15504=LINE('',#100706,#21538);
#15505=LINE('',#100707,#21539);
#15506=LINE('',#100710,#21540);
#15507=LINE('',#100712,#21541);
#15508=LINE('',#100713,#21542);
#15509=LINE('',#100716,#21543);
#15510=LINE('',#100718,#21544);
#15511=LINE('',#100719,#21545);
#15512=LINE('',#100722,#21546);
#15513=LINE('',#100724,#21547);
#15514=LINE('',#100725,#21548);
#15515=LINE('',#100728,#21549);
#15516=LINE('',#100730,#21550);
#15517=LINE('',#100731,#21551);
#15518=LINE('',#100734,#21552);
#15519=LINE('',#100736,#21553);
#15520=LINE('',#100737,#21554);
#15521=LINE('',#100740,#21555);
#15522=LINE('',#100742,#21556);
#15523=LINE('',#100743,#21557);
#15524=LINE('',#100746,#21558);
#15525=LINE('',#100748,#21559);
#15526=LINE('',#100749,#21560);
#15527=LINE('',#100752,#21561);
#15528=LINE('',#100754,#21562);
#15529=LINE('',#100755,#21563);
#15530=LINE('',#100758,#21564);
#15531=LINE('',#100760,#21565);
#15532=LINE('',#100761,#21566);
#15533=LINE('',#100764,#21567);
#15534=LINE('',#100766,#21568);
#15535=LINE('',#100767,#21569);
#15536=LINE('',#100770,#21570);
#15537=LINE('',#100772,#21571);
#15538=LINE('',#100773,#21572);
#15539=LINE('',#100776,#21573);
#15540=LINE('',#100778,#21574);
#15541=LINE('',#100779,#21575);
#15542=LINE('',#100782,#21576);
#15543=LINE('',#100784,#21577);
#15544=LINE('',#100785,#21578);
#15545=LINE('',#100788,#21579);
#15546=LINE('',#100790,#21580);
#15547=LINE('',#100791,#21581);
#15548=LINE('',#100794,#21582);
#15549=LINE('',#100796,#21583);
#15550=LINE('',#100797,#21584);
#15551=LINE('',#100800,#21585);
#15552=LINE('',#100802,#21586);
#15553=LINE('',#100803,#21587);
#15554=LINE('',#100806,#21588);
#15555=LINE('',#100808,#21589);
#15556=LINE('',#100809,#21590);
#15557=LINE('',#100812,#21591);
#15558=LINE('',#100814,#21592);
#15559=LINE('',#100815,#21593);
#15560=LINE('',#100818,#21594);
#15561=LINE('',#100820,#21595);
#15562=LINE('',#100821,#21596);
#15563=LINE('',#100824,#21597);
#15564=LINE('',#100826,#21598);
#15565=LINE('',#100827,#21599);
#15566=LINE('',#100830,#21600);
#15567=LINE('',#100832,#21601);
#15568=LINE('',#100833,#21602);
#15569=LINE('',#100836,#21603);
#15570=LINE('',#100838,#21604);
#15571=LINE('',#100839,#21605);
#15572=LINE('',#100842,#21606);
#15573=LINE('',#100844,#21607);
#15574=LINE('',#100845,#21608);
#15575=LINE('',#100848,#21609);
#15576=LINE('',#100850,#21610);
#15577=LINE('',#100851,#21611);
#15578=LINE('',#100854,#21612);
#15579=LINE('',#100856,#21613);
#15580=LINE('',#100857,#21614);
#15581=LINE('',#100860,#21615);
#15582=LINE('',#100862,#21616);
#15583=LINE('',#100863,#21617);
#15584=LINE('',#100866,#21618);
#15585=LINE('',#100868,#21619);
#15586=LINE('',#100869,#21620);
#15587=LINE('',#100872,#21621);
#15588=LINE('',#100874,#21622);
#15589=LINE('',#100875,#21623);
#15590=LINE('',#100878,#21624);
#15591=LINE('',#100880,#21625);
#15592=LINE('',#100881,#21626);
#15593=LINE('',#100884,#21627);
#15594=LINE('',#100886,#21628);
#15595=LINE('',#100887,#21629);
#15596=LINE('',#100890,#21630);
#15597=LINE('',#100892,#21631);
#15598=LINE('',#100893,#21632);
#15599=LINE('',#100896,#21633);
#15600=LINE('',#100898,#21634);
#15601=LINE('',#100899,#21635);
#15602=LINE('',#100902,#21636);
#15603=LINE('',#100904,#21637);
#15604=LINE('',#100905,#21638);
#15605=LINE('',#100908,#21639);
#15606=LINE('',#100910,#21640);
#15607=LINE('',#100911,#21641);
#15608=LINE('',#100914,#21642);
#15609=LINE('',#100916,#21643);
#15610=LINE('',#100917,#21644);
#15611=LINE('',#100920,#21645);
#15612=LINE('',#100922,#21646);
#15613=LINE('',#100923,#21647);
#15614=LINE('',#100926,#21648);
#15615=LINE('',#100928,#21649);
#15616=LINE('',#100929,#21650);
#15617=LINE('',#100932,#21651);
#15618=LINE('',#100934,#21652);
#15619=LINE('',#100935,#21653);
#15620=LINE('',#100938,#21654);
#15621=LINE('',#100940,#21655);
#15622=LINE('',#100941,#21656);
#15623=LINE('',#100944,#21657);
#15624=LINE('',#100946,#21658);
#15625=LINE('',#100947,#21659);
#15626=LINE('',#100950,#21660);
#15627=LINE('',#100952,#21661);
#15628=LINE('',#100953,#21662);
#15629=LINE('',#100956,#21663);
#15630=LINE('',#100958,#21664);
#15631=LINE('',#100959,#21665);
#15632=LINE('',#100962,#21666);
#15633=LINE('',#100964,#21667);
#15634=LINE('',#100965,#21668);
#15635=LINE('',#100968,#21669);
#15636=LINE('',#100970,#21670);
#15637=LINE('',#100971,#21671);
#15638=LINE('',#100974,#21672);
#15639=LINE('',#100976,#21673);
#15640=LINE('',#100977,#21674);
#15641=LINE('',#100980,#21675);
#15642=LINE('',#100982,#21676);
#15643=LINE('',#100983,#21677);
#15644=LINE('',#100986,#21678);
#15645=LINE('',#100988,#21679);
#15646=LINE('',#100989,#21680);
#15647=LINE('',#100992,#21681);
#15648=LINE('',#100994,#21682);
#15649=LINE('',#100995,#21683);
#15650=LINE('',#100998,#21684);
#15651=LINE('',#101000,#21685);
#15652=LINE('',#101001,#21686);
#15653=LINE('',#101004,#21687);
#15654=LINE('',#101006,#21688);
#15655=LINE('',#101007,#21689);
#15656=LINE('',#101010,#21690);
#15657=LINE('',#101012,#21691);
#15658=LINE('',#101013,#21692);
#15659=LINE('',#101016,#21693);
#15660=LINE('',#101018,#21694);
#15661=LINE('',#101019,#21695);
#15662=LINE('',#101022,#21696);
#15663=LINE('',#101024,#21697);
#15664=LINE('',#101025,#21698);
#15665=LINE('',#101028,#21699);
#15666=LINE('',#101030,#21700);
#15667=LINE('',#101031,#21701);
#15668=LINE('',#101034,#21702);
#15669=LINE('',#101036,#21703);
#15670=LINE('',#101037,#21704);
#15671=LINE('',#101040,#21705);
#15672=LINE('',#101042,#21706);
#15673=LINE('',#101043,#21707);
#15674=LINE('',#101046,#21708);
#15675=LINE('',#101048,#21709);
#15676=LINE('',#101049,#21710);
#15677=LINE('',#101052,#21711);
#15678=LINE('',#101054,#21712);
#15679=LINE('',#101055,#21713);
#15680=LINE('',#101058,#21714);
#15681=LINE('',#101060,#21715);
#15682=LINE('',#101061,#21716);
#15683=LINE('',#101064,#21717);
#15684=LINE('',#101066,#21718);
#15685=LINE('',#101067,#21719);
#15686=LINE('',#101070,#21720);
#15687=LINE('',#101072,#21721);
#15688=LINE('',#101073,#21722);
#15689=LINE('',#101076,#21723);
#15690=LINE('',#101078,#21724);
#15691=LINE('',#101079,#21725);
#15692=LINE('',#101082,#21726);
#15693=LINE('',#101084,#21727);
#15694=LINE('',#101085,#21728);
#15695=LINE('',#101088,#21729);
#15696=LINE('',#101090,#21730);
#15697=LINE('',#101091,#21731);
#15698=LINE('',#101094,#21732);
#15699=LINE('',#101096,#21733);
#15700=LINE('',#101097,#21734);
#15701=LINE('',#101100,#21735);
#15702=LINE('',#101102,#21736);
#15703=LINE('',#101103,#21737);
#15704=LINE('',#101106,#21738);
#15705=LINE('',#101108,#21739);
#15706=LINE('',#101109,#21740);
#15707=LINE('',#101112,#21741);
#15708=LINE('',#101114,#21742);
#15709=LINE('',#101115,#21743);
#15710=LINE('',#101118,#21744);
#15711=LINE('',#101120,#21745);
#15712=LINE('',#101121,#21746);
#15713=LINE('',#101124,#21747);
#15714=LINE('',#101126,#21748);
#15715=LINE('',#101127,#21749);
#15716=LINE('',#101130,#21750);
#15717=LINE('',#101132,#21751);
#15718=LINE('',#101133,#21752);
#15719=LINE('',#101136,#21753);
#15720=LINE('',#101138,#21754);
#15721=LINE('',#101139,#21755);
#15722=LINE('',#101142,#21756);
#15723=LINE('',#101144,#21757);
#15724=LINE('',#101145,#21758);
#15725=LINE('',#101148,#21759);
#15726=LINE('',#101150,#21760);
#15727=LINE('',#101151,#21761);
#15728=LINE('',#101154,#21762);
#15729=LINE('',#101156,#21763);
#15730=LINE('',#101157,#21764);
#15731=LINE('',#101160,#21765);
#15732=LINE('',#101162,#21766);
#15733=LINE('',#101163,#21767);
#15734=LINE('',#101166,#21768);
#15735=LINE('',#101168,#21769);
#15736=LINE('',#101169,#21770);
#15737=LINE('',#101172,#21771);
#15738=LINE('',#101174,#21772);
#15739=LINE('',#101175,#21773);
#15740=LINE('',#101178,#21774);
#15741=LINE('',#101180,#21775);
#15742=LINE('',#101181,#21776);
#15743=LINE('',#101184,#21777);
#15744=LINE('',#101186,#21778);
#15745=LINE('',#101187,#21779);
#15746=LINE('',#101190,#21780);
#15747=LINE('',#101192,#21781);
#15748=LINE('',#101193,#21782);
#15749=LINE('',#101196,#21783);
#15750=LINE('',#101198,#21784);
#15751=LINE('',#101199,#21785);
#15752=LINE('',#101202,#21786);
#15753=LINE('',#101204,#21787);
#15754=LINE('',#101205,#21788);
#15755=LINE('',#101208,#21789);
#15756=LINE('',#101210,#21790);
#15757=LINE('',#101211,#21791);
#15758=LINE('',#101214,#21792);
#15759=LINE('',#101216,#21793);
#15760=LINE('',#101217,#21794);
#15761=LINE('',#101220,#21795);
#15762=LINE('',#101222,#21796);
#15763=LINE('',#101223,#21797);
#15764=LINE('',#101226,#21798);
#15765=LINE('',#101228,#21799);
#15766=LINE('',#101229,#21800);
#15767=LINE('',#101232,#21801);
#15768=LINE('',#101234,#21802);
#15769=LINE('',#101235,#21803);
#15770=LINE('',#101238,#21804);
#15771=LINE('',#101240,#21805);
#15772=LINE('',#101241,#21806);
#15773=LINE('',#101244,#21807);
#15774=LINE('',#101246,#21808);
#15775=LINE('',#101247,#21809);
#15776=LINE('',#101250,#21810);
#15777=LINE('',#101252,#21811);
#15778=LINE('',#101253,#21812);
#15779=LINE('',#101256,#21813);
#15780=LINE('',#101258,#21814);
#15781=LINE('',#101259,#21815);
#15782=LINE('',#101262,#21816);
#15783=LINE('',#101264,#21817);
#15784=LINE('',#101265,#21818);
#15785=LINE('',#101268,#21819);
#15786=LINE('',#101270,#21820);
#15787=LINE('',#101271,#21821);
#15788=LINE('',#101274,#21822);
#15789=LINE('',#101276,#21823);
#15790=LINE('',#101277,#21824);
#15791=LINE('',#101280,#21825);
#15792=LINE('',#101282,#21826);
#15793=LINE('',#101283,#21827);
#15794=LINE('',#101286,#21828);
#15795=LINE('',#101288,#21829);
#15796=LINE('',#101289,#21830);
#15797=LINE('',#101292,#21831);
#15798=LINE('',#101294,#21832);
#15799=LINE('',#101295,#21833);
#15800=LINE('',#101298,#21834);
#15801=LINE('',#101300,#21835);
#15802=LINE('',#101301,#21836);
#15803=LINE('',#101304,#21837);
#15804=LINE('',#101306,#21838);
#15805=LINE('',#101307,#21839);
#15806=LINE('',#101310,#21840);
#15807=LINE('',#101312,#21841);
#15808=LINE('',#101313,#21842);
#15809=LINE('',#101316,#21843);
#15810=LINE('',#101318,#21844);
#15811=LINE('',#101319,#21845);
#15812=LINE('',#101322,#21846);
#15813=LINE('',#101324,#21847);
#15814=LINE('',#101325,#21848);
#15815=LINE('',#101328,#21849);
#15816=LINE('',#101330,#21850);
#15817=LINE('',#101331,#21851);
#15818=LINE('',#101334,#21852);
#15819=LINE('',#101336,#21853);
#15820=LINE('',#101337,#21854);
#15821=LINE('',#101340,#21855);
#15822=LINE('',#101342,#21856);
#15823=LINE('',#101343,#21857);
#15824=LINE('',#101346,#21858);
#15825=LINE('',#101348,#21859);
#15826=LINE('',#101349,#21860);
#15827=LINE('',#101352,#21861);
#15828=LINE('',#101354,#21862);
#15829=LINE('',#101355,#21863);
#15830=LINE('',#101358,#21864);
#15831=LINE('',#101360,#21865);
#15832=LINE('',#101361,#21866);
#15833=LINE('',#101364,#21867);
#15834=LINE('',#101366,#21868);
#15835=LINE('',#101367,#21869);
#15836=LINE('',#101370,#21870);
#15837=LINE('',#101372,#21871);
#15838=LINE('',#101373,#21872);
#15839=LINE('',#101376,#21873);
#15840=LINE('',#101378,#21874);
#15841=LINE('',#101379,#21875);
#15842=LINE('',#101382,#21876);
#15843=LINE('',#101384,#21877);
#15844=LINE('',#101385,#21878);
#15845=LINE('',#101388,#21879);
#15846=LINE('',#101390,#21880);
#15847=LINE('',#101391,#21881);
#15848=LINE('',#101394,#21882);
#15849=LINE('',#101396,#21883);
#15850=LINE('',#101397,#21884);
#15851=LINE('',#101400,#21885);
#15852=LINE('',#101402,#21886);
#15853=LINE('',#101403,#21887);
#15854=LINE('',#101406,#21888);
#15855=LINE('',#101408,#21889);
#15856=LINE('',#101409,#21890);
#15857=LINE('',#101412,#21891);
#15858=LINE('',#101414,#21892);
#15859=LINE('',#101415,#21893);
#15860=LINE('',#101418,#21894);
#15861=LINE('',#101420,#21895);
#15862=LINE('',#101421,#21896);
#15863=LINE('',#101424,#21897);
#15864=LINE('',#101426,#21898);
#15865=LINE('',#101427,#21899);
#15866=LINE('',#101430,#21900);
#15867=LINE('',#101432,#21901);
#15868=LINE('',#101433,#21902);
#15869=LINE('',#101436,#21903);
#15870=LINE('',#101438,#21904);
#15871=LINE('',#101439,#21905);
#15872=LINE('',#101442,#21906);
#15873=LINE('',#101444,#21907);
#15874=LINE('',#101445,#21908);
#15875=LINE('',#101448,#21909);
#15876=LINE('',#101450,#21910);
#15877=LINE('',#101451,#21911);
#15878=LINE('',#101454,#21912);
#15879=LINE('',#101456,#21913);
#15880=LINE('',#101457,#21914);
#15881=LINE('',#101460,#21915);
#15882=LINE('',#101462,#21916);
#15883=LINE('',#101463,#21917);
#15884=LINE('',#101466,#21918);
#15885=LINE('',#101468,#21919);
#15886=LINE('',#101469,#21920);
#15887=LINE('',#101472,#21921);
#15888=LINE('',#101474,#21922);
#15889=LINE('',#101475,#21923);
#15890=LINE('',#101478,#21924);
#15891=LINE('',#101480,#21925);
#15892=LINE('',#101481,#21926);
#15893=LINE('',#101484,#21927);
#15894=LINE('',#101486,#21928);
#15895=LINE('',#101487,#21929);
#15896=LINE('',#101490,#21930);
#15897=LINE('',#101492,#21931);
#15898=LINE('',#101493,#21932);
#15899=LINE('',#101496,#21933);
#15900=LINE('',#101498,#21934);
#15901=LINE('',#101499,#21935);
#15902=LINE('',#101502,#21936);
#15903=LINE('',#101504,#21937);
#15904=LINE('',#101505,#21938);
#15905=LINE('',#101508,#21939);
#15906=LINE('',#101510,#21940);
#15907=LINE('',#101511,#21941);
#15908=LINE('',#101514,#21942);
#15909=LINE('',#101516,#21943);
#15910=LINE('',#101517,#21944);
#15911=LINE('',#101520,#21945);
#15912=LINE('',#101522,#21946);
#15913=LINE('',#101523,#21947);
#15914=LINE('',#101526,#21948);
#15915=LINE('',#101528,#21949);
#15916=LINE('',#101529,#21950);
#15917=LINE('',#101532,#21951);
#15918=LINE('',#101534,#21952);
#15919=LINE('',#101535,#21953);
#15920=LINE('',#101538,#21954);
#15921=LINE('',#101540,#21955);
#15922=LINE('',#101541,#21956);
#15923=LINE('',#101544,#21957);
#15924=LINE('',#101546,#21958);
#15925=LINE('',#101547,#21959);
#15926=LINE('',#101550,#21960);
#15927=LINE('',#101552,#21961);
#15928=LINE('',#101553,#21962);
#15929=LINE('',#101556,#21963);
#15930=LINE('',#101558,#21964);
#15931=LINE('',#101559,#21965);
#15932=LINE('',#101562,#21966);
#15933=LINE('',#101564,#21967);
#15934=LINE('',#101565,#21968);
#15935=LINE('',#101568,#21969);
#15936=LINE('',#101570,#21970);
#15937=LINE('',#101571,#21971);
#15938=LINE('',#101574,#21972);
#15939=LINE('',#101576,#21973);
#15940=LINE('',#101577,#21974);
#15941=LINE('',#101580,#21975);
#15942=LINE('',#101582,#21976);
#15943=LINE('',#101583,#21977);
#15944=LINE('',#101586,#21978);
#15945=LINE('',#101588,#21979);
#15946=LINE('',#101589,#21980);
#15947=LINE('',#101592,#21981);
#15948=LINE('',#101594,#21982);
#15949=LINE('',#101595,#21983);
#15950=LINE('',#101598,#21984);
#15951=LINE('',#101600,#21985);
#15952=LINE('',#101601,#21986);
#15953=LINE('',#101604,#21987);
#15954=LINE('',#101606,#21988);
#15955=LINE('',#101607,#21989);
#15956=LINE('',#101610,#21990);
#15957=LINE('',#101612,#21991);
#15958=LINE('',#101613,#21992);
#15959=LINE('',#101616,#21993);
#15960=LINE('',#101618,#21994);
#15961=LINE('',#101619,#21995);
#15962=LINE('',#101622,#21996);
#15963=LINE('',#101624,#21997);
#15964=LINE('',#101625,#21998);
#15965=LINE('',#101628,#21999);
#15966=LINE('',#101630,#22000);
#15967=LINE('',#101631,#22001);
#15968=LINE('',#101634,#22002);
#15969=LINE('',#101636,#22003);
#15970=LINE('',#101637,#22004);
#15971=LINE('',#101640,#22005);
#15972=LINE('',#101642,#22006);
#15973=LINE('',#101643,#22007);
#15974=LINE('',#101646,#22008);
#15975=LINE('',#101648,#22009);
#15976=LINE('',#101649,#22010);
#15977=LINE('',#101652,#22011);
#15978=LINE('',#101654,#22012);
#15979=LINE('',#101655,#22013);
#15980=LINE('',#101658,#22014);
#15981=LINE('',#101660,#22015);
#15982=LINE('',#101661,#22016);
#15983=LINE('',#101664,#22017);
#15984=LINE('',#101666,#22018);
#15985=LINE('',#101667,#22019);
#15986=LINE('',#101670,#22020);
#15987=LINE('',#101672,#22021);
#15988=LINE('',#101673,#22022);
#15989=LINE('',#101676,#22023);
#15990=LINE('',#101678,#22024);
#15991=LINE('',#101679,#22025);
#15992=LINE('',#101682,#22026);
#15993=LINE('',#101684,#22027);
#15994=LINE('',#101685,#22028);
#15995=LINE('',#101688,#22029);
#15996=LINE('',#101690,#22030);
#15997=LINE('',#101691,#22031);
#15998=LINE('',#101694,#22032);
#15999=LINE('',#101696,#22033);
#16000=LINE('',#101697,#22034);
#16001=LINE('',#101700,#22035);
#16002=LINE('',#101702,#22036);
#16003=LINE('',#101703,#22037);
#16004=LINE('',#101706,#22038);
#16005=LINE('',#101708,#22039);
#16006=LINE('',#101709,#22040);
#16007=LINE('',#101712,#22041);
#16008=LINE('',#101714,#22042);
#16009=LINE('',#101715,#22043);
#16010=LINE('',#101718,#22044);
#16011=LINE('',#101720,#22045);
#16012=LINE('',#101721,#22046);
#16013=LINE('',#101724,#22047);
#16014=LINE('',#101726,#22048);
#16015=LINE('',#101727,#22049);
#16016=LINE('',#101730,#22050);
#16017=LINE('',#101732,#22051);
#16018=LINE('',#101733,#22052);
#16019=LINE('',#101736,#22053);
#16020=LINE('',#101738,#22054);
#16021=LINE('',#101739,#22055);
#16022=LINE('',#101742,#22056);
#16023=LINE('',#101744,#22057);
#16024=LINE('',#101745,#22058);
#16025=LINE('',#101748,#22059);
#16026=LINE('',#101750,#22060);
#16027=LINE('',#101751,#22061);
#16028=LINE('',#101754,#22062);
#16029=LINE('',#101756,#22063);
#16030=LINE('',#101757,#22064);
#16031=LINE('',#101760,#22065);
#16032=LINE('',#101762,#22066);
#16033=LINE('',#101763,#22067);
#16034=LINE('',#101766,#22068);
#16035=LINE('',#101768,#22069);
#16036=LINE('',#101769,#22070);
#16037=LINE('',#101772,#22071);
#16038=LINE('',#101774,#22072);
#16039=LINE('',#101775,#22073);
#16040=LINE('',#101778,#22074);
#16041=LINE('',#101780,#22075);
#16042=LINE('',#101781,#22076);
#16043=LINE('',#101784,#22077);
#16044=LINE('',#101786,#22078);
#16045=LINE('',#101787,#22079);
#16046=LINE('',#101790,#22080);
#16047=LINE('',#101792,#22081);
#16048=LINE('',#101793,#22082);
#16049=LINE('',#101796,#22083);
#16050=LINE('',#101798,#22084);
#16051=LINE('',#101799,#22085);
#16052=LINE('',#101802,#22086);
#16053=LINE('',#101804,#22087);
#16054=LINE('',#101805,#22088);
#16055=LINE('',#101808,#22089);
#16056=LINE('',#101810,#22090);
#16057=LINE('',#101811,#22091);
#16058=LINE('',#101814,#22092);
#16059=LINE('',#101816,#22093);
#16060=LINE('',#101817,#22094);
#16061=LINE('',#101820,#22095);
#16062=LINE('',#101822,#22096);
#16063=LINE('',#101823,#22097);
#16064=LINE('',#101826,#22098);
#16065=LINE('',#101828,#22099);
#16066=LINE('',#101829,#22100);
#16067=LINE('',#101832,#22101);
#16068=LINE('',#101834,#22102);
#16069=LINE('',#101835,#22103);
#16070=LINE('',#101838,#22104);
#16071=LINE('',#101840,#22105);
#16072=LINE('',#101841,#22106);
#16073=LINE('',#101844,#22107);
#16074=LINE('',#101846,#22108);
#16075=LINE('',#101847,#22109);
#16076=LINE('',#101850,#22110);
#16077=LINE('',#101852,#22111);
#16078=LINE('',#101853,#22112);
#16079=LINE('',#101856,#22113);
#16080=LINE('',#101858,#22114);
#16081=LINE('',#101859,#22115);
#16082=LINE('',#101862,#22116);
#16083=LINE('',#101864,#22117);
#16084=LINE('',#101865,#22118);
#16085=LINE('',#101868,#22119);
#16086=LINE('',#101870,#22120);
#16087=LINE('',#101871,#22121);
#16088=LINE('',#101874,#22122);
#16089=LINE('',#101876,#22123);
#16090=LINE('',#101877,#22124);
#16091=LINE('',#101880,#22125);
#16092=LINE('',#101882,#22126);
#16093=LINE('',#101883,#22127);
#16094=LINE('',#101886,#22128);
#16095=LINE('',#101888,#22129);
#16096=LINE('',#101889,#22130);
#16097=LINE('',#101892,#22131);
#16098=LINE('',#101894,#22132);
#16099=LINE('',#101895,#22133);
#16100=LINE('',#101898,#22134);
#16101=LINE('',#101900,#22135);
#16102=LINE('',#101901,#22136);
#16103=LINE('',#101904,#22137);
#16104=LINE('',#101906,#22138);
#16105=LINE('',#101907,#22139);
#16106=LINE('',#101910,#22140);
#16107=LINE('',#101912,#22141);
#16108=LINE('',#101913,#22142);
#16109=LINE('',#101916,#22143);
#16110=LINE('',#101918,#22144);
#16111=LINE('',#101919,#22145);
#16112=LINE('',#101922,#22146);
#16113=LINE('',#101924,#22147);
#16114=LINE('',#101925,#22148);
#16115=LINE('',#101928,#22149);
#16116=LINE('',#101930,#22150);
#16117=LINE('',#101931,#22151);
#16118=LINE('',#101934,#22152);
#16119=LINE('',#101936,#22153);
#16120=LINE('',#101937,#22154);
#16121=LINE('',#101940,#22155);
#16122=LINE('',#101942,#22156);
#16123=LINE('',#101943,#22157);
#16124=LINE('',#101946,#22158);
#16125=LINE('',#101948,#22159);
#16126=LINE('',#101949,#22160);
#16127=LINE('',#101952,#22161);
#16128=LINE('',#101954,#22162);
#16129=LINE('',#101955,#22163);
#16130=LINE('',#101958,#22164);
#16131=LINE('',#101960,#22165);
#16132=LINE('',#101961,#22166);
#16133=LINE('',#101964,#22167);
#16134=LINE('',#101966,#22168);
#16135=LINE('',#101967,#22169);
#16136=LINE('',#101970,#22170);
#16137=LINE('',#101972,#22171);
#16138=LINE('',#101973,#22172);
#16139=LINE('',#101976,#22173);
#16140=LINE('',#101978,#22174);
#16141=LINE('',#101979,#22175);
#16142=LINE('',#101982,#22176);
#16143=LINE('',#101984,#22177);
#16144=LINE('',#101985,#22178);
#16145=LINE('',#101988,#22179);
#16146=LINE('',#101990,#22180);
#16147=LINE('',#101991,#22181);
#16148=LINE('',#101994,#22182);
#16149=LINE('',#101996,#22183);
#16150=LINE('',#101997,#22184);
#16151=LINE('',#102000,#22185);
#16152=LINE('',#102002,#22186);
#16153=LINE('',#102003,#22187);
#16154=LINE('',#102006,#22188);
#16155=LINE('',#102008,#22189);
#16156=LINE('',#102009,#22190);
#16157=LINE('',#102011,#22191);
#16158=LINE('',#102012,#22192);
#16159=LINE('',#102014,#22193);
#16160=LINE('',#102015,#22194);
#20671=VECTOR('',#71117,2.65000000000001);
#20672=VECTOR('',#71122,2.5);
#20673=VECTOR('',#71127,10.);
#20674=VECTOR('',#71128,10.);
#20675=VECTOR('',#71129,10.);
#20676=VECTOR('',#71130,10.);
#20677=VECTOR('',#71135,2.65);
#20678=VECTOR('',#71140,2.5);
#20679=VECTOR('',#71145,10.);
#20680=VECTOR('',#71146,10.);
#20681=VECTOR('',#71147,10.);
#20682=VECTOR('',#71148,10.);
#20683=VECTOR('',#71159,1.45);
#20684=VECTOR('',#71164,1.45);
#20685=VECTOR('',#71169,10.);
#20686=VECTOR('',#71170,10.);
#20687=VECTOR('',#71171,10.);
#20688=VECTOR('',#71172,10.);
#20689=VECTOR('',#71175,10.);
#20690=VECTOR('',#71176,10.);
#20691=VECTOR('',#71177,10.);
#20692=VECTOR('',#71178,10.);
#20693=VECTOR('',#71181,10.);
#20694=VECTOR('',#71182,10.);
#20695=VECTOR('',#71185,10.);
#20696=VECTOR('',#71186,10.);
#20697=VECTOR('',#71189,10.);
#20698=VECTOR('',#71190,10.);
#20699=VECTOR('',#71191,10.);
#20700=VECTOR('',#71194,10.);
#20701=VECTOR('',#71195,10.);
#20702=VECTOR('',#71196,10.);
#20703=VECTOR('',#71199,10.);
#20704=VECTOR('',#71200,10.);
#20705=VECTOR('',#71201,10.);
#20706=VECTOR('',#71204,10.);
#20707=VECTOR('',#71205,10.);
#20708=VECTOR('',#71206,10.);
#20709=VECTOR('',#71209,10.);
#20710=VECTOR('',#71210,10.);
#20711=VECTOR('',#71211,10.);
#20712=VECTOR('',#71214,10.);
#20713=VECTOR('',#71215,10.);
#20714=VECTOR('',#71216,10.);
#20715=VECTOR('',#71219,10.);
#20716=VECTOR('',#71220,10.);
#20717=VECTOR('',#71221,10.);
#20718=VECTOR('',#71224,10.);
#20719=VECTOR('',#71225,10.);
#20720=VECTOR('',#71226,10.);
#20721=VECTOR('',#71229,10.);
#20722=VECTOR('',#71230,10.);
#20723=VECTOR('',#71231,10.);
#20724=VECTOR('',#71234,10.);
#20725=VECTOR('',#71235,10.);
#20726=VECTOR('',#71236,10.);
#20727=VECTOR('',#71239,10.);
#20728=VECTOR('',#71240,10.);
#20729=VECTOR('',#71241,10.);
#20730=VECTOR('',#71244,10.);
#20731=VECTOR('',#71245,10.);
#20732=VECTOR('',#71246,10.);
#20733=VECTOR('',#71249,10.);
#20734=VECTOR('',#71250,10.);
#20735=VECTOR('',#71251,10.);
#20736=VECTOR('',#71254,10.);
#20737=VECTOR('',#71255,10.);
#20738=VECTOR('',#71256,10.);
#20739=VECTOR('',#71259,10.);
#20740=VECTOR('',#71260,10.);
#20741=VECTOR('',#71261,10.);
#20742=VECTOR('',#71264,10.);
#20743=VECTOR('',#71265,10.);
#20744=VECTOR('',#71266,10.);
#20745=VECTOR('',#71269,10.);
#20746=VECTOR('',#71270,10.);
#20747=VECTOR('',#71271,10.);
#20748=VECTOR('',#71274,10.);
#20749=VECTOR('',#71275,10.);
#20750=VECTOR('',#71276,10.);
#20751=VECTOR('',#71279,10.);
#20752=VECTOR('',#71280,10.);
#20753=VECTOR('',#71281,10.);
#20754=VECTOR('',#71284,10.);
#20755=VECTOR('',#71285,10.);
#20756=VECTOR('',#71286,10.);
#20757=VECTOR('',#71289,10.);
#20758=VECTOR('',#71290,10.);
#20759=VECTOR('',#71291,10.);
#20760=VECTOR('',#71294,10.);
#20761=VECTOR('',#71295,10.);
#20762=VECTOR('',#71296,10.);
#20763=VECTOR('',#71299,10.);
#20764=VECTOR('',#71300,10.);
#20765=VECTOR('',#71301,10.);
#20766=VECTOR('',#71304,10.);
#20767=VECTOR('',#71305,10.);
#20768=VECTOR('',#71306,10.);
#20769=VECTOR('',#71309,10.);
#20770=VECTOR('',#71310,10.);
#20771=VECTOR('',#71311,10.);
#20772=VECTOR('',#71314,10.);
#20773=VECTOR('',#71315,10.);
#20774=VECTOR('',#71316,10.);
#20775=VECTOR('',#71319,10.);
#20776=VECTOR('',#71320,10.);
#20777=VECTOR('',#71321,10.);
#20778=VECTOR('',#71324,10.);
#20779=VECTOR('',#71325,10.);
#20780=VECTOR('',#71326,10.);
#20781=VECTOR('',#71329,10.);
#20782=VECTOR('',#71330,10.);
#20783=VECTOR('',#71331,10.);
#20784=VECTOR('',#71334,10.);
#20785=VECTOR('',#71335,10.);
#20786=VECTOR('',#71336,10.);
#20787=VECTOR('',#71339,10.);
#20788=VECTOR('',#71340,10.);
#20789=VECTOR('',#71341,10.);
#20790=VECTOR('',#71344,10.);
#20791=VECTOR('',#71345,10.);
#20792=VECTOR('',#71346,10.);
#20793=VECTOR('',#71349,10.);
#20794=VECTOR('',#71350,10.);
#20795=VECTOR('',#71351,10.);
#20796=VECTOR('',#71354,10.);
#20797=VECTOR('',#71355,10.);
#20798=VECTOR('',#71356,10.);
#20799=VECTOR('',#71359,10.);
#20800=VECTOR('',#71360,10.);
#20801=VECTOR('',#71361,10.);
#20802=VECTOR('',#71364,10.);
#20803=VECTOR('',#71365,10.);
#20804=VECTOR('',#71366,10.);
#20805=VECTOR('',#71369,10.);
#20806=VECTOR('',#71370,10.);
#20807=VECTOR('',#71371,10.);
#20808=VECTOR('',#71374,10.);
#20809=VECTOR('',#71375,10.);
#20810=VECTOR('',#71376,10.);
#20811=VECTOR('',#71379,10.);
#20812=VECTOR('',#71380,10.);
#20813=VECTOR('',#71381,10.);
#20814=VECTOR('',#71384,10.);
#20815=VECTOR('',#71385,10.);
#20816=VECTOR('',#71386,10.);
#20817=VECTOR('',#71389,10.);
#20818=VECTOR('',#71390,10.);
#20819=VECTOR('',#71391,10.);
#20820=VECTOR('',#71394,10.);
#20821=VECTOR('',#71395,10.);
#20822=VECTOR('',#71396,10.);
#20823=VECTOR('',#71399,10.);
#20824=VECTOR('',#71400,10.);
#20825=VECTOR('',#71401,10.);
#20826=VECTOR('',#71404,10.);
#20827=VECTOR('',#71405,10.);
#20828=VECTOR('',#71406,10.);
#20829=VECTOR('',#71409,10.);
#20830=VECTOR('',#71410,10.);
#20831=VECTOR('',#71411,10.);
#20832=VECTOR('',#71414,10.);
#20833=VECTOR('',#71415,10.);
#20834=VECTOR('',#71416,10.);
#20835=VECTOR('',#71419,10.);
#20836=VECTOR('',#71420,10.);
#20837=VECTOR('',#71421,10.);
#20838=VECTOR('',#71424,10.);
#20839=VECTOR('',#71425,10.);
#20840=VECTOR('',#71426,10.);
#20841=VECTOR('',#71429,10.);
#20842=VECTOR('',#71430,10.);
#20843=VECTOR('',#71431,10.);
#20844=VECTOR('',#71434,10.);
#20845=VECTOR('',#71435,10.);
#20846=VECTOR('',#71436,10.);
#20847=VECTOR('',#71439,10.);
#20848=VECTOR('',#71440,10.);
#20849=VECTOR('',#71441,10.);
#20850=VECTOR('',#71444,10.);
#20851=VECTOR('',#71445,10.);
#20852=VECTOR('',#71446,10.);
#20853=VECTOR('',#71449,10.);
#20854=VECTOR('',#71450,10.);
#20855=VECTOR('',#71451,10.);
#20856=VECTOR('',#71454,10.);
#20857=VECTOR('',#71455,10.);
#20858=VECTOR('',#71456,10.);
#20859=VECTOR('',#71459,10.);
#20860=VECTOR('',#71460,10.);
#20861=VECTOR('',#71461,10.);
#20862=VECTOR('',#71464,10.);
#20863=VECTOR('',#71465,10.);
#20864=VECTOR('',#71466,10.);
#20865=VECTOR('',#71469,10.);
#20866=VECTOR('',#71470,10.);
#20867=VECTOR('',#71471,10.);
#20868=VECTOR('',#71474,10.);
#20869=VECTOR('',#71475,10.);
#20870=VECTOR('',#71476,10.);
#20871=VECTOR('',#71479,10.);
#20872=VECTOR('',#71480,10.);
#20873=VECTOR('',#71481,10.);
#20874=VECTOR('',#71484,10.);
#20875=VECTOR('',#71485,10.);
#20876=VECTOR('',#71486,10.);
#20877=VECTOR('',#71489,10.);
#20878=VECTOR('',#71490,10.);
#20879=VECTOR('',#71491,10.);
#20880=VECTOR('',#71494,10.);
#20881=VECTOR('',#71495,10.);
#20882=VECTOR('',#71496,10.);
#20883=VECTOR('',#71499,10.);
#20884=VECTOR('',#71500,10.);
#20885=VECTOR('',#71501,10.);
#20886=VECTOR('',#71504,10.);
#20887=VECTOR('',#71505,10.);
#20888=VECTOR('',#71506,10.);
#20889=VECTOR('',#71509,10.);
#20890=VECTOR('',#71510,10.);
#20891=VECTOR('',#71511,10.);
#20892=VECTOR('',#71514,10.);
#20893=VECTOR('',#71515,10.);
#20894=VECTOR('',#71516,10.);
#20895=VECTOR('',#71519,10.);
#20896=VECTOR('',#71520,10.);
#20897=VECTOR('',#71521,10.);
#20898=VECTOR('',#71524,10.);
#20899=VECTOR('',#71525,10.);
#20900=VECTOR('',#71526,10.);
#20901=VECTOR('',#71529,10.);
#20902=VECTOR('',#71530,10.);
#20903=VECTOR('',#71531,10.);
#20904=VECTOR('',#71534,10.);
#20905=VECTOR('',#71535,10.);
#20906=VECTOR('',#71536,10.);
#20907=VECTOR('',#71539,10.);
#20908=VECTOR('',#71540,10.);
#20909=VECTOR('',#71541,10.);
#20910=VECTOR('',#71544,10.);
#20911=VECTOR('',#71545,10.);
#20912=VECTOR('',#71546,10.);
#20913=VECTOR('',#71549,10.);
#20914=VECTOR('',#71550,10.);
#20915=VECTOR('',#71551,10.);
#20916=VECTOR('',#71554,10.);
#20917=VECTOR('',#71555,10.);
#20918=VECTOR('',#71556,10.);
#20919=VECTOR('',#71559,10.);
#20920=VECTOR('',#71560,10.);
#20921=VECTOR('',#71561,10.);
#20922=VECTOR('',#71564,10.);
#20923=VECTOR('',#71565,10.);
#20924=VECTOR('',#71566,10.);
#20925=VECTOR('',#71569,10.);
#20926=VECTOR('',#71570,10.);
#20927=VECTOR('',#71571,10.);
#20928=VECTOR('',#71574,10.);
#20929=VECTOR('',#71575,10.);
#20930=VECTOR('',#71576,10.);
#20931=VECTOR('',#71579,10.);
#20932=VECTOR('',#71580,10.);
#20933=VECTOR('',#71581,10.);
#20934=VECTOR('',#71584,10.);
#20935=VECTOR('',#71585,10.);
#20936=VECTOR('',#71586,10.);
#20937=VECTOR('',#71589,10.);
#20938=VECTOR('',#71590,10.);
#20939=VECTOR('',#71591,10.);
#20940=VECTOR('',#71594,10.);
#20941=VECTOR('',#71595,10.);
#20942=VECTOR('',#71596,10.);
#20943=VECTOR('',#71599,10.);
#20944=VECTOR('',#71600,10.);
#20945=VECTOR('',#71601,10.);
#20946=VECTOR('',#71604,10.);
#20947=VECTOR('',#71605,10.);
#20948=VECTOR('',#71606,10.);
#20949=VECTOR('',#71609,10.);
#20950=VECTOR('',#71610,10.);
#20951=VECTOR('',#71611,10.);
#20952=VECTOR('',#71614,10.);
#20953=VECTOR('',#71615,10.);
#20954=VECTOR('',#71616,10.);
#20955=VECTOR('',#71619,10.);
#20956=VECTOR('',#71620,10.);
#20957=VECTOR('',#71621,10.);
#20958=VECTOR('',#71624,10.);
#20959=VECTOR('',#71625,10.);
#20960=VECTOR('',#71626,10.);
#20961=VECTOR('',#71629,10.);
#20962=VECTOR('',#71630,10.);
#20963=VECTOR('',#71631,10.);
#20964=VECTOR('',#71634,10.);
#20965=VECTOR('',#71635,10.);
#20966=VECTOR('',#71636,10.);
#20967=VECTOR('',#71639,10.);
#20968=VECTOR('',#71640,10.);
#20969=VECTOR('',#71641,10.);
#20970=VECTOR('',#71644,10.);
#20971=VECTOR('',#71645,10.);
#20972=VECTOR('',#71646,10.);
#20973=VECTOR('',#71649,10.);
#20974=VECTOR('',#71650,10.);
#20975=VECTOR('',#71651,10.);
#20976=VECTOR('',#71654,10.);
#20977=VECTOR('',#71655,10.);
#20978=VECTOR('',#71656,10.);
#20979=VECTOR('',#71659,10.);
#20980=VECTOR('',#71660,10.);
#20981=VECTOR('',#71661,10.);
#20982=VECTOR('',#71664,10.);
#20983=VECTOR('',#71665,10.);
#20984=VECTOR('',#71666,10.);
#20985=VECTOR('',#71669,10.);
#20986=VECTOR('',#71670,10.);
#20987=VECTOR('',#71671,10.);
#20988=VECTOR('',#71674,10.);
#20989=VECTOR('',#71675,10.);
#20990=VECTOR('',#71676,10.);
#20991=VECTOR('',#71679,10.);
#20992=VECTOR('',#71680,10.);
#20993=VECTOR('',#71681,10.);
#20994=VECTOR('',#71684,10.);
#20995=VECTOR('',#71685,10.);
#20996=VECTOR('',#71686,10.);
#20997=VECTOR('',#71689,10.);
#20998=VECTOR('',#71690,10.);
#20999=VECTOR('',#71691,10.);
#21000=VECTOR('',#71694,10.);
#21001=VECTOR('',#71695,10.);
#21002=VECTOR('',#71696,10.);
#21003=VECTOR('',#71699,10.);
#21004=VECTOR('',#71700,10.);
#21005=VECTOR('',#71701,10.);
#21006=VECTOR('',#71704,10.);
#21007=VECTOR('',#71705,10.);
#21008=VECTOR('',#71706,10.);
#21009=VECTOR('',#71709,10.);
#21010=VECTOR('',#71710,10.);
#21011=VECTOR('',#71711,10.);
#21012=VECTOR('',#71714,10.);
#21013=VECTOR('',#71715,10.);
#21014=VECTOR('',#71716,10.);
#21015=VECTOR('',#71719,10.);
#21016=VECTOR('',#71720,10.);
#21017=VECTOR('',#71721,10.);
#21018=VECTOR('',#71724,10.);
#21019=VECTOR('',#71725,10.);
#21020=VECTOR('',#71726,10.);
#21021=VECTOR('',#71729,10.);
#21022=VECTOR('',#71730,10.);
#21023=VECTOR('',#71731,10.);
#21024=VECTOR('',#71734,10.);
#21025=VECTOR('',#71735,10.);
#21026=VECTOR('',#71736,10.);
#21027=VECTOR('',#71739,10.);
#21028=VECTOR('',#71740,10.);
#21029=VECTOR('',#71741,10.);
#21030=VECTOR('',#71744,10.);
#21031=VECTOR('',#71745,10.);
#21032=VECTOR('',#71746,10.);
#21033=VECTOR('',#71749,10.);
#21034=VECTOR('',#71750,10.);
#21035=VECTOR('',#71751,10.);
#21036=VECTOR('',#71754,10.);
#21037=VECTOR('',#71755,10.);
#21038=VECTOR('',#71756,10.);
#21039=VECTOR('',#71759,10.);
#21040=VECTOR('',#71760,10.);
#21041=VECTOR('',#71761,10.);
#21042=VECTOR('',#71764,10.);
#21043=VECTOR('',#71765,10.);
#21044=VECTOR('',#71766,10.);
#21045=VECTOR('',#71769,10.);
#21046=VECTOR('',#71770,10.);
#21047=VECTOR('',#71771,10.);
#21048=VECTOR('',#71774,10.);
#21049=VECTOR('',#71775,10.);
#21050=VECTOR('',#71776,10.);
#21051=VECTOR('',#71779,10.);
#21052=VECTOR('',#71780,10.);
#21053=VECTOR('',#71781,10.);
#21054=VECTOR('',#71784,10.);
#21055=VECTOR('',#71785,10.);
#21056=VECTOR('',#71786,10.);
#21057=VECTOR('',#71789,10.);
#21058=VECTOR('',#71790,10.);
#21059=VECTOR('',#71791,10.);
#21060=VECTOR('',#71794,10.);
#21061=VECTOR('',#71795,10.);
#21062=VECTOR('',#71796,10.);
#21063=VECTOR('',#71799,10.);
#21064=VECTOR('',#71800,10.);
#21065=VECTOR('',#71801,10.);
#21066=VECTOR('',#71804,10.);
#21067=VECTOR('',#71805,10.);
#21068=VECTOR('',#71806,10.);
#21069=VECTOR('',#71809,10.);
#21070=VECTOR('',#71810,10.);
#21071=VECTOR('',#71811,10.);
#21072=VECTOR('',#71814,10.);
#21073=VECTOR('',#71815,10.);
#21074=VECTOR('',#71816,10.);
#21075=VECTOR('',#71819,10.);
#21076=VECTOR('',#71820,10.);
#21077=VECTOR('',#71821,10.);
#21078=VECTOR('',#71824,10.);
#21079=VECTOR('',#71825,10.);
#21080=VECTOR('',#71826,10.);
#21081=VECTOR('',#71829,10.);
#21082=VECTOR('',#71830,10.);
#21083=VECTOR('',#71831,10.);
#21084=VECTOR('',#71834,10.);
#21085=VECTOR('',#71835,10.);
#21086=VECTOR('',#71836,10.);
#21087=VECTOR('',#71839,10.);
#21088=VECTOR('',#71840,10.);
#21089=VECTOR('',#71841,10.);
#21090=VECTOR('',#71844,10.);
#21091=VECTOR('',#71845,10.);
#21092=VECTOR('',#71846,10.);
#21093=VECTOR('',#71849,10.);
#21094=VECTOR('',#71850,10.);
#21095=VECTOR('',#71851,10.);
#21096=VECTOR('',#71854,10.);
#21097=VECTOR('',#71855,10.);
#21098=VECTOR('',#71856,10.);
#21099=VECTOR('',#71859,10.);
#21100=VECTOR('',#71860,10.);
#21101=VECTOR('',#71861,10.);
#21102=VECTOR('',#71864,10.);
#21103=VECTOR('',#71865,10.);
#21104=VECTOR('',#71866,10.);
#21105=VECTOR('',#71869,10.);
#21106=VECTOR('',#71870,10.);
#21107=VECTOR('',#71871,10.);
#21108=VECTOR('',#71874,10.);
#21109=VECTOR('',#71875,10.);
#21110=VECTOR('',#71876,10.);
#21111=VECTOR('',#71879,10.);
#21112=VECTOR('',#71880,10.);
#21113=VECTOR('',#71881,10.);
#21114=VECTOR('',#71884,10.);
#21115=VECTOR('',#71885,10.);
#21116=VECTOR('',#71886,10.);
#21117=VECTOR('',#71889,10.);
#21118=VECTOR('',#71890,10.);
#21119=VECTOR('',#71891,10.);
#21120=VECTOR('',#71894,10.);
#21121=VECTOR('',#71895,10.);
#21122=VECTOR('',#71896,10.);
#21123=VECTOR('',#71899,10.);
#21124=VECTOR('',#71900,10.);
#21125=VECTOR('',#71901,10.);
#21126=VECTOR('',#71904,10.);
#21127=VECTOR('',#71905,10.);
#21128=VECTOR('',#71906,10.);
#21129=VECTOR('',#71909,10.);
#21130=VECTOR('',#71910,10.);
#21131=VECTOR('',#71911,10.);
#21132=VECTOR('',#71914,10.);
#21133=VECTOR('',#71915,10.);
#21134=VECTOR('',#71916,10.);
#21135=VECTOR('',#71919,10.);
#21136=VECTOR('',#71920,10.);
#21137=VECTOR('',#71921,10.);
#21138=VECTOR('',#71924,10.);
#21139=VECTOR('',#71925,10.);
#21140=VECTOR('',#71926,10.);
#21141=VECTOR('',#71929,10.);
#21142=VECTOR('',#71930,10.);
#21143=VECTOR('',#71931,10.);
#21144=VECTOR('',#71934,10.);
#21145=VECTOR('',#71935,10.);
#21146=VECTOR('',#71936,10.);
#21147=VECTOR('',#71939,10.);
#21148=VECTOR('',#71940,10.);
#21149=VECTOR('',#71941,10.);
#21150=VECTOR('',#71944,10.);
#21151=VECTOR('',#71945,10.);
#21152=VECTOR('',#71946,10.);
#21153=VECTOR('',#71949,10.);
#21154=VECTOR('',#71950,10.);
#21155=VECTOR('',#71951,10.);
#21156=VECTOR('',#71954,10.);
#21157=VECTOR('',#71955,10.);
#21158=VECTOR('',#71956,10.);
#21159=VECTOR('',#71959,10.);
#21160=VECTOR('',#71960,10.);
#21161=VECTOR('',#71961,10.);
#21162=VECTOR('',#71964,10.);
#21163=VECTOR('',#71965,10.);
#21164=VECTOR('',#71966,10.);
#21165=VECTOR('',#71969,10.);
#21166=VECTOR('',#71970,10.);
#21167=VECTOR('',#71971,10.);
#21168=VECTOR('',#71974,10.);
#21169=VECTOR('',#71975,10.);
#21170=VECTOR('',#71976,10.);
#21171=VECTOR('',#71979,10.);
#21172=VECTOR('',#71980,10.);
#21173=VECTOR('',#71981,10.);
#21174=VECTOR('',#71984,10.);
#21175=VECTOR('',#71985,10.);
#21176=VECTOR('',#71986,10.);
#21177=VECTOR('',#71989,10.);
#21178=VECTOR('',#71990,10.);
#21179=VECTOR('',#71991,10.);
#21180=VECTOR('',#71994,10.);
#21181=VECTOR('',#71995,10.);
#21182=VECTOR('',#71996,10.);
#21183=VECTOR('',#71999,10.);
#21184=VECTOR('',#72000,10.);
#21185=VECTOR('',#72001,10.);
#21186=VECTOR('',#72004,10.);
#21187=VECTOR('',#72005,10.);
#21188=VECTOR('',#72006,10.);
#21189=VECTOR('',#72009,10.);
#21190=VECTOR('',#72010,10.);
#21191=VECTOR('',#72011,10.);
#21192=VECTOR('',#72014,10.);
#21193=VECTOR('',#72015,10.);
#21194=VECTOR('',#72016,10.);
#21195=VECTOR('',#72019,10.);
#21196=VECTOR('',#72020,10.);
#21197=VECTOR('',#72021,10.);
#21198=VECTOR('',#72024,10.);
#21199=VECTOR('',#72025,10.);
#21200=VECTOR('',#72026,10.);
#21201=VECTOR('',#72029,10.);
#21202=VECTOR('',#72030,10.);
#21203=VECTOR('',#72031,10.);
#21204=VECTOR('',#72034,10.);
#21205=VECTOR('',#72035,10.);
#21206=VECTOR('',#72036,10.);
#21207=VECTOR('',#72039,10.);
#21208=VECTOR('',#72040,10.);
#21209=VECTOR('',#72041,10.);
#21210=VECTOR('',#72044,10.);
#21211=VECTOR('',#72045,10.);
#21212=VECTOR('',#72046,10.);
#21213=VECTOR('',#72049,10.);
#21214=VECTOR('',#72050,10.);
#21215=VECTOR('',#72051,10.);
#21216=VECTOR('',#72054,10.);
#21217=VECTOR('',#72055,10.);
#21218=VECTOR('',#72056,10.);
#21219=VECTOR('',#72059,10.);
#21220=VECTOR('',#72060,10.);
#21221=VECTOR('',#72061,10.);
#21222=VECTOR('',#72064,10.);
#21223=VECTOR('',#72065,10.);
#21224=VECTOR('',#72066,10.);
#21225=VECTOR('',#72069,10.);
#21226=VECTOR('',#72070,10.);
#21227=VECTOR('',#72071,10.);
#21228=VECTOR('',#72074,10.);
#21229=VECTOR('',#72075,10.);
#21230=VECTOR('',#72076,10.);
#21231=VECTOR('',#72079,10.);
#21232=VECTOR('',#72080,10.);
#21233=VECTOR('',#72081,10.);
#21234=VECTOR('',#72084,10.);
#21235=VECTOR('',#72085,10.);
#21236=VECTOR('',#72086,10.);
#21237=VECTOR('',#72089,10.);
#21238=VECTOR('',#72090,10.);
#21239=VECTOR('',#72091,10.);
#21240=VECTOR('',#72094,10.);
#21241=VECTOR('',#72095,10.);
#21242=VECTOR('',#72096,10.);
#21243=VECTOR('',#72099,10.);
#21244=VECTOR('',#72100,10.);
#21245=VECTOR('',#72101,10.);
#21246=VECTOR('',#72104,10.);
#21247=VECTOR('',#72105,10.);
#21248=VECTOR('',#72106,10.);
#21249=VECTOR('',#72109,10.);
#21250=VECTOR('',#72110,10.);
#21251=VECTOR('',#72111,10.);
#21252=VECTOR('',#72114,10.);
#21253=VECTOR('',#72115,10.);
#21254=VECTOR('',#72116,10.);
#21255=VECTOR('',#72119,10.);
#21256=VECTOR('',#72120,10.);
#21257=VECTOR('',#72121,10.);
#21258=VECTOR('',#72124,10.);
#21259=VECTOR('',#72125,10.);
#21260=VECTOR('',#72126,10.);
#21261=VECTOR('',#72129,10.);
#21262=VECTOR('',#72130,10.);
#21263=VECTOR('',#72131,10.);
#21264=VECTOR('',#72134,10.);
#21265=VECTOR('',#72135,10.);
#21266=VECTOR('',#72136,10.);
#21267=VECTOR('',#72139,10.);
#21268=VECTOR('',#72140,10.);
#21269=VECTOR('',#72141,10.);
#21270=VECTOR('',#72144,10.);
#21271=VECTOR('',#72145,10.);
#21272=VECTOR('',#72146,10.);
#21273=VECTOR('',#72149,10.);
#21274=VECTOR('',#72150,10.);
#21275=VECTOR('',#72151,10.);
#21276=VECTOR('',#72154,10.);
#21277=VECTOR('',#72155,10.);
#21278=VECTOR('',#72156,10.);
#21279=VECTOR('',#72159,10.);
#21280=VECTOR('',#72160,10.);
#21281=VECTOR('',#72161,10.);
#21282=VECTOR('',#72164,10.);
#21283=VECTOR('',#72165,10.);
#21284=VECTOR('',#72166,10.);
#21285=VECTOR('',#72169,10.);
#21286=VECTOR('',#72170,10.);
#21287=VECTOR('',#72171,10.);
#21288=VECTOR('',#72174,10.);
#21289=VECTOR('',#72175,10.);
#21290=VECTOR('',#72176,10.);
#21291=VECTOR('',#72179,10.);
#21292=VECTOR('',#72180,10.);
#21293=VECTOR('',#72181,10.);
#21294=VECTOR('',#72184,10.);
#21295=VECTOR('',#72185,10.);
#21296=VECTOR('',#72186,10.);
#21297=VECTOR('',#72189,10.);
#21298=VECTOR('',#72190,10.);
#21299=VECTOR('',#72191,10.);
#21300=VECTOR('',#72194,10.);
#21301=VECTOR('',#72195,10.);
#21302=VECTOR('',#72196,10.);
#21303=VECTOR('',#72199,10.);
#21304=VECTOR('',#72200,10.);
#21305=VECTOR('',#72201,10.);
#21306=VECTOR('',#72204,10.);
#21307=VECTOR('',#72205,10.);
#21308=VECTOR('',#72206,10.);
#21309=VECTOR('',#72209,10.);
#21310=VECTOR('',#72210,10.);
#21311=VECTOR('',#72211,10.);
#21312=VECTOR('',#72214,10.);
#21313=VECTOR('',#72215,10.);
#21314=VECTOR('',#72216,10.);
#21315=VECTOR('',#72219,10.);
#21316=VECTOR('',#72220,10.);
#21317=VECTOR('',#72221,10.);
#21318=VECTOR('',#72224,10.);
#21319=VECTOR('',#72225,10.);
#21320=VECTOR('',#72226,10.);
#21321=VECTOR('',#72229,10.);
#21322=VECTOR('',#72230,10.);
#21323=VECTOR('',#72231,10.);
#21324=VECTOR('',#72234,10.);
#21325=VECTOR('',#72235,10.);
#21326=VECTOR('',#72236,10.);
#21327=VECTOR('',#72239,10.);
#21328=VECTOR('',#72240,10.);
#21329=VECTOR('',#72241,10.);
#21330=VECTOR('',#72244,10.);
#21331=VECTOR('',#72245,10.);
#21332=VECTOR('',#72246,10.);
#21333=VECTOR('',#72249,10.);
#21334=VECTOR('',#72250,10.);
#21335=VECTOR('',#72251,10.);
#21336=VECTOR('',#72254,10.);
#21337=VECTOR('',#72255,10.);
#21338=VECTOR('',#72256,10.);
#21339=VECTOR('',#72259,10.);
#21340=VECTOR('',#72260,10.);
#21341=VECTOR('',#72261,10.);
#21342=VECTOR('',#72264,10.);
#21343=VECTOR('',#72265,10.);
#21344=VECTOR('',#72266,10.);
#21345=VECTOR('',#72269,10.);
#21346=VECTOR('',#72270,10.);
#21347=VECTOR('',#72271,10.);
#21348=VECTOR('',#72274,10.);
#21349=VECTOR('',#72275,10.);
#21350=VECTOR('',#72276,10.);
#21351=VECTOR('',#72279,10.);
#21352=VECTOR('',#72280,10.);
#21353=VECTOR('',#72281,10.);
#21354=VECTOR('',#72284,10.);
#21355=VECTOR('',#72285,10.);
#21356=VECTOR('',#72286,10.);
#21357=VECTOR('',#72289,10.);
#21358=VECTOR('',#72290,10.);
#21359=VECTOR('',#72291,10.);
#21360=VECTOR('',#72294,10.);
#21361=VECTOR('',#72295,10.);
#21362=VECTOR('',#72296,10.);
#21363=VECTOR('',#72299,10.);
#21364=VECTOR('',#72300,10.);
#21365=VECTOR('',#72301,10.);
#21366=VECTOR('',#72304,10.);
#21367=VECTOR('',#72305,10.);
#21368=VECTOR('',#72306,10.);
#21369=VECTOR('',#72309,10.);
#21370=VECTOR('',#72310,10.);
#21371=VECTOR('',#72311,10.);
#21372=VECTOR('',#72314,10.);
#21373=VECTOR('',#72315,10.);
#21374=VECTOR('',#72316,10.);
#21375=VECTOR('',#72319,10.);
#21376=VECTOR('',#72320,10.);
#21377=VECTOR('',#72321,10.);
#21378=VECTOR('',#72324,10.);
#21379=VECTOR('',#72325,10.);
#21380=VECTOR('',#72326,10.);
#21381=VECTOR('',#72329,10.);
#21382=VECTOR('',#72330,10.);
#21383=VECTOR('',#72331,10.);
#21384=VECTOR('',#72334,10.);
#21385=VECTOR('',#72335,10.);
#21386=VECTOR('',#72336,10.);
#21387=VECTOR('',#72339,10.);
#21388=VECTOR('',#72340,10.);
#21389=VECTOR('',#72341,10.);
#21390=VECTOR('',#72344,10.);
#21391=VECTOR('',#72345,10.);
#21392=VECTOR('',#72346,10.);
#21393=VECTOR('',#72349,10.);
#21394=VECTOR('',#72350,10.);
#21395=VECTOR('',#72351,10.);
#21396=VECTOR('',#72354,10.);
#21397=VECTOR('',#72355,10.);
#21398=VECTOR('',#72356,10.);
#21399=VECTOR('',#72359,10.);
#21400=VECTOR('',#72360,10.);
#21401=VECTOR('',#72361,10.);
#21402=VECTOR('',#72364,10.);
#21403=VECTOR('',#72365,10.);
#21404=VECTOR('',#72366,10.);
#21405=VECTOR('',#72369,10.);
#21406=VECTOR('',#72370,10.);
#21407=VECTOR('',#72371,10.);
#21408=VECTOR('',#72374,10.);
#21409=VECTOR('',#72375,10.);
#21410=VECTOR('',#72376,10.);
#21411=VECTOR('',#72379,10.);
#21412=VECTOR('',#72380,10.);
#21413=VECTOR('',#72381,10.);
#21414=VECTOR('',#72384,10.);
#21415=VECTOR('',#72385,10.);
#21416=VECTOR('',#72386,10.);
#21417=VECTOR('',#72389,10.);
#21418=VECTOR('',#72390,10.);
#21419=VECTOR('',#72391,10.);
#21420=VECTOR('',#72394,10.);
#21421=VECTOR('',#72395,10.);
#21422=VECTOR('',#72396,10.);
#21423=VECTOR('',#72399,10.);
#21424=VECTOR('',#72400,10.);
#21425=VECTOR('',#72401,10.);
#21426=VECTOR('',#72404,10.);
#21427=VECTOR('',#72405,10.);
#21428=VECTOR('',#72406,10.);
#21429=VECTOR('',#72409,10.);
#21430=VECTOR('',#72410,10.);
#21431=VECTOR('',#72411,10.);
#21432=VECTOR('',#72414,10.);
#21433=VECTOR('',#72415,10.);
#21434=VECTOR('',#72416,10.);
#21435=VECTOR('',#72419,10.);
#21436=VECTOR('',#72420,10.);
#21437=VECTOR('',#72421,10.);
#21438=VECTOR('',#72424,10.);
#21439=VECTOR('',#72425,10.);
#21440=VECTOR('',#72426,10.);
#21441=VECTOR('',#72429,10.);
#21442=VECTOR('',#72430,10.);
#21443=VECTOR('',#72431,10.);
#21444=VECTOR('',#72434,10.);
#21445=VECTOR('',#72435,10.);
#21446=VECTOR('',#72436,10.);
#21447=VECTOR('',#72439,10.);
#21448=VECTOR('',#72440,10.);
#21449=VECTOR('',#72441,10.);
#21450=VECTOR('',#72444,10.);
#21451=VECTOR('',#72445,10.);
#21452=VECTOR('',#72446,10.);
#21453=VECTOR('',#72449,10.);
#21454=VECTOR('',#72450,10.);
#21455=VECTOR('',#72451,10.);
#21456=VECTOR('',#72454,10.);
#21457=VECTOR('',#72455,10.);
#21458=VECTOR('',#72456,10.);
#21459=VECTOR('',#72459,10.);
#21460=VECTOR('',#72460,10.);
#21461=VECTOR('',#72461,10.);
#21462=VECTOR('',#72464,10.);
#21463=VECTOR('',#72465,10.);
#21464=VECTOR('',#72466,10.);
#21465=VECTOR('',#72469,10.);
#21466=VECTOR('',#72470,10.);
#21467=VECTOR('',#72471,10.);
#21468=VECTOR('',#72474,10.);
#21469=VECTOR('',#72475,10.);
#21470=VECTOR('',#72476,10.);
#21471=VECTOR('',#72479,10.);
#21472=VECTOR('',#72480,10.);
#21473=VECTOR('',#72481,10.);
#21474=VECTOR('',#72484,10.);
#21475=VECTOR('',#72485,10.);
#21476=VECTOR('',#72486,10.);
#21477=VECTOR('',#72489,10.);
#21478=VECTOR('',#72490,10.);
#21479=VECTOR('',#72491,10.);
#21480=VECTOR('',#72494,10.);
#21481=VECTOR('',#72495,10.);
#21482=VECTOR('',#72496,10.);
#21483=VECTOR('',#72499,10.);
#21484=VECTOR('',#72500,10.);
#21485=VECTOR('',#72501,10.);
#21486=VECTOR('',#72504,10.);
#21487=VECTOR('',#72505,10.);
#21488=VECTOR('',#72506,10.);
#21489=VECTOR('',#72509,10.);
#21490=VECTOR('',#72510,10.);
#21491=VECTOR('',#72511,10.);
#21492=VECTOR('',#72514,10.);
#21493=VECTOR('',#72515,10.);
#21494=VECTOR('',#72516,10.);
#21495=VECTOR('',#72519,10.);
#21496=VECTOR('',#72520,10.);
#21497=VECTOR('',#72521,10.);
#21498=VECTOR('',#72524,10.);
#21499=VECTOR('',#72525,10.);
#21500=VECTOR('',#72526,10.);
#21501=VECTOR('',#72529,10.);
#21502=VECTOR('',#72530,10.);
#21503=VECTOR('',#72531,10.);
#21504=VECTOR('',#72534,10.);
#21505=VECTOR('',#72535,10.);
#21506=VECTOR('',#72536,10.);
#21507=VECTOR('',#72539,10.);
#21508=VECTOR('',#72540,10.);
#21509=VECTOR('',#72541,10.);
#21510=VECTOR('',#72544,10.);
#21511=VECTOR('',#72545,10.);
#21512=VECTOR('',#72546,10.);
#21513=VECTOR('',#72549,10.);
#21514=VECTOR('',#72550,10.);
#21515=VECTOR('',#72551,10.);
#21516=VECTOR('',#72554,10.);
#21517=VECTOR('',#72555,10.);
#21518=VECTOR('',#72556,10.);
#21519=VECTOR('',#72559,10.);
#21520=VECTOR('',#72560,10.);
#21521=VECTOR('',#72561,10.);
#21522=VECTOR('',#72564,10.);
#21523=VECTOR('',#72565,10.);
#21524=VECTOR('',#72566,10.);
#21525=VECTOR('',#72569,10.);
#21526=VECTOR('',#72570,10.);
#21527=VECTOR('',#72571,10.);
#21528=VECTOR('',#72574,10.);
#21529=VECTOR('',#72575,10.);
#21530=VECTOR('',#72576,10.);
#21531=VECTOR('',#72579,10.);
#21532=VECTOR('',#72580,10.);
#21533=VECTOR('',#72581,10.);
#21534=VECTOR('',#72584,10.);
#21535=VECTOR('',#72585,10.);
#21536=VECTOR('',#72586,10.);
#21537=VECTOR('',#72589,10.);
#21538=VECTOR('',#72590,10.);
#21539=VECTOR('',#72591,10.);
#21540=VECTOR('',#72594,10.);
#21541=VECTOR('',#72595,10.);
#21542=VECTOR('',#72596,10.);
#21543=VECTOR('',#72599,10.);
#21544=VECTOR('',#72600,10.);
#21545=VECTOR('',#72601,10.);
#21546=VECTOR('',#72604,10.);
#21547=VECTOR('',#72605,10.);
#21548=VECTOR('',#72606,10.);
#21549=VECTOR('',#72609,10.);
#21550=VECTOR('',#72610,10.);
#21551=VECTOR('',#72611,10.);
#21552=VECTOR('',#72614,10.);
#21553=VECTOR('',#72615,10.);
#21554=VECTOR('',#72616,10.);
#21555=VECTOR('',#72619,10.);
#21556=VECTOR('',#72620,10.);
#21557=VECTOR('',#72621,10.);
#21558=VECTOR('',#72624,10.);
#21559=VECTOR('',#72625,10.);
#21560=VECTOR('',#72626,10.);
#21561=VECTOR('',#72629,10.);
#21562=VECTOR('',#72630,10.);
#21563=VECTOR('',#72631,10.);
#21564=VECTOR('',#72634,10.);
#21565=VECTOR('',#72635,10.);
#21566=VECTOR('',#72636,10.);
#21567=VECTOR('',#72639,10.);
#21568=VECTOR('',#72640,10.);
#21569=VECTOR('',#72641,10.);
#21570=VECTOR('',#72644,10.);
#21571=VECTOR('',#72645,10.);
#21572=VECTOR('',#72646,10.);
#21573=VECTOR('',#72649,10.);
#21574=VECTOR('',#72650,10.);
#21575=VECTOR('',#72651,10.);
#21576=VECTOR('',#72654,10.);
#21577=VECTOR('',#72655,10.);
#21578=VECTOR('',#72656,10.);
#21579=VECTOR('',#72659,10.);
#21580=VECTOR('',#72660,10.);
#21581=VECTOR('',#72661,10.);
#21582=VECTOR('',#72664,10.);
#21583=VECTOR('',#72665,10.);
#21584=VECTOR('',#72666,10.);
#21585=VECTOR('',#72669,10.);
#21586=VECTOR('',#72670,10.);
#21587=VECTOR('',#72671,10.);
#21588=VECTOR('',#72674,10.);
#21589=VECTOR('',#72675,10.);
#21590=VECTOR('',#72676,10.);
#21591=VECTOR('',#72679,10.);
#21592=VECTOR('',#72680,10.);
#21593=VECTOR('',#72681,10.);
#21594=VECTOR('',#72684,10.);
#21595=VECTOR('',#72685,10.);
#21596=VECTOR('',#72686,10.);
#21597=VECTOR('',#72689,10.);
#21598=VECTOR('',#72690,10.);
#21599=VECTOR('',#72691,10.);
#21600=VECTOR('',#72694,10.);
#21601=VECTOR('',#72695,10.);
#21602=VECTOR('',#72696,10.);
#21603=VECTOR('',#72699,10.);
#21604=VECTOR('',#72700,10.);
#21605=VECTOR('',#72701,10.);
#21606=VECTOR('',#72704,10.);
#21607=VECTOR('',#72705,10.);
#21608=VECTOR('',#72706,10.);
#21609=VECTOR('',#72709,10.);
#21610=VECTOR('',#72710,10.);
#21611=VECTOR('',#72711,10.);
#21612=VECTOR('',#72714,10.);
#21613=VECTOR('',#72715,10.);
#21614=VECTOR('',#72716,10.);
#21615=VECTOR('',#72719,10.);
#21616=VECTOR('',#72720,10.);
#21617=VECTOR('',#72721,10.);
#21618=VECTOR('',#72724,10.);
#21619=VECTOR('',#72725,10.);
#21620=VECTOR('',#72726,10.);
#21621=VECTOR('',#72729,10.);
#21622=VECTOR('',#72730,10.);
#21623=VECTOR('',#72731,10.);
#21624=VECTOR('',#72734,10.);
#21625=VECTOR('',#72735,10.);
#21626=VECTOR('',#72736,10.);
#21627=VECTOR('',#72739,10.);
#21628=VECTOR('',#72740,10.);
#21629=VECTOR('',#72741,10.);
#21630=VECTOR('',#72744,10.);
#21631=VECTOR('',#72745,10.);
#21632=VECTOR('',#72746,10.);
#21633=VECTOR('',#72749,10.);
#21634=VECTOR('',#72750,10.);
#21635=VECTOR('',#72751,10.);
#21636=VECTOR('',#72754,10.);
#21637=VECTOR('',#72755,10.);
#21638=VECTOR('',#72756,10.);
#21639=VECTOR('',#72759,10.);
#21640=VECTOR('',#72760,10.);
#21641=VECTOR('',#72761,10.);
#21642=VECTOR('',#72764,10.);
#21643=VECTOR('',#72765,10.);
#21644=VECTOR('',#72766,10.);
#21645=VECTOR('',#72769,10.);
#21646=VECTOR('',#72770,10.);
#21647=VECTOR('',#72771,10.);
#21648=VECTOR('',#72774,10.);
#21649=VECTOR('',#72775,10.);
#21650=VECTOR('',#72776,10.);
#21651=VECTOR('',#72779,10.);
#21652=VECTOR('',#72780,10.);
#21653=VECTOR('',#72781,10.);
#21654=VECTOR('',#72784,10.);
#21655=VECTOR('',#72785,10.);
#21656=VECTOR('',#72786,10.);
#21657=VECTOR('',#72789,10.);
#21658=VECTOR('',#72790,10.);
#21659=VECTOR('',#72791,10.);
#21660=VECTOR('',#72794,10.);
#21661=VECTOR('',#72795,10.);
#21662=VECTOR('',#72796,10.);
#21663=VECTOR('',#72799,10.);
#21664=VECTOR('',#72800,10.);
#21665=VECTOR('',#72801,10.);
#21666=VECTOR('',#72804,10.);
#21667=VECTOR('',#72805,10.);
#21668=VECTOR('',#72806,10.);
#21669=VECTOR('',#72809,10.);
#21670=VECTOR('',#72810,10.);
#21671=VECTOR('',#72811,10.);
#21672=VECTOR('',#72814,10.);
#21673=VECTOR('',#72815,10.);
#21674=VECTOR('',#72816,10.);
#21675=VECTOR('',#72819,10.);
#21676=VECTOR('',#72820,10.);
#21677=VECTOR('',#72821,10.);
#21678=VECTOR('',#72824,10.);
#21679=VECTOR('',#72825,10.);
#21680=VECTOR('',#72826,10.);
#21681=VECTOR('',#72829,10.);
#21682=VECTOR('',#72830,10.);
#21683=VECTOR('',#72831,10.);
#21684=VECTOR('',#72834,10.);
#21685=VECTOR('',#72835,10.);
#21686=VECTOR('',#72836,10.);
#21687=VECTOR('',#72839,10.);
#21688=VECTOR('',#72840,10.);
#21689=VECTOR('',#72841,10.);
#21690=VECTOR('',#72844,10.);
#21691=VECTOR('',#72845,10.);
#21692=VECTOR('',#72846,10.);
#21693=VECTOR('',#72849,10.);
#21694=VECTOR('',#72850,10.);
#21695=VECTOR('',#72851,10.);
#21696=VECTOR('',#72854,10.);
#21697=VECTOR('',#72855,10.);
#21698=VECTOR('',#72856,10.);
#21699=VECTOR('',#72859,10.);
#21700=VECTOR('',#72860,10.);
#21701=VECTOR('',#72861,10.);
#21702=VECTOR('',#72864,10.);
#21703=VECTOR('',#72865,10.);
#21704=VECTOR('',#72866,10.);
#21705=VECTOR('',#72869,10.);
#21706=VECTOR('',#72870,10.);
#21707=VECTOR('',#72871,10.);
#21708=VECTOR('',#72874,10.);
#21709=VECTOR('',#72875,10.);
#21710=VECTOR('',#72876,10.);
#21711=VECTOR('',#72879,10.);
#21712=VECTOR('',#72880,10.);
#21713=VECTOR('',#72881,10.);
#21714=VECTOR('',#72884,10.);
#21715=VECTOR('',#72885,10.);
#21716=VECTOR('',#72886,10.);
#21717=VECTOR('',#72889,10.);
#21718=VECTOR('',#72890,10.);
#21719=VECTOR('',#72891,10.);
#21720=VECTOR('',#72894,10.);
#21721=VECTOR('',#72895,10.);
#21722=VECTOR('',#72896,10.);
#21723=VECTOR('',#72899,10.);
#21724=VECTOR('',#72900,10.);
#21725=VECTOR('',#72901,10.);
#21726=VECTOR('',#72904,10.);
#21727=VECTOR('',#72905,10.);
#21728=VECTOR('',#72906,10.);
#21729=VECTOR('',#72909,10.);
#21730=VECTOR('',#72910,10.);
#21731=VECTOR('',#72911,10.);
#21732=VECTOR('',#72914,10.);
#21733=VECTOR('',#72915,10.);
#21734=VECTOR('',#72916,10.);
#21735=VECTOR('',#72919,10.);
#21736=VECTOR('',#72920,10.);
#21737=VECTOR('',#72921,10.);
#21738=VECTOR('',#72924,10.);
#21739=VECTOR('',#72925,10.);
#21740=VECTOR('',#72926,10.);
#21741=VECTOR('',#72929,10.);
#21742=VECTOR('',#72930,10.);
#21743=VECTOR('',#72931,10.);
#21744=VECTOR('',#72934,10.);
#21745=VECTOR('',#72935,10.);
#21746=VECTOR('',#72936,10.);
#21747=VECTOR('',#72939,10.);
#21748=VECTOR('',#72940,10.);
#21749=VECTOR('',#72941,10.);
#21750=VECTOR('',#72944,10.);
#21751=VECTOR('',#72945,10.);
#21752=VECTOR('',#72946,10.);
#21753=VECTOR('',#72949,10.);
#21754=VECTOR('',#72950,10.);
#21755=VECTOR('',#72951,10.);
#21756=VECTOR('',#72954,10.);
#21757=VECTOR('',#72955,10.);
#21758=VECTOR('',#72956,10.);
#21759=VECTOR('',#72959,10.);
#21760=VECTOR('',#72960,10.);
#21761=VECTOR('',#72961,10.);
#21762=VECTOR('',#72964,10.);
#21763=VECTOR('',#72965,10.);
#21764=VECTOR('',#72966,10.);
#21765=VECTOR('',#72969,10.);
#21766=VECTOR('',#72970,10.);
#21767=VECTOR('',#72971,10.);
#21768=VECTOR('',#72974,10.);
#21769=VECTOR('',#72975,10.);
#21770=VECTOR('',#72976,10.);
#21771=VECTOR('',#72979,10.);
#21772=VECTOR('',#72980,10.);
#21773=VECTOR('',#72981,10.);
#21774=VECTOR('',#72984,10.);
#21775=VECTOR('',#72985,10.);
#21776=VECTOR('',#72986,10.);
#21777=VECTOR('',#72989,10.);
#21778=VECTOR('',#72990,10.);
#21779=VECTOR('',#72991,10.);
#21780=VECTOR('',#72994,10.);
#21781=VECTOR('',#72995,10.);
#21782=VECTOR('',#72996,10.);
#21783=VECTOR('',#72999,10.);
#21784=VECTOR('',#73000,10.);
#21785=VECTOR('',#73001,10.);
#21786=VECTOR('',#73004,10.);
#21787=VECTOR('',#73005,10.);
#21788=VECTOR('',#73006,10.);
#21789=VECTOR('',#73009,10.);
#21790=VECTOR('',#73010,10.);
#21791=VECTOR('',#73011,10.);
#21792=VECTOR('',#73014,10.);
#21793=VECTOR('',#73015,10.);
#21794=VECTOR('',#73016,10.);
#21795=VECTOR('',#73019,10.);
#21796=VECTOR('',#73020,10.);
#21797=VECTOR('',#73021,10.);
#21798=VECTOR('',#73024,10.);
#21799=VECTOR('',#73025,10.);
#21800=VECTOR('',#73026,10.);
#21801=VECTOR('',#73029,10.);
#21802=VECTOR('',#73030,10.);
#21803=VECTOR('',#73031,10.);
#21804=VECTOR('',#73034,10.);
#21805=VECTOR('',#73035,10.);
#21806=VECTOR('',#73036,10.);
#21807=VECTOR('',#73039,10.);
#21808=VECTOR('',#73040,10.);
#21809=VECTOR('',#73041,10.);
#21810=VECTOR('',#73044,10.);
#21811=VECTOR('',#73045,10.);
#21812=VECTOR('',#73046,10.);
#21813=VECTOR('',#73049,10.);
#21814=VECTOR('',#73050,10.);
#21815=VECTOR('',#73051,10.);
#21816=VECTOR('',#73054,10.);
#21817=VECTOR('',#73055,10.);
#21818=VECTOR('',#73056,10.);
#21819=VECTOR('',#73059,10.);
#21820=VECTOR('',#73060,10.);
#21821=VECTOR('',#73061,10.);
#21822=VECTOR('',#73064,10.);
#21823=VECTOR('',#73065,10.);
#21824=VECTOR('',#73066,10.);
#21825=VECTOR('',#73069,10.);
#21826=VECTOR('',#73070,10.);
#21827=VECTOR('',#73071,10.);
#21828=VECTOR('',#73074,10.);
#21829=VECTOR('',#73075,10.);
#21830=VECTOR('',#73076,10.);
#21831=VECTOR('',#73079,10.);
#21832=VECTOR('',#73080,10.);
#21833=VECTOR('',#73081,10.);
#21834=VECTOR('',#73084,10.);
#21835=VECTOR('',#73085,10.);
#21836=VECTOR('',#73086,10.);
#21837=VECTOR('',#73089,10.);
#21838=VECTOR('',#73090,10.);
#21839=VECTOR('',#73091,10.);
#21840=VECTOR('',#73094,10.);
#21841=VECTOR('',#73095,10.);
#21842=VECTOR('',#73096,10.);
#21843=VECTOR('',#73099,10.);
#21844=VECTOR('',#73100,10.);
#21845=VECTOR('',#73101,10.);
#21846=VECTOR('',#73104,10.);
#21847=VECTOR('',#73105,10.);
#21848=VECTOR('',#73106,10.);
#21849=VECTOR('',#73109,10.);
#21850=VECTOR('',#73110,10.);
#21851=VECTOR('',#73111,10.);
#21852=VECTOR('',#73114,10.);
#21853=VECTOR('',#73115,10.);
#21854=VECTOR('',#73116,10.);
#21855=VECTOR('',#73119,10.);
#21856=VECTOR('',#73120,10.);
#21857=VECTOR('',#73121,10.);
#21858=VECTOR('',#73124,10.);
#21859=VECTOR('',#73125,10.);
#21860=VECTOR('',#73126,10.);
#21861=VECTOR('',#73129,10.);
#21862=VECTOR('',#73130,10.);
#21863=VECTOR('',#73131,10.);
#21864=VECTOR('',#73134,10.);
#21865=VECTOR('',#73135,10.);
#21866=VECTOR('',#73136,10.);
#21867=VECTOR('',#73139,10.);
#21868=VECTOR('',#73140,10.);
#21869=VECTOR('',#73141,10.);
#21870=VECTOR('',#73144,10.);
#21871=VECTOR('',#73145,10.);
#21872=VECTOR('',#73146,10.);
#21873=VECTOR('',#73149,10.);
#21874=VECTOR('',#73150,10.);
#21875=VECTOR('',#73151,10.);
#21876=VECTOR('',#73154,10.);
#21877=VECTOR('',#73155,10.);
#21878=VECTOR('',#73156,10.);
#21879=VECTOR('',#73159,10.);
#21880=VECTOR('',#73160,10.);
#21881=VECTOR('',#73161,10.);
#21882=VECTOR('',#73164,10.);
#21883=VECTOR('',#73165,10.);
#21884=VECTOR('',#73166,10.);
#21885=VECTOR('',#73169,10.);
#21886=VECTOR('',#73170,10.);
#21887=VECTOR('',#73171,10.);
#21888=VECTOR('',#73174,10.);
#21889=VECTOR('',#73175,10.);
#21890=VECTOR('',#73176,10.);
#21891=VECTOR('',#73179,10.);
#21892=VECTOR('',#73180,10.);
#21893=VECTOR('',#73181,10.);
#21894=VECTOR('',#73184,10.);
#21895=VECTOR('',#73185,10.);
#21896=VECTOR('',#73186,10.);
#21897=VECTOR('',#73189,10.);
#21898=VECTOR('',#73190,10.);
#21899=VECTOR('',#73191,10.);
#21900=VECTOR('',#73194,10.);
#21901=VECTOR('',#73195,10.);
#21902=VECTOR('',#73196,10.);
#21903=VECTOR('',#73199,10.);
#21904=VECTOR('',#73200,10.);
#21905=VECTOR('',#73201,10.);
#21906=VECTOR('',#73204,10.);
#21907=VECTOR('',#73205,10.);
#21908=VECTOR('',#73206,10.);
#21909=VECTOR('',#73209,10.);
#21910=VECTOR('',#73210,10.);
#21911=VECTOR('',#73211,10.);
#21912=VECTOR('',#73214,10.);
#21913=VECTOR('',#73215,10.);
#21914=VECTOR('',#73216,10.);
#21915=VECTOR('',#73219,10.);
#21916=VECTOR('',#73220,10.);
#21917=VECTOR('',#73221,10.);
#21918=VECTOR('',#73224,10.);
#21919=VECTOR('',#73225,10.);
#21920=VECTOR('',#73226,10.);
#21921=VECTOR('',#73229,10.);
#21922=VECTOR('',#73230,10.);
#21923=VECTOR('',#73231,10.);
#21924=VECTOR('',#73234,10.);
#21925=VECTOR('',#73235,10.);
#21926=VECTOR('',#73236,10.);
#21927=VECTOR('',#73239,10.);
#21928=VECTOR('',#73240,10.);
#21929=VECTOR('',#73241,10.);
#21930=VECTOR('',#73244,10.);
#21931=VECTOR('',#73245,10.);
#21932=VECTOR('',#73246,10.);
#21933=VECTOR('',#73249,10.);
#21934=VECTOR('',#73250,10.);
#21935=VECTOR('',#73251,10.);
#21936=VECTOR('',#73254,10.);
#21937=VECTOR('',#73255,10.);
#21938=VECTOR('',#73256,10.);
#21939=VECTOR('',#73259,10.);
#21940=VECTOR('',#73260,10.);
#21941=VECTOR('',#73261,10.);
#21942=VECTOR('',#73264,10.);
#21943=VECTOR('',#73265,10.);
#21944=VECTOR('',#73266,10.);
#21945=VECTOR('',#73269,10.);
#21946=VECTOR('',#73270,10.);
#21947=VECTOR('',#73271,10.);
#21948=VECTOR('',#73274,10.);
#21949=VECTOR('',#73275,10.);
#21950=VECTOR('',#73276,10.);
#21951=VECTOR('',#73279,10.);
#21952=VECTOR('',#73280,10.);
#21953=VECTOR('',#73281,10.);
#21954=VECTOR('',#73284,10.);
#21955=VECTOR('',#73285,10.);
#21956=VECTOR('',#73286,10.);
#21957=VECTOR('',#73289,10.);
#21958=VECTOR('',#73290,10.);
#21959=VECTOR('',#73291,10.);
#21960=VECTOR('',#73294,10.);
#21961=VECTOR('',#73295,10.);
#21962=VECTOR('',#73296,10.);
#21963=VECTOR('',#73299,10.);
#21964=VECTOR('',#73300,10.);
#21965=VECTOR('',#73301,10.);
#21966=VECTOR('',#73304,10.);
#21967=VECTOR('',#73305,10.);
#21968=VECTOR('',#73306,10.);
#21969=VECTOR('',#73309,10.);
#21970=VECTOR('',#73310,10.);
#21971=VECTOR('',#73311,10.);
#21972=VECTOR('',#73314,10.);
#21973=VECTOR('',#73315,10.);
#21974=VECTOR('',#73316,10.);
#21975=VECTOR('',#73319,10.);
#21976=VECTOR('',#73320,10.);
#21977=VECTOR('',#73321,10.);
#21978=VECTOR('',#73324,10.);
#21979=VECTOR('',#73325,10.);
#21980=VECTOR('',#73326,10.);
#21981=VECTOR('',#73329,10.);
#21982=VECTOR('',#73330,10.);
#21983=VECTOR('',#73331,10.);
#21984=VECTOR('',#73334,10.);
#21985=VECTOR('',#73335,10.);
#21986=VECTOR('',#73336,10.);
#21987=VECTOR('',#73339,10.);
#21988=VECTOR('',#73340,10.);
#21989=VECTOR('',#73341,10.);
#21990=VECTOR('',#73344,10.);
#21991=VECTOR('',#73345,10.);
#21992=VECTOR('',#73346,10.);
#21993=VECTOR('',#73349,10.);
#21994=VECTOR('',#73350,10.);
#21995=VECTOR('',#73351,10.);
#21996=VECTOR('',#73354,10.);
#21997=VECTOR('',#73355,10.);
#21998=VECTOR('',#73356,10.);
#21999=VECTOR('',#73359,10.);
#22000=VECTOR('',#73360,10.);
#22001=VECTOR('',#73361,10.);
#22002=VECTOR('',#73364,10.);
#22003=VECTOR('',#73365,10.);
#22004=VECTOR('',#73366,10.);
#22005=VECTOR('',#73369,10.);
#22006=VECTOR('',#73370,10.);
#22007=VECTOR('',#73371,10.);
#22008=VECTOR('',#73374,10.);
#22009=VECTOR('',#73375,10.);
#22010=VECTOR('',#73376,10.);
#22011=VECTOR('',#73379,10.);
#22012=VECTOR('',#73380,10.);
#22013=VECTOR('',#73381,10.);
#22014=VECTOR('',#73384,10.);
#22015=VECTOR('',#73385,10.);
#22016=VECTOR('',#73386,10.);
#22017=VECTOR('',#73389,10.);
#22018=VECTOR('',#73390,10.);
#22019=VECTOR('',#73391,10.);
#22020=VECTOR('',#73394,10.);
#22021=VECTOR('',#73395,10.);
#22022=VECTOR('',#73396,10.);
#22023=VECTOR('',#73399,10.);
#22024=VECTOR('',#73400,10.);
#22025=VECTOR('',#73401,10.);
#22026=VECTOR('',#73404,10.);
#22027=VECTOR('',#73405,10.);
#22028=VECTOR('',#73406,10.);
#22029=VECTOR('',#73409,10.);
#22030=VECTOR('',#73410,10.);
#22031=VECTOR('',#73411,10.);
#22032=VECTOR('',#73414,10.);
#22033=VECTOR('',#73415,10.);
#22034=VECTOR('',#73416,10.);
#22035=VECTOR('',#73419,10.);
#22036=VECTOR('',#73420,10.);
#22037=VECTOR('',#73421,10.);
#22038=VECTOR('',#73424,10.);
#22039=VECTOR('',#73425,10.);
#22040=VECTOR('',#73426,10.);
#22041=VECTOR('',#73429,10.);
#22042=VECTOR('',#73430,10.);
#22043=VECTOR('',#73431,10.);
#22044=VECTOR('',#73434,10.);
#22045=VECTOR('',#73435,10.);
#22046=VECTOR('',#73436,10.);
#22047=VECTOR('',#73439,10.);
#22048=VECTOR('',#73440,10.);
#22049=VECTOR('',#73441,10.);
#22050=VECTOR('',#73444,10.);
#22051=VECTOR('',#73445,10.);
#22052=VECTOR('',#73446,10.);
#22053=VECTOR('',#73449,10.);
#22054=VECTOR('',#73450,10.);
#22055=VECTOR('',#73451,10.);
#22056=VECTOR('',#73454,10.);
#22057=VECTOR('',#73455,10.);
#22058=VECTOR('',#73456,10.);
#22059=VECTOR('',#73459,10.);
#22060=VECTOR('',#73460,10.);
#22061=VECTOR('',#73461,10.);
#22062=VECTOR('',#73464,10.);
#22063=VECTOR('',#73465,10.);
#22064=VECTOR('',#73466,10.);
#22065=VECTOR('',#73469,10.);
#22066=VECTOR('',#73470,10.);
#22067=VECTOR('',#73471,10.);
#22068=VECTOR('',#73474,10.);
#22069=VECTOR('',#73475,10.);
#22070=VECTOR('',#73476,10.);
#22071=VECTOR('',#73479,10.);
#22072=VECTOR('',#73480,10.);
#22073=VECTOR('',#73481,10.);
#22074=VECTOR('',#73484,10.);
#22075=VECTOR('',#73485,10.);
#22076=VECTOR('',#73486,10.);
#22077=VECTOR('',#73489,10.);
#22078=VECTOR('',#73490,10.);
#22079=VECTOR('',#73491,10.);
#22080=VECTOR('',#73494,10.);
#22081=VECTOR('',#73495,10.);
#22082=VECTOR('',#73496,10.);
#22083=VECTOR('',#73499,10.);
#22084=VECTOR('',#73500,10.);
#22085=VECTOR('',#73501,10.);
#22086=VECTOR('',#73504,10.);
#22087=VECTOR('',#73505,10.);
#22088=VECTOR('',#73506,10.);
#22089=VECTOR('',#73509,10.);
#22090=VECTOR('',#73510,10.);
#22091=VECTOR('',#73511,10.);
#22092=VECTOR('',#73514,10.);
#22093=VECTOR('',#73515,10.);
#22094=VECTOR('',#73516,10.);
#22095=VECTOR('',#73519,10.);
#22096=VECTOR('',#73520,10.);
#22097=VECTOR('',#73521,10.);
#22098=VECTOR('',#73524,10.);
#22099=VECTOR('',#73525,10.);
#22100=VECTOR('',#73526,10.);
#22101=VECTOR('',#73529,10.);
#22102=VECTOR('',#73530,10.);
#22103=VECTOR('',#73531,10.);
#22104=VECTOR('',#73534,10.);
#22105=VECTOR('',#73535,10.);
#22106=VECTOR('',#73536,10.);
#22107=VECTOR('',#73539,10.);
#22108=VECTOR('',#73540,10.);
#22109=VECTOR('',#73541,10.);
#22110=VECTOR('',#73544,10.);
#22111=VECTOR('',#73545,10.);
#22112=VECTOR('',#73546,10.);
#22113=VECTOR('',#73549,10.);
#22114=VECTOR('',#73550,10.);
#22115=VECTOR('',#73551,10.);
#22116=VECTOR('',#73554,10.);
#22117=VECTOR('',#73555,10.);
#22118=VECTOR('',#73556,10.);
#22119=VECTOR('',#73559,10.);
#22120=VECTOR('',#73560,10.);
#22121=VECTOR('',#73561,10.);
#22122=VECTOR('',#73564,10.);
#22123=VECTOR('',#73565,10.);
#22124=VECTOR('',#73566,10.);
#22125=VECTOR('',#73569,10.);
#22126=VECTOR('',#73570,10.);
#22127=VECTOR('',#73571,10.);
#22128=VECTOR('',#73574,10.);
#22129=VECTOR('',#73575,10.);
#22130=VECTOR('',#73576,10.);
#22131=VECTOR('',#73579,10.);
#22132=VECTOR('',#73580,10.);
#22133=VECTOR('',#73581,10.);
#22134=VECTOR('',#73584,10.);
#22135=VECTOR('',#73585,10.);
#22136=VECTOR('',#73586,10.);
#22137=VECTOR('',#73589,10.);
#22138=VECTOR('',#73590,10.);
#22139=VECTOR('',#73591,10.);
#22140=VECTOR('',#73594,10.);
#22141=VECTOR('',#73595,10.);
#22142=VECTOR('',#73596,10.);
#22143=VECTOR('',#73599,10.);
#22144=VECTOR('',#73600,10.);
#22145=VECTOR('',#73601,10.);
#22146=VECTOR('',#73604,10.);
#22147=VECTOR('',#73605,10.);
#22148=VECTOR('',#73606,10.);
#22149=VECTOR('',#73609,10.);
#22150=VECTOR('',#73610,10.);
#22151=VECTOR('',#73611,10.);
#22152=VECTOR('',#73614,10.);
#22153=VECTOR('',#73615,10.);
#22154=VECTOR('',#73616,10.);
#22155=VECTOR('',#73619,10.);
#22156=VECTOR('',#73620,10.);
#22157=VECTOR('',#73621,10.);
#22158=VECTOR('',#73624,10.);
#22159=VECTOR('',#73625,10.);
#22160=VECTOR('',#73626,10.);
#22161=VECTOR('',#73629,10.);
#22162=VECTOR('',#73630,10.);
#22163=VECTOR('',#73631,10.);
#22164=VECTOR('',#73634,10.);
#22165=VECTOR('',#73635,10.);
#22166=VECTOR('',#73636,10.);
#22167=VECTOR('',#73639,10.);
#22168=VECTOR('',#73640,10.);
#22169=VECTOR('',#73641,10.);
#22170=VECTOR('',#73644,10.);
#22171=VECTOR('',#73645,10.);
#22172=VECTOR('',#73646,10.);
#22173=VECTOR('',#73649,10.);
#22174=VECTOR('',#73650,10.);
#22175=VECTOR('',#73651,10.);
#22176=VECTOR('',#73654,10.);
#22177=VECTOR('',#73655,10.);
#22178=VECTOR('',#73656,10.);
#22179=VECTOR('',#73659,10.);
#22180=VECTOR('',#73660,10.);
#22181=VECTOR('',#73661,10.);
#22182=VECTOR('',#73664,10.);
#22183=VECTOR('',#73665,10.);
#22184=VECTOR('',#73666,10.);
#22185=VECTOR('',#73669,10.);
#22186=VECTOR('',#73670,10.);
#22187=VECTOR('',#73671,10.);
#22188=VECTOR('',#73674,10.);
#22189=VECTOR('',#73675,10.);
#22190=VECTOR('',#73676,10.);
#22191=VECTOR('',#73679,10.);
#22192=VECTOR('',#73680,10.);
#22193=VECTOR('',#73683,10.);
#22194=VECTOR('',#73684,10.);
#28391=VERTEX_POINT('',#98947);
#28392=VERTEX_POINT('',#98949);
#28393=VERTEX_POINT('',#98953);
#28394=VERTEX_POINT('',#98957);
#28395=VERTEX_POINT('',#98958);
#28396=VERTEX_POINT('',#98960);
#28397=VERTEX_POINT('',#98962);
#28398=VERTEX_POINT('',#98966);
#28399=VERTEX_POINT('',#98968);
#28400=VERTEX_POINT('',#98972);
#28401=VERTEX_POINT('',#98976);
#28402=VERTEX_POINT('',#98977);
#28403=VERTEX_POINT('',#98979);
#28404=VERTEX_POINT('',#98981);
#28405=VERTEX_POINT('',#98985);
#28406=VERTEX_POINT('',#98988);
#28407=VERTEX_POINT('',#98991);
#28408=VERTEX_POINT('',#98995);
#28409=VERTEX_POINT('',#98999);
#28410=VERTEX_POINT('',#99000);
#28411=VERTEX_POINT('',#99002);
#28412=VERTEX_POINT('',#99004);
#28413=VERTEX_POINT('',#99008);
#28414=VERTEX_POINT('',#99010);
#28415=VERTEX_POINT('',#99015);
#28416=VERTEX_POINT('',#99019);
#28417=VERTEX_POINT('',#99023);
#28418=VERTEX_POINT('',#99025);
#28419=VERTEX_POINT('',#99029);
#28420=VERTEX_POINT('',#99031);
#28421=VERTEX_POINT('',#99035);
#28422=VERTEX_POINT('',#99037);
#28423=VERTEX_POINT('',#99041);
#28424=VERTEX_POINT('',#99043);
#28425=VERTEX_POINT('',#99047);
#28426=VERTEX_POINT('',#99049);
#28427=VERTEX_POINT('',#99053);
#28428=VERTEX_POINT('',#99055);
#28429=VERTEX_POINT('',#99059);
#28430=VERTEX_POINT('',#99061);
#28431=VERTEX_POINT('',#99065);
#28432=VERTEX_POINT('',#99067);
#28433=VERTEX_POINT('',#99071);
#28434=VERTEX_POINT('',#99073);
#28435=VERTEX_POINT('',#99077);
#28436=VERTEX_POINT('',#99079);
#28437=VERTEX_POINT('',#99083);
#28438=VERTEX_POINT('',#99085);
#28439=VERTEX_POINT('',#99089);
#28440=VERTEX_POINT('',#99091);
#28441=VERTEX_POINT('',#99095);
#28442=VERTEX_POINT('',#99097);
#28443=VERTEX_POINT('',#99101);
#28444=VERTEX_POINT('',#99103);
#28445=VERTEX_POINT('',#99107);
#28446=VERTEX_POINT('',#99109);
#28447=VERTEX_POINT('',#99113);
#28448=VERTEX_POINT('',#99115);
#28449=VERTEX_POINT('',#99119);
#28450=VERTEX_POINT('',#99121);
#28451=VERTEX_POINT('',#99125);
#28452=VERTEX_POINT('',#99127);
#28453=VERTEX_POINT('',#99131);
#28454=VERTEX_POINT('',#99133);
#28455=VERTEX_POINT('',#99137);
#28456=VERTEX_POINT('',#99139);
#28457=VERTEX_POINT('',#99143);
#28458=VERTEX_POINT('',#99145);
#28459=VERTEX_POINT('',#99149);
#28460=VERTEX_POINT('',#99151);
#28461=VERTEX_POINT('',#99155);
#28462=VERTEX_POINT('',#99157);
#28463=VERTEX_POINT('',#99161);
#28464=VERTEX_POINT('',#99163);
#28465=VERTEX_POINT('',#99167);
#28466=VERTEX_POINT('',#99169);
#28467=VERTEX_POINT('',#99173);
#28468=VERTEX_POINT('',#99175);
#28469=VERTEX_POINT('',#99179);
#28470=VERTEX_POINT('',#99181);
#28471=VERTEX_POINT('',#99185);
#28472=VERTEX_POINT('',#99187);
#28473=VERTEX_POINT('',#99191);
#28474=VERTEX_POINT('',#99193);
#28475=VERTEX_POINT('',#99197);
#28476=VERTEX_POINT('',#99199);
#28477=VERTEX_POINT('',#99203);
#28478=VERTEX_POINT('',#99205);
#28479=VERTEX_POINT('',#99209);
#28480=VERTEX_POINT('',#99211);
#28481=VERTEX_POINT('',#99215);
#28482=VERTEX_POINT('',#99217);
#28483=VERTEX_POINT('',#99221);
#28484=VERTEX_POINT('',#99223);
#28485=VERTEX_POINT('',#99227);
#28486=VERTEX_POINT('',#99229);
#28487=VERTEX_POINT('',#99233);
#28488=VERTEX_POINT('',#99235);
#28489=VERTEX_POINT('',#99239);
#28490=VERTEX_POINT('',#99241);
#28491=VERTEX_POINT('',#99245);
#28492=VERTEX_POINT('',#99247);
#28493=VERTEX_POINT('',#99251);
#28494=VERTEX_POINT('',#99253);
#28495=VERTEX_POINT('',#99257);
#28496=VERTEX_POINT('',#99259);
#28497=VERTEX_POINT('',#99263);
#28498=VERTEX_POINT('',#99265);
#28499=VERTEX_POINT('',#99269);
#28500=VERTEX_POINT('',#99271);
#28501=VERTEX_POINT('',#99275);
#28502=VERTEX_POINT('',#99277);
#28503=VERTEX_POINT('',#99281);
#28504=VERTEX_POINT('',#99283);
#28505=VERTEX_POINT('',#99287);
#28506=VERTEX_POINT('',#99289);
#28507=VERTEX_POINT('',#99293);
#28508=VERTEX_POINT('',#99295);
#28509=VERTEX_POINT('',#99299);
#28510=VERTEX_POINT('',#99301);
#28511=VERTEX_POINT('',#99305);
#28512=VERTEX_POINT('',#99307);
#28513=VERTEX_POINT('',#99311);
#28514=VERTEX_POINT('',#99313);
#28515=VERTEX_POINT('',#99317);
#28516=VERTEX_POINT('',#99319);
#28517=VERTEX_POINT('',#99323);
#28518=VERTEX_POINT('',#99325);
#28519=VERTEX_POINT('',#99329);
#28520=VERTEX_POINT('',#99331);
#28521=VERTEX_POINT('',#99335);
#28522=VERTEX_POINT('',#99337);
#28523=VERTEX_POINT('',#99341);
#28524=VERTEX_POINT('',#99343);
#28525=VERTEX_POINT('',#99347);
#28526=VERTEX_POINT('',#99349);
#28527=VERTEX_POINT('',#99353);
#28528=VERTEX_POINT('',#99355);
#28529=VERTEX_POINT('',#99359);
#28530=VERTEX_POINT('',#99361);
#28531=VERTEX_POINT('',#99365);
#28532=VERTEX_POINT('',#99367);
#28533=VERTEX_POINT('',#99371);
#28534=VERTEX_POINT('',#99373);
#28535=VERTEX_POINT('',#99377);
#28536=VERTEX_POINT('',#99379);
#28537=VERTEX_POINT('',#99383);
#28538=VERTEX_POINT('',#99385);
#28539=VERTEX_POINT('',#99389);
#28540=VERTEX_POINT('',#99391);
#28541=VERTEX_POINT('',#99395);
#28542=VERTEX_POINT('',#99397);
#28543=VERTEX_POINT('',#99401);
#28544=VERTEX_POINT('',#99403);
#28545=VERTEX_POINT('',#99407);
#28546=VERTEX_POINT('',#99409);
#28547=VERTEX_POINT('',#99413);
#28548=VERTEX_POINT('',#99415);
#28549=VERTEX_POINT('',#99419);
#28550=VERTEX_POINT('',#99421);
#28551=VERTEX_POINT('',#99425);
#28552=VERTEX_POINT('',#99427);
#28553=VERTEX_POINT('',#99431);
#28554=VERTEX_POINT('',#99433);
#28555=VERTEX_POINT('',#99437);
#28556=VERTEX_POINT('',#99439);
#28557=VERTEX_POINT('',#99443);
#28558=VERTEX_POINT('',#99445);
#28559=VERTEX_POINT('',#99449);
#28560=VERTEX_POINT('',#99451);
#28561=VERTEX_POINT('',#99455);
#28562=VERTEX_POINT('',#99457);
#28563=VERTEX_POINT('',#99461);
#28564=VERTEX_POINT('',#99463);
#28565=VERTEX_POINT('',#99467);
#28566=VERTEX_POINT('',#99469);
#28567=VERTEX_POINT('',#99473);
#28568=VERTEX_POINT('',#99475);
#28569=VERTEX_POINT('',#99479);
#28570=VERTEX_POINT('',#99481);
#28571=VERTEX_POINT('',#99485);
#28572=VERTEX_POINT('',#99487);
#28573=VERTEX_POINT('',#99491);
#28574=VERTEX_POINT('',#99493);
#28575=VERTEX_POINT('',#99497);
#28576=VERTEX_POINT('',#99499);
#28577=VERTEX_POINT('',#99503);
#28578=VERTEX_POINT('',#99505);
#28579=VERTEX_POINT('',#99509);
#28580=VERTEX_POINT('',#99511);
#28581=VERTEX_POINT('',#99515);
#28582=VERTEX_POINT('',#99517);
#28583=VERTEX_POINT('',#99521);
#28584=VERTEX_POINT('',#99523);
#28585=VERTEX_POINT('',#99527);
#28586=VERTEX_POINT('',#99529);
#28587=VERTEX_POINT('',#99533);
#28588=VERTEX_POINT('',#99535);
#28589=VERTEX_POINT('',#99539);
#28590=VERTEX_POINT('',#99541);
#28591=VERTEX_POINT('',#99545);
#28592=VERTEX_POINT('',#99547);
#28593=VERTEX_POINT('',#99551);
#28594=VERTEX_POINT('',#99553);
#28595=VERTEX_POINT('',#99557);
#28596=VERTEX_POINT('',#99559);
#28597=VERTEX_POINT('',#99563);
#28598=VERTEX_POINT('',#99565);
#28599=VERTEX_POINT('',#99569);
#28600=VERTEX_POINT('',#99571);
#28601=VERTEX_POINT('',#99575);
#28602=VERTEX_POINT('',#99577);
#28603=VERTEX_POINT('',#99581);
#28604=VERTEX_POINT('',#99583);
#28605=VERTEX_POINT('',#99587);
#28606=VERTEX_POINT('',#99589);
#28607=VERTEX_POINT('',#99593);
#28608=VERTEX_POINT('',#99595);
#28609=VERTEX_POINT('',#99599);
#28610=VERTEX_POINT('',#99601);
#28611=VERTEX_POINT('',#99605);
#28612=VERTEX_POINT('',#99607);
#28613=VERTEX_POINT('',#99611);
#28614=VERTEX_POINT('',#99613);
#28615=VERTEX_POINT('',#99617);
#28616=VERTEX_POINT('',#99619);
#28617=VERTEX_POINT('',#99623);
#28618=VERTEX_POINT('',#99625);
#28619=VERTEX_POINT('',#99629);
#28620=VERTEX_POINT('',#99631);
#28621=VERTEX_POINT('',#99635);
#28622=VERTEX_POINT('',#99637);
#28623=VERTEX_POINT('',#99641);
#28624=VERTEX_POINT('',#99643);
#28625=VERTEX_POINT('',#99647);
#28626=VERTEX_POINT('',#99649);
#28627=VERTEX_POINT('',#99653);
#28628=VERTEX_POINT('',#99655);
#28629=VERTEX_POINT('',#99659);
#28630=VERTEX_POINT('',#99661);
#28631=VERTEX_POINT('',#99665);
#28632=VERTEX_POINT('',#99667);
#28633=VERTEX_POINT('',#99671);
#28634=VERTEX_POINT('',#99673);
#28635=VERTEX_POINT('',#99677);
#28636=VERTEX_POINT('',#99679);
#28637=VERTEX_POINT('',#99683);
#28638=VERTEX_POINT('',#99685);
#28639=VERTEX_POINT('',#99689);
#28640=VERTEX_POINT('',#99691);
#28641=VERTEX_POINT('',#99695);
#28642=VERTEX_POINT('',#99697);
#28643=VERTEX_POINT('',#99701);
#28644=VERTEX_POINT('',#99703);
#28645=VERTEX_POINT('',#99707);
#28646=VERTEX_POINT('',#99709);
#28647=VERTEX_POINT('',#99713);
#28648=VERTEX_POINT('',#99715);
#28649=VERTEX_POINT('',#99719);
#28650=VERTEX_POINT('',#99721);
#28651=VERTEX_POINT('',#99725);
#28652=VERTEX_POINT('',#99727);
#28653=VERTEX_POINT('',#99731);
#28654=VERTEX_POINT('',#99733);
#28655=VERTEX_POINT('',#99737);
#28656=VERTEX_POINT('',#99739);
#28657=VERTEX_POINT('',#99743);
#28658=VERTEX_POINT('',#99745);
#28659=VERTEX_POINT('',#99749);
#28660=VERTEX_POINT('',#99751);
#28661=VERTEX_POINT('',#99755);
#28662=VERTEX_POINT('',#99757);
#28663=VERTEX_POINT('',#99761);
#28664=VERTEX_POINT('',#99763);
#28665=VERTEX_POINT('',#99767);
#28666=VERTEX_POINT('',#99769);
#28667=VERTEX_POINT('',#99773);
#28668=VERTEX_POINT('',#99775);
#28669=VERTEX_POINT('',#99779);
#28670=VERTEX_POINT('',#99781);
#28671=VERTEX_POINT('',#99785);
#28672=VERTEX_POINT('',#99787);
#28673=VERTEX_POINT('',#99791);
#28674=VERTEX_POINT('',#99793);
#28675=VERTEX_POINT('',#99797);
#28676=VERTEX_POINT('',#99799);
#28677=VERTEX_POINT('',#99803);
#28678=VERTEX_POINT('',#99805);
#28679=VERTEX_POINT('',#99809);
#28680=VERTEX_POINT('',#99811);
#28681=VERTEX_POINT('',#99815);
#28682=VERTEX_POINT('',#99817);
#28683=VERTEX_POINT('',#99821);
#28684=VERTEX_POINT('',#99823);
#28685=VERTEX_POINT('',#99827);
#28686=VERTEX_POINT('',#99829);
#28687=VERTEX_POINT('',#99833);
#28688=VERTEX_POINT('',#99835);
#28689=VERTEX_POINT('',#99839);
#28690=VERTEX_POINT('',#99841);
#28691=VERTEX_POINT('',#99845);
#28692=VERTEX_POINT('',#99847);
#28693=VERTEX_POINT('',#99851);
#28694=VERTEX_POINT('',#99853);
#28695=VERTEX_POINT('',#99857);
#28696=VERTEX_POINT('',#99859);
#28697=VERTEX_POINT('',#99863);
#28698=VERTEX_POINT('',#99865);
#28699=VERTEX_POINT('',#99869);
#28700=VERTEX_POINT('',#99871);
#28701=VERTEX_POINT('',#99875);
#28702=VERTEX_POINT('',#99877);
#28703=VERTEX_POINT('',#99881);
#28704=VERTEX_POINT('',#99883);
#28705=VERTEX_POINT('',#99887);
#28706=VERTEX_POINT('',#99889);
#28707=VERTEX_POINT('',#99893);
#28708=VERTEX_POINT('',#99895);
#28709=VERTEX_POINT('',#99899);
#28710=VERTEX_POINT('',#99901);
#28711=VERTEX_POINT('',#99905);
#28712=VERTEX_POINT('',#99907);
#28713=VERTEX_POINT('',#99911);
#28714=VERTEX_POINT('',#99913);
#28715=VERTEX_POINT('',#99917);
#28716=VERTEX_POINT('',#99919);
#28717=VERTEX_POINT('',#99923);
#28718=VERTEX_POINT('',#99925);
#28719=VERTEX_POINT('',#99929);
#28720=VERTEX_POINT('',#99931);
#28721=VERTEX_POINT('',#99935);
#28722=VERTEX_POINT('',#99937);
#28723=VERTEX_POINT('',#99941);
#28724=VERTEX_POINT('',#99943);
#28725=VERTEX_POINT('',#99947);
#28726=VERTEX_POINT('',#99949);
#28727=VERTEX_POINT('',#99953);
#28728=VERTEX_POINT('',#99955);
#28729=VERTEX_POINT('',#99959);
#28730=VERTEX_POINT('',#99961);
#28731=VERTEX_POINT('',#99965);
#28732=VERTEX_POINT('',#99967);
#28733=VERTEX_POINT('',#99971);
#28734=VERTEX_POINT('',#99973);
#28735=VERTEX_POINT('',#99977);
#28736=VERTEX_POINT('',#99979);
#28737=VERTEX_POINT('',#99983);
#28738=VERTEX_POINT('',#99985);
#28739=VERTEX_POINT('',#99989);
#28740=VERTEX_POINT('',#99991);
#28741=VERTEX_POINT('',#99995);
#28742=VERTEX_POINT('',#99997);
#28743=VERTEX_POINT('',#100001);
#28744=VERTEX_POINT('',#100003);
#28745=VERTEX_POINT('',#100007);
#28746=VERTEX_POINT('',#100009);
#28747=VERTEX_POINT('',#100013);
#28748=VERTEX_POINT('',#100015);
#28749=VERTEX_POINT('',#100019);
#28750=VERTEX_POINT('',#100021);
#28751=VERTEX_POINT('',#100025);
#28752=VERTEX_POINT('',#100027);
#28753=VERTEX_POINT('',#100031);
#28754=VERTEX_POINT('',#100033);
#28755=VERTEX_POINT('',#100037);
#28756=VERTEX_POINT('',#100039);
#28757=VERTEX_POINT('',#100043);
#28758=VERTEX_POINT('',#100045);
#28759=VERTEX_POINT('',#100049);
#28760=VERTEX_POINT('',#100051);
#28761=VERTEX_POINT('',#100055);
#28762=VERTEX_POINT('',#100057);
#28763=VERTEX_POINT('',#100061);
#28764=VERTEX_POINT('',#100063);
#28765=VERTEX_POINT('',#100067);
#28766=VERTEX_POINT('',#100069);
#28767=VERTEX_POINT('',#100073);
#28768=VERTEX_POINT('',#100075);
#28769=VERTEX_POINT('',#100079);
#28770=VERTEX_POINT('',#100081);
#28771=VERTEX_POINT('',#100085);
#28772=VERTEX_POINT('',#100087);
#28773=VERTEX_POINT('',#100091);
#28774=VERTEX_POINT('',#100093);
#28775=VERTEX_POINT('',#100097);
#28776=VERTEX_POINT('',#100099);
#28777=VERTEX_POINT('',#100103);
#28778=VERTEX_POINT('',#100105);
#28779=VERTEX_POINT('',#100109);
#28780=VERTEX_POINT('',#100111);
#28781=VERTEX_POINT('',#100115);
#28782=VERTEX_POINT('',#100117);
#28783=VERTEX_POINT('',#100121);
#28784=VERTEX_POINT('',#100123);
#28785=VERTEX_POINT('',#100127);
#28786=VERTEX_POINT('',#100129);
#28787=VERTEX_POINT('',#100133);
#28788=VERTEX_POINT('',#100135);
#28789=VERTEX_POINT('',#100139);
#28790=VERTEX_POINT('',#100141);
#28791=VERTEX_POINT('',#100145);
#28792=VERTEX_POINT('',#100147);
#28793=VERTEX_POINT('',#100151);
#28794=VERTEX_POINT('',#100153);
#28795=VERTEX_POINT('',#100157);
#28796=VERTEX_POINT('',#100159);
#28797=VERTEX_POINT('',#100163);
#28798=VERTEX_POINT('',#100165);
#28799=VERTEX_POINT('',#100169);
#28800=VERTEX_POINT('',#100171);
#28801=VERTEX_POINT('',#100175);
#28802=VERTEX_POINT('',#100177);
#28803=VERTEX_POINT('',#100181);
#28804=VERTEX_POINT('',#100183);
#28805=VERTEX_POINT('',#100187);
#28806=VERTEX_POINT('',#100189);
#28807=VERTEX_POINT('',#100193);
#28808=VERTEX_POINT('',#100195);
#28809=VERTEX_POINT('',#100199);
#28810=VERTEX_POINT('',#100201);
#28811=VERTEX_POINT('',#100205);
#28812=VERTEX_POINT('',#100207);
#28813=VERTEX_POINT('',#100211);
#28814=VERTEX_POINT('',#100213);
#28815=VERTEX_POINT('',#100217);
#28816=VERTEX_POINT('',#100219);
#28817=VERTEX_POINT('',#100223);
#28818=VERTEX_POINT('',#100225);
#28819=VERTEX_POINT('',#100229);
#28820=VERTEX_POINT('',#100231);
#28821=VERTEX_POINT('',#100235);
#28822=VERTEX_POINT('',#100237);
#28823=VERTEX_POINT('',#100241);
#28824=VERTEX_POINT('',#100243);
#28825=VERTEX_POINT('',#100247);
#28826=VERTEX_POINT('',#100249);
#28827=VERTEX_POINT('',#100253);
#28828=VERTEX_POINT('',#100255);
#28829=VERTEX_POINT('',#100259);
#28830=VERTEX_POINT('',#100261);
#28831=VERTEX_POINT('',#100265);
#28832=VERTEX_POINT('',#100267);
#28833=VERTEX_POINT('',#100271);
#28834=VERTEX_POINT('',#100273);
#28835=VERTEX_POINT('',#100277);
#28836=VERTEX_POINT('',#100279);
#28837=VERTEX_POINT('',#100283);
#28838=VERTEX_POINT('',#100285);
#28839=VERTEX_POINT('',#100289);
#28840=VERTEX_POINT('',#100291);
#28841=VERTEX_POINT('',#100295);
#28842=VERTEX_POINT('',#100297);
#28843=VERTEX_POINT('',#100301);
#28844=VERTEX_POINT('',#100303);
#28845=VERTEX_POINT('',#100307);
#28846=VERTEX_POINT('',#100309);
#28847=VERTEX_POINT('',#100313);
#28848=VERTEX_POINT('',#100315);
#28849=VERTEX_POINT('',#100319);
#28850=VERTEX_POINT('',#100321);
#28851=VERTEX_POINT('',#100325);
#28852=VERTEX_POINT('',#100327);
#28853=VERTEX_POINT('',#100331);
#28854=VERTEX_POINT('',#100333);
#28855=VERTEX_POINT('',#100337);
#28856=VERTEX_POINT('',#100339);
#28857=VERTEX_POINT('',#100343);
#28858=VERTEX_POINT('',#100345);
#28859=VERTEX_POINT('',#100349);
#28860=VERTEX_POINT('',#100351);
#28861=VERTEX_POINT('',#100355);
#28862=VERTEX_POINT('',#100357);
#28863=VERTEX_POINT('',#100361);
#28864=VERTEX_POINT('',#100363);
#28865=VERTEX_POINT('',#100367);
#28866=VERTEX_POINT('',#100369);
#28867=VERTEX_POINT('',#100373);
#28868=VERTEX_POINT('',#100375);
#28869=VERTEX_POINT('',#100379);
#28870=VERTEX_POINT('',#100381);
#28871=VERTEX_POINT('',#100385);
#28872=VERTEX_POINT('',#100387);
#28873=VERTEX_POINT('',#100391);
#28874=VERTEX_POINT('',#100393);
#28875=VERTEX_POINT('',#100397);
#28876=VERTEX_POINT('',#100399);
#28877=VERTEX_POINT('',#100403);
#28878=VERTEX_POINT('',#100405);
#28879=VERTEX_POINT('',#100409);
#28880=VERTEX_POINT('',#100411);
#28881=VERTEX_POINT('',#100415);
#28882=VERTEX_POINT('',#100417);
#28883=VERTEX_POINT('',#100421);
#28884=VERTEX_POINT('',#100423);
#28885=VERTEX_POINT('',#100427);
#28886=VERTEX_POINT('',#100429);
#28887=VERTEX_POINT('',#100433);
#28888=VERTEX_POINT('',#100435);
#28889=VERTEX_POINT('',#100439);
#28890=VERTEX_POINT('',#100441);
#28891=VERTEX_POINT('',#100445);
#28892=VERTEX_POINT('',#100447);
#28893=VERTEX_POINT('',#100451);
#28894=VERTEX_POINT('',#100453);
#28895=VERTEX_POINT('',#100457);
#28896=VERTEX_POINT('',#100459);
#28897=VERTEX_POINT('',#100463);
#28898=VERTEX_POINT('',#100465);
#28899=VERTEX_POINT('',#100469);
#28900=VERTEX_POINT('',#100471);
#28901=VERTEX_POINT('',#100475);
#28902=VERTEX_POINT('',#100477);
#28903=VERTEX_POINT('',#100481);
#28904=VERTEX_POINT('',#100483);
#28905=VERTEX_POINT('',#100487);
#28906=VERTEX_POINT('',#100489);
#28907=VERTEX_POINT('',#100493);
#28908=VERTEX_POINT('',#100495);
#28909=VERTEX_POINT('',#100499);
#28910=VERTEX_POINT('',#100501);
#28911=VERTEX_POINT('',#100505);
#28912=VERTEX_POINT('',#100507);
#28913=VERTEX_POINT('',#100511);
#28914=VERTEX_POINT('',#100513);
#28915=VERTEX_POINT('',#100517);
#28916=VERTEX_POINT('',#100519);
#28917=VERTEX_POINT('',#100523);
#28918=VERTEX_POINT('',#100525);
#28919=VERTEX_POINT('',#100529);
#28920=VERTEX_POINT('',#100531);
#28921=VERTEX_POINT('',#100535);
#28922=VERTEX_POINT('',#100537);
#28923=VERTEX_POINT('',#100541);
#28924=VERTEX_POINT('',#100543);
#28925=VERTEX_POINT('',#100547);
#28926=VERTEX_POINT('',#100549);
#28927=VERTEX_POINT('',#100553);
#28928=VERTEX_POINT('',#100555);
#28929=VERTEX_POINT('',#100559);
#28930=VERTEX_POINT('',#100561);
#28931=VERTEX_POINT('',#100565);
#28932=VERTEX_POINT('',#100567);
#28933=VERTEX_POINT('',#100571);
#28934=VERTEX_POINT('',#100573);
#28935=VERTEX_POINT('',#100577);
#28936=VERTEX_POINT('',#100579);
#28937=VERTEX_POINT('',#100583);
#28938=VERTEX_POINT('',#100585);
#28939=VERTEX_POINT('',#100589);
#28940=VERTEX_POINT('',#100591);
#28941=VERTEX_POINT('',#100595);
#28942=VERTEX_POINT('',#100597);
#28943=VERTEX_POINT('',#100601);
#28944=VERTEX_POINT('',#100603);
#28945=VERTEX_POINT('',#100607);
#28946=VERTEX_POINT('',#100609);
#28947=VERTEX_POINT('',#100613);
#28948=VERTEX_POINT('',#100615);
#28949=VERTEX_POINT('',#100619);
#28950=VERTEX_POINT('',#100621);
#28951=VERTEX_POINT('',#100625);
#28952=VERTEX_POINT('',#100627);
#28953=VERTEX_POINT('',#100631);
#28954=VERTEX_POINT('',#100633);
#28955=VERTEX_POINT('',#100637);
#28956=VERTEX_POINT('',#100639);
#28957=VERTEX_POINT('',#100643);
#28958=VERTEX_POINT('',#100645);
#28959=VERTEX_POINT('',#100649);
#28960=VERTEX_POINT('',#100651);
#28961=VERTEX_POINT('',#100655);
#28962=VERTEX_POINT('',#100657);
#28963=VERTEX_POINT('',#100661);
#28964=VERTEX_POINT('',#100663);
#28965=VERTEX_POINT('',#100667);
#28966=VERTEX_POINT('',#100669);
#28967=VERTEX_POINT('',#100673);
#28968=VERTEX_POINT('',#100675);
#28969=VERTEX_POINT('',#100679);
#28970=VERTEX_POINT('',#100681);
#28971=VERTEX_POINT('',#100685);
#28972=VERTEX_POINT('',#100687);
#28973=VERTEX_POINT('',#100691);
#28974=VERTEX_POINT('',#100693);
#28975=VERTEX_POINT('',#100697);
#28976=VERTEX_POINT('',#100699);
#28977=VERTEX_POINT('',#100703);
#28978=VERTEX_POINT('',#100705);
#28979=VERTEX_POINT('',#100709);
#28980=VERTEX_POINT('',#100711);
#28981=VERTEX_POINT('',#100715);
#28982=VERTEX_POINT('',#100717);
#28983=VERTEX_POINT('',#100721);
#28984=VERTEX_POINT('',#100723);
#28985=VERTEX_POINT('',#100727);
#28986=VERTEX_POINT('',#100729);
#28987=VERTEX_POINT('',#100733);
#28988=VERTEX_POINT('',#100735);
#28989=VERTEX_POINT('',#100739);
#28990=VERTEX_POINT('',#100741);
#28991=VERTEX_POINT('',#100745);
#28992=VERTEX_POINT('',#100747);
#28993=VERTEX_POINT('',#100751);
#28994=VERTEX_POINT('',#100753);
#28995=VERTEX_POINT('',#100757);
#28996=VERTEX_POINT('',#100759);
#28997=VERTEX_POINT('',#100763);
#28998=VERTEX_POINT('',#100765);
#28999=VERTEX_POINT('',#100769);
#29000=VERTEX_POINT('',#100771);
#29001=VERTEX_POINT('',#100775);
#29002=VERTEX_POINT('',#100777);
#29003=VERTEX_POINT('',#100781);
#29004=VERTEX_POINT('',#100783);
#29005=VERTEX_POINT('',#100787);
#29006=VERTEX_POINT('',#100789);
#29007=VERTEX_POINT('',#100793);
#29008=VERTEX_POINT('',#100795);
#29009=VERTEX_POINT('',#100799);
#29010=VERTEX_POINT('',#100801);
#29011=VERTEX_POINT('',#100805);
#29012=VERTEX_POINT('',#100807);
#29013=VERTEX_POINT('',#100811);
#29014=VERTEX_POINT('',#100813);
#29015=VERTEX_POINT('',#100817);
#29016=VERTEX_POINT('',#100819);
#29017=VERTEX_POINT('',#100823);
#29018=VERTEX_POINT('',#100825);
#29019=VERTEX_POINT('',#100829);
#29020=VERTEX_POINT('',#100831);
#29021=VERTEX_POINT('',#100835);
#29022=VERTEX_POINT('',#100837);
#29023=VERTEX_POINT('',#100841);
#29024=VERTEX_POINT('',#100843);
#29025=VERTEX_POINT('',#100847);
#29026=VERTEX_POINT('',#100849);
#29027=VERTEX_POINT('',#100853);
#29028=VERTEX_POINT('',#100855);
#29029=VERTEX_POINT('',#100859);
#29030=VERTEX_POINT('',#100861);
#29031=VERTEX_POINT('',#100865);
#29032=VERTEX_POINT('',#100867);
#29033=VERTEX_POINT('',#100871);
#29034=VERTEX_POINT('',#100873);
#29035=VERTEX_POINT('',#100877);
#29036=VERTEX_POINT('',#100879);
#29037=VERTEX_POINT('',#100883);
#29038=VERTEX_POINT('',#100885);
#29039=VERTEX_POINT('',#100889);
#29040=VERTEX_POINT('',#100891);
#29041=VERTEX_POINT('',#100895);
#29042=VERTEX_POINT('',#100897);
#29043=VERTEX_POINT('',#100901);
#29044=VERTEX_POINT('',#100903);
#29045=VERTEX_POINT('',#100907);
#29046=VERTEX_POINT('',#100909);
#29047=VERTEX_POINT('',#100913);
#29048=VERTEX_POINT('',#100915);
#29049=VERTEX_POINT('',#100919);
#29050=VERTEX_POINT('',#100921);
#29051=VERTEX_POINT('',#100925);
#29052=VERTEX_POINT('',#100927);
#29053=VERTEX_POINT('',#100931);
#29054=VERTEX_POINT('',#100933);
#29055=VERTEX_POINT('',#100937);
#29056=VERTEX_POINT('',#100939);
#29057=VERTEX_POINT('',#100943);
#29058=VERTEX_POINT('',#100945);
#29059=VERTEX_POINT('',#100949);
#29060=VERTEX_POINT('',#100951);
#29061=VERTEX_POINT('',#100955);
#29062=VERTEX_POINT('',#100957);
#29063=VERTEX_POINT('',#100961);
#29064=VERTEX_POINT('',#100963);
#29065=VERTEX_POINT('',#100967);
#29066=VERTEX_POINT('',#100969);
#29067=VERTEX_POINT('',#100973);
#29068=VERTEX_POINT('',#100975);
#29069=VERTEX_POINT('',#100979);
#29070=VERTEX_POINT('',#100981);
#29071=VERTEX_POINT('',#100985);
#29072=VERTEX_POINT('',#100987);
#29073=VERTEX_POINT('',#100991);
#29074=VERTEX_POINT('',#100993);
#29075=VERTEX_POINT('',#100997);
#29076=VERTEX_POINT('',#100999);
#29077=VERTEX_POINT('',#101003);
#29078=VERTEX_POINT('',#101005);
#29079=VERTEX_POINT('',#101009);
#29080=VERTEX_POINT('',#101011);
#29081=VERTEX_POINT('',#101015);
#29082=VERTEX_POINT('',#101017);
#29083=VERTEX_POINT('',#101021);
#29084=VERTEX_POINT('',#101023);
#29085=VERTEX_POINT('',#101027);
#29086=VERTEX_POINT('',#101029);
#29087=VERTEX_POINT('',#101033);
#29088=VERTEX_POINT('',#101035);
#29089=VERTEX_POINT('',#101039);
#29090=VERTEX_POINT('',#101041);
#29091=VERTEX_POINT('',#101045);
#29092=VERTEX_POINT('',#101047);
#29093=VERTEX_POINT('',#101051);
#29094=VERTEX_POINT('',#101053);
#29095=VERTEX_POINT('',#101057);
#29096=VERTEX_POINT('',#101059);
#29097=VERTEX_POINT('',#101063);
#29098=VERTEX_POINT('',#101065);
#29099=VERTEX_POINT('',#101069);
#29100=VERTEX_POINT('',#101071);
#29101=VERTEX_POINT('',#101075);
#29102=VERTEX_POINT('',#101077);
#29103=VERTEX_POINT('',#101081);
#29104=VERTEX_POINT('',#101083);
#29105=VERTEX_POINT('',#101087);
#29106=VERTEX_POINT('',#101089);
#29107=VERTEX_POINT('',#101093);
#29108=VERTEX_POINT('',#101095);
#29109=VERTEX_POINT('',#101099);
#29110=VERTEX_POINT('',#101101);
#29111=VERTEX_POINT('',#101105);
#29112=VERTEX_POINT('',#101107);
#29113=VERTEX_POINT('',#101111);
#29114=VERTEX_POINT('',#101113);
#29115=VERTEX_POINT('',#101117);
#29116=VERTEX_POINT('',#101119);
#29117=VERTEX_POINT('',#101123);
#29118=VERTEX_POINT('',#101125);
#29119=VERTEX_POINT('',#101129);
#29120=VERTEX_POINT('',#101131);
#29121=VERTEX_POINT('',#101135);
#29122=VERTEX_POINT('',#101137);
#29123=VERTEX_POINT('',#101141);
#29124=VERTEX_POINT('',#101143);
#29125=VERTEX_POINT('',#101147);
#29126=VERTEX_POINT('',#101149);
#29127=VERTEX_POINT('',#101153);
#29128=VERTEX_POINT('',#101155);
#29129=VERTEX_POINT('',#101159);
#29130=VERTEX_POINT('',#101161);
#29131=VERTEX_POINT('',#101165);
#29132=VERTEX_POINT('',#101167);
#29133=VERTEX_POINT('',#101171);
#29134=VERTEX_POINT('',#101173);
#29135=VERTEX_POINT('',#101177);
#29136=VERTEX_POINT('',#101179);
#29137=VERTEX_POINT('',#101183);
#29138=VERTEX_POINT('',#101185);
#29139=VERTEX_POINT('',#101189);
#29140=VERTEX_POINT('',#101191);
#29141=VERTEX_POINT('',#101195);
#29142=VERTEX_POINT('',#101197);
#29143=VERTEX_POINT('',#101201);
#29144=VERTEX_POINT('',#101203);
#29145=VERTEX_POINT('',#101207);
#29146=VERTEX_POINT('',#101209);
#29147=VERTEX_POINT('',#101213);
#29148=VERTEX_POINT('',#101215);
#29149=VERTEX_POINT('',#101219);
#29150=VERTEX_POINT('',#101221);
#29151=VERTEX_POINT('',#101225);
#29152=VERTEX_POINT('',#101227);
#29153=VERTEX_POINT('',#101231);
#29154=VERTEX_POINT('',#101233);
#29155=VERTEX_POINT('',#101237);
#29156=VERTEX_POINT('',#101239);
#29157=VERTEX_POINT('',#101243);
#29158=VERTEX_POINT('',#101245);
#29159=VERTEX_POINT('',#101249);
#29160=VERTEX_POINT('',#101251);
#29161=VERTEX_POINT('',#101255);
#29162=VERTEX_POINT('',#101257);
#29163=VERTEX_POINT('',#101261);
#29164=VERTEX_POINT('',#101263);
#29165=VERTEX_POINT('',#101267);
#29166=VERTEX_POINT('',#101269);
#29167=VERTEX_POINT('',#101273);
#29168=VERTEX_POINT('',#101275);
#29169=VERTEX_POINT('',#101279);
#29170=VERTEX_POINT('',#101281);
#29171=VERTEX_POINT('',#101285);
#29172=VERTEX_POINT('',#101287);
#29173=VERTEX_POINT('',#101291);
#29174=VERTEX_POINT('',#101293);
#29175=VERTEX_POINT('',#101297);
#29176=VERTEX_POINT('',#101299);
#29177=VERTEX_POINT('',#101303);
#29178=VERTEX_POINT('',#101305);
#29179=VERTEX_POINT('',#101309);
#29180=VERTEX_POINT('',#101311);
#29181=VERTEX_POINT('',#101315);
#29182=VERTEX_POINT('',#101317);
#29183=VERTEX_POINT('',#101321);
#29184=VERTEX_POINT('',#101323);
#29185=VERTEX_POINT('',#101327);
#29186=VERTEX_POINT('',#101329);
#29187=VERTEX_POINT('',#101333);
#29188=VERTEX_POINT('',#101335);
#29189=VERTEX_POINT('',#101339);
#29190=VERTEX_POINT('',#101341);
#29191=VERTEX_POINT('',#101345);
#29192=VERTEX_POINT('',#101347);
#29193=VERTEX_POINT('',#101351);
#29194=VERTEX_POINT('',#101353);
#29195=VERTEX_POINT('',#101357);
#29196=VERTEX_POINT('',#101359);
#29197=VERTEX_POINT('',#101363);
#29198=VERTEX_POINT('',#101365);
#29199=VERTEX_POINT('',#101369);
#29200=VERTEX_POINT('',#101371);
#29201=VERTEX_POINT('',#101375);
#29202=VERTEX_POINT('',#101377);
#29203=VERTEX_POINT('',#101381);
#29204=VERTEX_POINT('',#101383);
#29205=VERTEX_POINT('',#101387);
#29206=VERTEX_POINT('',#101389);
#29207=VERTEX_POINT('',#101393);
#29208=VERTEX_POINT('',#101395);
#29209=VERTEX_POINT('',#101399);
#29210=VERTEX_POINT('',#101401);
#29211=VERTEX_POINT('',#101405);
#29212=VERTEX_POINT('',#101407);
#29213=VERTEX_POINT('',#101411);
#29214=VERTEX_POINT('',#101413);
#29215=VERTEX_POINT('',#101417);
#29216=VERTEX_POINT('',#101419);
#29217=VERTEX_POINT('',#101423);
#29218=VERTEX_POINT('',#101425);
#29219=VERTEX_POINT('',#101429);
#29220=VERTEX_POINT('',#101431);
#29221=VERTEX_POINT('',#101435);
#29222=VERTEX_POINT('',#101437);
#29223=VERTEX_POINT('',#101441);
#29224=VERTEX_POINT('',#101443);
#29225=VERTEX_POINT('',#101447);
#29226=VERTEX_POINT('',#101449);
#29227=VERTEX_POINT('',#101453);
#29228=VERTEX_POINT('',#101455);
#29229=VERTEX_POINT('',#101459);
#29230=VERTEX_POINT('',#101461);
#29231=VERTEX_POINT('',#101465);
#29232=VERTEX_POINT('',#101467);
#29233=VERTEX_POINT('',#101471);
#29234=VERTEX_POINT('',#101473);
#29235=VERTEX_POINT('',#101477);
#29236=VERTEX_POINT('',#101479);
#29237=VERTEX_POINT('',#101483);
#29238=VERTEX_POINT('',#101485);
#29239=VERTEX_POINT('',#101489);
#29240=VERTEX_POINT('',#101491);
#29241=VERTEX_POINT('',#101495);
#29242=VERTEX_POINT('',#101497);
#29243=VERTEX_POINT('',#101501);
#29244=VERTEX_POINT('',#101503);
#29245=VERTEX_POINT('',#101507);
#29246=VERTEX_POINT('',#101509);
#29247=VERTEX_POINT('',#101513);
#29248=VERTEX_POINT('',#101515);
#29249=VERTEX_POINT('',#101519);
#29250=VERTEX_POINT('',#101521);
#29251=VERTEX_POINT('',#101525);
#29252=VERTEX_POINT('',#101527);
#29253=VERTEX_POINT('',#101531);
#29254=VERTEX_POINT('',#101533);
#29255=VERTEX_POINT('',#101537);
#29256=VERTEX_POINT('',#101539);
#29257=VERTEX_POINT('',#101543);
#29258=VERTEX_POINT('',#101545);
#29259=VERTEX_POINT('',#101549);
#29260=VERTEX_POINT('',#101551);
#29261=VERTEX_POINT('',#101555);
#29262=VERTEX_POINT('',#101557);
#29263=VERTEX_POINT('',#101561);
#29264=VERTEX_POINT('',#101563);
#29265=VERTEX_POINT('',#101567);
#29266=VERTEX_POINT('',#101569);
#29267=VERTEX_POINT('',#101573);
#29268=VERTEX_POINT('',#101575);
#29269=VERTEX_POINT('',#101579);
#29270=VERTEX_POINT('',#101581);
#29271=VERTEX_POINT('',#101585);
#29272=VERTEX_POINT('',#101587);
#29273=VERTEX_POINT('',#101591);
#29274=VERTEX_POINT('',#101593);
#29275=VERTEX_POINT('',#101597);
#29276=VERTEX_POINT('',#101599);
#29277=VERTEX_POINT('',#101603);
#29278=VERTEX_POINT('',#101605);
#29279=VERTEX_POINT('',#101609);
#29280=VERTEX_POINT('',#101611);
#29281=VERTEX_POINT('',#101615);
#29282=VERTEX_POINT('',#101617);
#29283=VERTEX_POINT('',#101621);
#29284=VERTEX_POINT('',#101623);
#29285=VERTEX_POINT('',#101627);
#29286=VERTEX_POINT('',#101629);
#29287=VERTEX_POINT('',#101633);
#29288=VERTEX_POINT('',#101635);
#29289=VERTEX_POINT('',#101639);
#29290=VERTEX_POINT('',#101641);
#29291=VERTEX_POINT('',#101645);
#29292=VERTEX_POINT('',#101647);
#29293=VERTEX_POINT('',#101651);
#29294=VERTEX_POINT('',#101653);
#29295=VERTEX_POINT('',#101657);
#29296=VERTEX_POINT('',#101659);
#29297=VERTEX_POINT('',#101663);
#29298=VERTEX_POINT('',#101665);
#29299=VERTEX_POINT('',#101669);
#29300=VERTEX_POINT('',#101671);
#29301=VERTEX_POINT('',#101675);
#29302=VERTEX_POINT('',#101677);
#29303=VERTEX_POINT('',#101681);
#29304=VERTEX_POINT('',#101683);
#29305=VERTEX_POINT('',#101687);
#29306=VERTEX_POINT('',#101689);
#29307=VERTEX_POINT('',#101693);
#29308=VERTEX_POINT('',#101695);
#29309=VERTEX_POINT('',#101699);
#29310=VERTEX_POINT('',#101701);
#29311=VERTEX_POINT('',#101705);
#29312=VERTEX_POINT('',#101707);
#29313=VERTEX_POINT('',#101711);
#29314=VERTEX_POINT('',#101713);
#29315=VERTEX_POINT('',#101717);
#29316=VERTEX_POINT('',#101719);
#29317=VERTEX_POINT('',#101723);
#29318=VERTEX_POINT('',#101725);
#29319=VERTEX_POINT('',#101729);
#29320=VERTEX_POINT('',#101731);
#29321=VERTEX_POINT('',#101735);
#29322=VERTEX_POINT('',#101737);
#29323=VERTEX_POINT('',#101741);
#29324=VERTEX_POINT('',#101743);
#29325=VERTEX_POINT('',#101747);
#29326=VERTEX_POINT('',#101749);
#29327=VERTEX_POINT('',#101753);
#29328=VERTEX_POINT('',#101755);
#29329=VERTEX_POINT('',#101759);
#29330=VERTEX_POINT('',#101761);
#29331=VERTEX_POINT('',#101765);
#29332=VERTEX_POINT('',#101767);
#29333=VERTEX_POINT('',#101771);
#29334=VERTEX_POINT('',#101773);
#29335=VERTEX_POINT('',#101777);
#29336=VERTEX_POINT('',#101779);
#29337=VERTEX_POINT('',#101783);
#29338=VERTEX_POINT('',#101785);
#29339=VERTEX_POINT('',#101789);
#29340=VERTEX_POINT('',#101791);
#29341=VERTEX_POINT('',#101795);
#29342=VERTEX_POINT('',#101797);
#29343=VERTEX_POINT('',#101801);
#29344=VERTEX_POINT('',#101803);
#29345=VERTEX_POINT('',#101807);
#29346=VERTEX_POINT('',#101809);
#29347=VERTEX_POINT('',#101813);
#29348=VERTEX_POINT('',#101815);
#29349=VERTEX_POINT('',#101819);
#29350=VERTEX_POINT('',#101821);
#29351=VERTEX_POINT('',#101825);
#29352=VERTEX_POINT('',#101827);
#29353=VERTEX_POINT('',#101831);
#29354=VERTEX_POINT('',#101833);
#29355=VERTEX_POINT('',#101837);
#29356=VERTEX_POINT('',#101839);
#29357=VERTEX_POINT('',#101843);
#29358=VERTEX_POINT('',#101845);
#29359=VERTEX_POINT('',#101849);
#29360=VERTEX_POINT('',#101851);
#29361=VERTEX_POINT('',#101855);
#29362=VERTEX_POINT('',#101857);
#29363=VERTEX_POINT('',#101861);
#29364=VERTEX_POINT('',#101863);
#29365=VERTEX_POINT('',#101867);
#29366=VERTEX_POINT('',#101869);
#29367=VERTEX_POINT('',#101873);
#29368=VERTEX_POINT('',#101875);
#29369=VERTEX_POINT('',#101879);
#29370=VERTEX_POINT('',#101881);
#29371=VERTEX_POINT('',#101885);
#29372=VERTEX_POINT('',#101887);
#29373=VERTEX_POINT('',#101891);
#29374=VERTEX_POINT('',#101893);
#29375=VERTEX_POINT('',#101897);
#29376=VERTEX_POINT('',#101899);
#29377=VERTEX_POINT('',#101903);
#29378=VERTEX_POINT('',#101905);
#29379=VERTEX_POINT('',#101909);
#29380=VERTEX_POINT('',#101911);
#29381=VERTEX_POINT('',#101915);
#29382=VERTEX_POINT('',#101917);
#29383=VERTEX_POINT('',#101921);
#29384=VERTEX_POINT('',#101923);
#29385=VERTEX_POINT('',#101927);
#29386=VERTEX_POINT('',#101929);
#29387=VERTEX_POINT('',#101933);
#29388=VERTEX_POINT('',#101935);
#29389=VERTEX_POINT('',#101939);
#29390=VERTEX_POINT('',#101941);
#29391=VERTEX_POINT('',#101945);
#29392=VERTEX_POINT('',#101947);
#29393=VERTEX_POINT('',#101951);
#29394=VERTEX_POINT('',#101953);
#29395=VERTEX_POINT('',#101957);
#29396=VERTEX_POINT('',#101959);
#29397=VERTEX_POINT('',#101963);
#29398=VERTEX_POINT('',#101965);
#29399=VERTEX_POINT('',#101969);
#29400=VERTEX_POINT('',#101971);
#29401=VERTEX_POINT('',#101975);
#29402=VERTEX_POINT('',#101977);
#29403=VERTEX_POINT('',#101981);
#29404=VERTEX_POINT('',#101983);
#29405=VERTEX_POINT('',#101987);
#29406=VERTEX_POINT('',#101989);
#29407=VERTEX_POINT('',#101993);
#29408=VERTEX_POINT('',#101995);
#29409=VERTEX_POINT('',#101999);
#29410=VERTEX_POINT('',#102001);
#29411=VERTEX_POINT('',#102005);
#29412=VERTEX_POINT('',#102007);
#36049=EDGE_CURVE('',#28391,#28391,#1244,.T.);
#36050=EDGE_CURVE('',#28391,#28392,#14637,.T.);
#36051=EDGE_CURVE('',#28392,#28392,#1245,.T.);
#36052=EDGE_CURVE('',#28392,#28393,#14638,.T.);
#36053=EDGE_CURVE('',#28393,#28393,#1246,.T.);
#36054=EDGE_CURVE('',#28394,#28395,#14639,.T.);
#36055=EDGE_CURVE('',#28395,#28396,#14640,.T.);
#36056=EDGE_CURVE('',#28397,#28396,#14641,.T.);
#36057=EDGE_CURVE('',#28394,#28397,#14642,.T.);
#36058=EDGE_CURVE('',#28398,#28398,#1247,.T.);
#36059=EDGE_CURVE('',#28398,#28399,#14643,.T.);
#36060=EDGE_CURVE('',#28399,#28399,#1248,.T.);
#36061=EDGE_CURVE('',#28399,#28400,#14644,.T.);
#36062=EDGE_CURVE('',#28400,#28400,#1249,.T.);
#36063=EDGE_CURVE('',#28401,#28402,#14645,.T.);
#36064=EDGE_CURVE('',#28402,#28403,#14646,.T.);
#36065=EDGE_CURVE('',#28404,#28403,#14647,.T.);
#36066=EDGE_CURVE('',#28401,#28404,#14648,.T.);
#36067=EDGE_CURVE('',#28405,#28405,#1250,.T.);
#36068=EDGE_CURVE('',#28406,#28406,#1251,.T.);
#36069=EDGE_CURVE('',#28405,#28407,#14649,.T.);
#36070=EDGE_CURVE('',#28407,#28407,#1252,.T.);
#36071=EDGE_CURVE('',#28406,#28408,#14650,.T.);
#36072=EDGE_CURVE('',#28408,#28408,#1253,.T.);
#36073=EDGE_CURVE('',#28409,#28410,#14651,.T.);
#36074=EDGE_CURVE('',#28410,#28411,#14652,.T.);
#36075=EDGE_CURVE('',#28411,#28412,#14653,.T.);
#36076=EDGE_CURVE('',#28412,#28409,#14654,.T.);
#36077=EDGE_CURVE('',#28413,#28409,#14655,.T.);
#36078=EDGE_CURVE('',#28414,#28413,#14656,.T.);
#36079=EDGE_CURVE('',#28414,#28394,#14657,.T.);
#36080=EDGE_CURVE('',#28410,#28397,#14658,.T.);
#36081=EDGE_CURVE('',#28415,#28412,#14659,.T.);
#36082=EDGE_CURVE('',#28413,#28415,#14660,.T.);
#36083=EDGE_CURVE('',#28415,#28416,#14661,.T.);
#36084=EDGE_CURVE('',#28416,#28414,#14662,.T.);
#36085=EDGE_CURVE('',#28417,#28401,#14663,.T.);
#36086=EDGE_CURVE('',#28418,#28404,#14664,.T.);
#36087=EDGE_CURVE('',#28417,#28418,#14665,.T.);
#36088=EDGE_CURVE('',#28419,#28417,#14666,.T.);
#36089=EDGE_CURVE('',#28420,#28418,#14667,.T.);
#36090=EDGE_CURVE('',#28419,#28420,#14668,.T.);
#36091=EDGE_CURVE('',#28421,#28419,#14669,.T.);
#36092=EDGE_CURVE('',#28422,#28420,#14670,.T.);
#36093=EDGE_CURVE('',#28421,#28422,#14671,.T.);
#36094=EDGE_CURVE('',#28423,#28421,#14672,.T.);
#36095=EDGE_CURVE('',#28424,#28422,#14673,.T.);
#36096=EDGE_CURVE('',#28423,#28424,#14674,.T.);
#36097=EDGE_CURVE('',#28425,#28423,#14675,.T.);
#36098=EDGE_CURVE('',#28426,#28424,#14676,.T.);
#36099=EDGE_CURVE('',#28425,#28426,#14677,.T.);
#36100=EDGE_CURVE('',#28427,#28425,#14678,.T.);
#36101=EDGE_CURVE('',#28428,#28426,#14679,.T.);
#36102=EDGE_CURVE('',#28427,#28428,#14680,.T.);
#36103=EDGE_CURVE('',#28429,#28427,#14681,.T.);
#36104=EDGE_CURVE('',#28430,#28428,#14682,.T.);
#36105=EDGE_CURVE('',#28429,#28430,#14683,.T.);
#36106=EDGE_CURVE('',#28431,#28429,#14684,.T.);
#36107=EDGE_CURVE('',#28432,#28430,#14685,.T.);
#36108=EDGE_CURVE('',#28431,#28432,#14686,.T.);
#36109=EDGE_CURVE('',#28433,#28431,#14687,.T.);
#36110=EDGE_CURVE('',#28434,#28432,#14688,.T.);
#36111=EDGE_CURVE('',#28433,#28434,#14689,.T.);
#36112=EDGE_CURVE('',#28435,#28433,#14690,.T.);
#36113=EDGE_CURVE('',#28436,#28434,#14691,.T.);
#36114=EDGE_CURVE('',#28435,#28436,#14692,.T.);
#36115=EDGE_CURVE('',#28437,#28435,#14693,.T.);
#36116=EDGE_CURVE('',#28438,#28436,#14694,.T.);
#36117=EDGE_CURVE('',#28437,#28438,#14695,.T.);
#36118=EDGE_CURVE('',#28439,#28437,#14696,.T.);
#36119=EDGE_CURVE('',#28440,#28438,#14697,.T.);
#36120=EDGE_CURVE('',#28439,#28440,#14698,.T.);
#36121=EDGE_CURVE('',#28441,#28439,#14699,.T.);
#36122=EDGE_CURVE('',#28442,#28440,#14700,.T.);
#36123=EDGE_CURVE('',#28441,#28442,#14701,.T.);
#36124=EDGE_CURVE('',#28443,#28441,#14702,.T.);
#36125=EDGE_CURVE('',#28444,#28442,#14703,.T.);
#36126=EDGE_CURVE('',#28443,#28444,#14704,.T.);
#36127=EDGE_CURVE('',#28445,#28443,#14705,.T.);
#36128=EDGE_CURVE('',#28446,#28444,#14706,.T.);
#36129=EDGE_CURVE('',#28445,#28446,#14707,.T.);
#36130=EDGE_CURVE('',#28447,#28445,#14708,.T.);
#36131=EDGE_CURVE('',#28448,#28446,#14709,.T.);
#36132=EDGE_CURVE('',#28447,#28448,#14710,.T.);
#36133=EDGE_CURVE('',#28449,#28447,#14711,.T.);
#36134=EDGE_CURVE('',#28450,#28448,#14712,.T.);
#36135=EDGE_CURVE('',#28449,#28450,#14713,.T.);
#36136=EDGE_CURVE('',#28451,#28449,#14714,.T.);
#36137=EDGE_CURVE('',#28452,#28450,#14715,.T.);
#36138=EDGE_CURVE('',#28451,#28452,#14716,.T.);
#36139=EDGE_CURVE('',#28453,#28451,#14717,.T.);
#36140=EDGE_CURVE('',#28454,#28452,#14718,.T.);
#36141=EDGE_CURVE('',#28453,#28454,#14719,.T.);
#36142=EDGE_CURVE('',#28455,#28453,#14720,.T.);
#36143=EDGE_CURVE('',#28456,#28454,#14721,.T.);
#36144=EDGE_CURVE('',#28455,#28456,#14722,.T.);
#36145=EDGE_CURVE('',#28457,#28455,#14723,.T.);
#36146=EDGE_CURVE('',#28458,#28456,#14724,.T.);
#36147=EDGE_CURVE('',#28457,#28458,#14725,.T.);
#36148=EDGE_CURVE('',#28459,#28457,#14726,.T.);
#36149=EDGE_CURVE('',#28460,#28458,#14727,.T.);
#36150=EDGE_CURVE('',#28459,#28460,#14728,.T.);
#36151=EDGE_CURVE('',#28461,#28459,#14729,.T.);
#36152=EDGE_CURVE('',#28462,#28460,#14730,.T.);
#36153=EDGE_CURVE('',#28461,#28462,#14731,.T.);
#36154=EDGE_CURVE('',#28463,#28461,#14732,.T.);
#36155=EDGE_CURVE('',#28464,#28462,#14733,.T.);
#36156=EDGE_CURVE('',#28463,#28464,#14734,.T.);
#36157=EDGE_CURVE('',#28465,#28463,#14735,.T.);
#36158=EDGE_CURVE('',#28466,#28464,#14736,.T.);
#36159=EDGE_CURVE('',#28465,#28466,#14737,.T.);
#36160=EDGE_CURVE('',#28467,#28465,#14738,.T.);
#36161=EDGE_CURVE('',#28468,#28466,#14739,.T.);
#36162=EDGE_CURVE('',#28467,#28468,#14740,.T.);
#36163=EDGE_CURVE('',#28469,#28467,#14741,.T.);
#36164=EDGE_CURVE('',#28470,#28468,#14742,.T.);
#36165=EDGE_CURVE('',#28469,#28470,#14743,.T.);
#36166=EDGE_CURVE('',#28471,#28469,#14744,.T.);
#36167=EDGE_CURVE('',#28472,#28470,#14745,.T.);
#36168=EDGE_CURVE('',#28471,#28472,#14746,.T.);
#36169=EDGE_CURVE('',#28473,#28471,#14747,.T.);
#36170=EDGE_CURVE('',#28474,#28472,#14748,.T.);
#36171=EDGE_CURVE('',#28473,#28474,#14749,.T.);
#36172=EDGE_CURVE('',#28475,#28473,#14750,.T.);
#36173=EDGE_CURVE('',#28476,#28474,#14751,.T.);
#36174=EDGE_CURVE('',#28475,#28476,#14752,.T.);
#36175=EDGE_CURVE('',#28477,#28475,#14753,.T.);
#36176=EDGE_CURVE('',#28478,#28476,#14754,.T.);
#36177=EDGE_CURVE('',#28477,#28478,#14755,.T.);
#36178=EDGE_CURVE('',#28479,#28477,#14756,.T.);
#36179=EDGE_CURVE('',#28480,#28478,#14757,.T.);
#36180=EDGE_CURVE('',#28479,#28480,#14758,.T.);
#36181=EDGE_CURVE('',#28481,#28479,#14759,.T.);
#36182=EDGE_CURVE('',#28482,#28480,#14760,.T.);
#36183=EDGE_CURVE('',#28481,#28482,#14761,.T.);
#36184=EDGE_CURVE('',#28483,#28481,#14762,.T.);
#36185=EDGE_CURVE('',#28484,#28482,#14763,.T.);
#36186=EDGE_CURVE('',#28483,#28484,#14764,.T.);
#36187=EDGE_CURVE('',#28485,#28483,#14765,.T.);
#36188=EDGE_CURVE('',#28486,#28484,#14766,.T.);
#36189=EDGE_CURVE('',#28485,#28486,#14767,.T.);
#36190=EDGE_CURVE('',#28487,#28485,#14768,.T.);
#36191=EDGE_CURVE('',#28488,#28486,#14769,.T.);
#36192=EDGE_CURVE('',#28487,#28488,#14770,.T.);
#36193=EDGE_CURVE('',#28489,#28487,#14771,.T.);
#36194=EDGE_CURVE('',#28490,#28488,#14772,.T.);
#36195=EDGE_CURVE('',#28489,#28490,#14773,.T.);
#36196=EDGE_CURVE('',#28491,#28489,#14774,.T.);
#36197=EDGE_CURVE('',#28492,#28490,#14775,.T.);
#36198=EDGE_CURVE('',#28491,#28492,#14776,.T.);
#36199=EDGE_CURVE('',#28493,#28491,#14777,.T.);
#36200=EDGE_CURVE('',#28494,#28492,#14778,.T.);
#36201=EDGE_CURVE('',#28493,#28494,#14779,.T.);
#36202=EDGE_CURVE('',#28495,#28493,#14780,.T.);
#36203=EDGE_CURVE('',#28496,#28494,#14781,.T.);
#36204=EDGE_CURVE('',#28495,#28496,#14782,.T.);
#36205=EDGE_CURVE('',#28497,#28495,#14783,.T.);
#36206=EDGE_CURVE('',#28498,#28496,#14784,.T.);
#36207=EDGE_CURVE('',#28497,#28498,#14785,.T.);
#36208=EDGE_CURVE('',#28499,#28497,#14786,.T.);
#36209=EDGE_CURVE('',#28500,#28498,#14787,.T.);
#36210=EDGE_CURVE('',#28499,#28500,#14788,.T.);
#36211=EDGE_CURVE('',#28501,#28499,#14789,.T.);
#36212=EDGE_CURVE('',#28502,#28500,#14790,.T.);
#36213=EDGE_CURVE('',#28501,#28502,#14791,.T.);
#36214=EDGE_CURVE('',#28503,#28501,#14792,.T.);
#36215=EDGE_CURVE('',#28504,#28502,#14793,.T.);
#36216=EDGE_CURVE('',#28503,#28504,#14794,.T.);
#36217=EDGE_CURVE('',#28505,#28503,#14795,.T.);
#36218=EDGE_CURVE('',#28506,#28504,#14796,.T.);
#36219=EDGE_CURVE('',#28505,#28506,#14797,.T.);
#36220=EDGE_CURVE('',#28507,#28505,#14798,.T.);
#36221=EDGE_CURVE('',#28508,#28506,#14799,.T.);
#36222=EDGE_CURVE('',#28507,#28508,#14800,.T.);
#36223=EDGE_CURVE('',#28509,#28507,#14801,.T.);
#36224=EDGE_CURVE('',#28510,#28508,#14802,.T.);
#36225=EDGE_CURVE('',#28509,#28510,#14803,.T.);
#36226=EDGE_CURVE('',#28511,#28509,#14804,.T.);
#36227=EDGE_CURVE('',#28512,#28510,#14805,.T.);
#36228=EDGE_CURVE('',#28511,#28512,#14806,.T.);
#36229=EDGE_CURVE('',#28513,#28511,#14807,.T.);
#36230=EDGE_CURVE('',#28514,#28512,#14808,.T.);
#36231=EDGE_CURVE('',#28513,#28514,#14809,.T.);
#36232=EDGE_CURVE('',#28515,#28513,#14810,.T.);
#36233=EDGE_CURVE('',#28516,#28514,#14811,.T.);
#36234=EDGE_CURVE('',#28515,#28516,#14812,.T.);
#36235=EDGE_CURVE('',#28517,#28515,#14813,.T.);
#36236=EDGE_CURVE('',#28518,#28516,#14814,.T.);
#36237=EDGE_CURVE('',#28517,#28518,#14815,.T.);
#36238=EDGE_CURVE('',#28519,#28517,#14816,.T.);
#36239=EDGE_CURVE('',#28520,#28518,#14817,.T.);
#36240=EDGE_CURVE('',#28519,#28520,#14818,.T.);
#36241=EDGE_CURVE('',#28521,#28519,#14819,.T.);
#36242=EDGE_CURVE('',#28522,#28520,#14820,.T.);
#36243=EDGE_CURVE('',#28521,#28522,#14821,.T.);
#36244=EDGE_CURVE('',#28523,#28521,#14822,.T.);
#36245=EDGE_CURVE('',#28524,#28522,#14823,.T.);
#36246=EDGE_CURVE('',#28523,#28524,#14824,.T.);
#36247=EDGE_CURVE('',#28525,#28523,#14825,.T.);
#36248=EDGE_CURVE('',#28526,#28524,#14826,.T.);
#36249=EDGE_CURVE('',#28525,#28526,#14827,.T.);
#36250=EDGE_CURVE('',#28527,#28525,#14828,.T.);
#36251=EDGE_CURVE('',#28528,#28526,#14829,.T.);
#36252=EDGE_CURVE('',#28527,#28528,#14830,.T.);
#36253=EDGE_CURVE('',#28529,#28527,#14831,.T.);
#36254=EDGE_CURVE('',#28530,#28528,#14832,.T.);
#36255=EDGE_CURVE('',#28529,#28530,#14833,.T.);
#36256=EDGE_CURVE('',#28531,#28529,#14834,.T.);
#36257=EDGE_CURVE('',#28532,#28530,#14835,.T.);
#36258=EDGE_CURVE('',#28531,#28532,#14836,.T.);
#36259=EDGE_CURVE('',#28533,#28531,#14837,.T.);
#36260=EDGE_CURVE('',#28534,#28532,#14838,.T.);
#36261=EDGE_CURVE('',#28533,#28534,#14839,.T.);
#36262=EDGE_CURVE('',#28535,#28533,#14840,.T.);
#36263=EDGE_CURVE('',#28536,#28534,#14841,.T.);
#36264=EDGE_CURVE('',#28535,#28536,#14842,.T.);
#36265=EDGE_CURVE('',#28537,#28535,#14843,.T.);
#36266=EDGE_CURVE('',#28538,#28536,#14844,.T.);
#36267=EDGE_CURVE('',#28537,#28538,#14845,.T.);
#36268=EDGE_CURVE('',#28539,#28537,#14846,.T.);
#36269=EDGE_CURVE('',#28540,#28538,#14847,.T.);
#36270=EDGE_CURVE('',#28539,#28540,#14848,.T.);
#36271=EDGE_CURVE('',#28541,#28539,#14849,.T.);
#36272=EDGE_CURVE('',#28542,#28540,#14850,.T.);
#36273=EDGE_CURVE('',#28541,#28542,#14851,.T.);
#36274=EDGE_CURVE('',#28543,#28541,#14852,.T.);
#36275=EDGE_CURVE('',#28544,#28542,#14853,.T.);
#36276=EDGE_CURVE('',#28543,#28544,#14854,.T.);
#36277=EDGE_CURVE('',#28545,#28543,#14855,.T.);
#36278=EDGE_CURVE('',#28546,#28544,#14856,.T.);
#36279=EDGE_CURVE('',#28545,#28546,#14857,.T.);
#36280=EDGE_CURVE('',#28547,#28545,#14858,.T.);
#36281=EDGE_CURVE('',#28548,#28546,#14859,.T.);
#36282=EDGE_CURVE('',#28547,#28548,#14860,.T.);
#36283=EDGE_CURVE('',#28549,#28547,#14861,.T.);
#36284=EDGE_CURVE('',#28550,#28548,#14862,.T.);
#36285=EDGE_CURVE('',#28549,#28550,#14863,.T.);
#36286=EDGE_CURVE('',#28551,#28549,#14864,.T.);
#36287=EDGE_CURVE('',#28552,#28550,#14865,.T.);
#36288=EDGE_CURVE('',#28551,#28552,#14866,.T.);
#36289=EDGE_CURVE('',#28553,#28551,#14867,.T.);
#36290=EDGE_CURVE('',#28554,#28552,#14868,.T.);
#36291=EDGE_CURVE('',#28553,#28554,#14869,.T.);
#36292=EDGE_CURVE('',#28555,#28553,#14870,.T.);
#36293=EDGE_CURVE('',#28556,#28554,#14871,.T.);
#36294=EDGE_CURVE('',#28555,#28556,#14872,.T.);
#36295=EDGE_CURVE('',#28557,#28555,#14873,.T.);
#36296=EDGE_CURVE('',#28558,#28556,#14874,.T.);
#36297=EDGE_CURVE('',#28557,#28558,#14875,.T.);
#36298=EDGE_CURVE('',#28559,#28557,#14876,.T.);
#36299=EDGE_CURVE('',#28560,#28558,#14877,.T.);
#36300=EDGE_CURVE('',#28559,#28560,#14878,.T.);
#36301=EDGE_CURVE('',#28561,#28559,#14879,.T.);
#36302=EDGE_CURVE('',#28562,#28560,#14880,.T.);
#36303=EDGE_CURVE('',#28561,#28562,#14881,.T.);
#36304=EDGE_CURVE('',#28563,#28561,#14882,.T.);
#36305=EDGE_CURVE('',#28564,#28562,#14883,.T.);
#36306=EDGE_CURVE('',#28563,#28564,#14884,.T.);
#36307=EDGE_CURVE('',#28565,#28563,#14885,.T.);
#36308=EDGE_CURVE('',#28566,#28564,#14886,.T.);
#36309=EDGE_CURVE('',#28565,#28566,#14887,.T.);
#36310=EDGE_CURVE('',#28567,#28565,#14888,.T.);
#36311=EDGE_CURVE('',#28568,#28566,#14889,.T.);
#36312=EDGE_CURVE('',#28567,#28568,#14890,.T.);
#36313=EDGE_CURVE('',#28569,#28567,#14891,.T.);
#36314=EDGE_CURVE('',#28570,#28568,#14892,.T.);
#36315=EDGE_CURVE('',#28569,#28570,#14893,.T.);
#36316=EDGE_CURVE('',#28571,#28569,#14894,.T.);
#36317=EDGE_CURVE('',#28572,#28570,#14895,.T.);
#36318=EDGE_CURVE('',#28571,#28572,#14896,.T.);
#36319=EDGE_CURVE('',#28573,#28571,#14897,.T.);
#36320=EDGE_CURVE('',#28574,#28572,#14898,.T.);
#36321=EDGE_CURVE('',#28573,#28574,#14899,.T.);
#36322=EDGE_CURVE('',#28575,#28573,#14900,.T.);
#36323=EDGE_CURVE('',#28576,#28574,#14901,.T.);
#36324=EDGE_CURVE('',#28575,#28576,#14902,.T.);
#36325=EDGE_CURVE('',#28577,#28575,#14903,.T.);
#36326=EDGE_CURVE('',#28578,#28576,#14904,.T.);
#36327=EDGE_CURVE('',#28577,#28578,#14905,.T.);
#36328=EDGE_CURVE('',#28579,#28577,#14906,.T.);
#36329=EDGE_CURVE('',#28580,#28578,#14907,.T.);
#36330=EDGE_CURVE('',#28579,#28580,#14908,.T.);
#36331=EDGE_CURVE('',#28581,#28579,#14909,.T.);
#36332=EDGE_CURVE('',#28582,#28580,#14910,.T.);
#36333=EDGE_CURVE('',#28581,#28582,#14911,.T.);
#36334=EDGE_CURVE('',#28583,#28581,#14912,.T.);
#36335=EDGE_CURVE('',#28584,#28582,#14913,.T.);
#36336=EDGE_CURVE('',#28583,#28584,#14914,.T.);
#36337=EDGE_CURVE('',#28585,#28583,#14915,.T.);
#36338=EDGE_CURVE('',#28586,#28584,#14916,.T.);
#36339=EDGE_CURVE('',#28585,#28586,#14917,.T.);
#36340=EDGE_CURVE('',#28587,#28585,#14918,.T.);
#36341=EDGE_CURVE('',#28588,#28586,#14919,.T.);
#36342=EDGE_CURVE('',#28587,#28588,#14920,.T.);
#36343=EDGE_CURVE('',#28589,#28587,#14921,.T.);
#36344=EDGE_CURVE('',#28590,#28588,#14922,.T.);
#36345=EDGE_CURVE('',#28589,#28590,#14923,.T.);
#36346=EDGE_CURVE('',#28591,#28589,#14924,.T.);
#36347=EDGE_CURVE('',#28592,#28590,#14925,.T.);
#36348=EDGE_CURVE('',#28591,#28592,#14926,.T.);
#36349=EDGE_CURVE('',#28593,#28591,#14927,.T.);
#36350=EDGE_CURVE('',#28594,#28592,#14928,.T.);
#36351=EDGE_CURVE('',#28593,#28594,#14929,.T.);
#36352=EDGE_CURVE('',#28595,#28593,#14930,.T.);
#36353=EDGE_CURVE('',#28596,#28594,#14931,.T.);
#36354=EDGE_CURVE('',#28595,#28596,#14932,.T.);
#36355=EDGE_CURVE('',#28597,#28595,#14933,.T.);
#36356=EDGE_CURVE('',#28598,#28596,#14934,.T.);
#36357=EDGE_CURVE('',#28597,#28598,#14935,.T.);
#36358=EDGE_CURVE('',#28599,#28597,#14936,.T.);
#36359=EDGE_CURVE('',#28600,#28598,#14937,.T.);
#36360=EDGE_CURVE('',#28599,#28600,#14938,.T.);
#36361=EDGE_CURVE('',#28601,#28599,#14939,.T.);
#36362=EDGE_CURVE('',#28602,#28600,#14940,.T.);
#36363=EDGE_CURVE('',#28601,#28602,#14941,.T.);
#36364=EDGE_CURVE('',#28603,#28601,#14942,.T.);
#36365=EDGE_CURVE('',#28604,#28602,#14943,.T.);
#36366=EDGE_CURVE('',#28603,#28604,#14944,.T.);
#36367=EDGE_CURVE('',#28605,#28603,#14945,.T.);
#36368=EDGE_CURVE('',#28606,#28604,#14946,.T.);
#36369=EDGE_CURVE('',#28605,#28606,#14947,.T.);
#36370=EDGE_CURVE('',#28607,#28605,#14948,.T.);
#36371=EDGE_CURVE('',#28608,#28606,#14949,.T.);
#36372=EDGE_CURVE('',#28607,#28608,#14950,.T.);
#36373=EDGE_CURVE('',#28609,#28607,#14951,.T.);
#36374=EDGE_CURVE('',#28610,#28608,#14952,.T.);
#36375=EDGE_CURVE('',#28609,#28610,#14953,.T.);
#36376=EDGE_CURVE('',#28611,#28609,#14954,.T.);
#36377=EDGE_CURVE('',#28612,#28610,#14955,.T.);
#36378=EDGE_CURVE('',#28611,#28612,#14956,.T.);
#36379=EDGE_CURVE('',#28613,#28611,#14957,.T.);
#36380=EDGE_CURVE('',#28614,#28612,#14958,.T.);
#36381=EDGE_CURVE('',#28613,#28614,#14959,.T.);
#36382=EDGE_CURVE('',#28615,#28613,#14960,.T.);
#36383=EDGE_CURVE('',#28616,#28614,#14961,.T.);
#36384=EDGE_CURVE('',#28615,#28616,#14962,.T.);
#36385=EDGE_CURVE('',#28617,#28615,#14963,.T.);
#36386=EDGE_CURVE('',#28618,#28616,#14964,.T.);
#36387=EDGE_CURVE('',#28617,#28618,#14965,.T.);
#36388=EDGE_CURVE('',#28619,#28617,#14966,.T.);
#36389=EDGE_CURVE('',#28620,#28618,#14967,.T.);
#36390=EDGE_CURVE('',#28619,#28620,#14968,.T.);
#36391=EDGE_CURVE('',#28621,#28619,#14969,.T.);
#36392=EDGE_CURVE('',#28622,#28620,#14970,.T.);
#36393=EDGE_CURVE('',#28621,#28622,#14971,.T.);
#36394=EDGE_CURVE('',#28623,#28621,#14972,.T.);
#36395=EDGE_CURVE('',#28624,#28622,#14973,.T.);
#36396=EDGE_CURVE('',#28623,#28624,#14974,.T.);
#36397=EDGE_CURVE('',#28625,#28623,#14975,.T.);
#36398=EDGE_CURVE('',#28626,#28624,#14976,.T.);
#36399=EDGE_CURVE('',#28625,#28626,#14977,.T.);
#36400=EDGE_CURVE('',#28627,#28625,#14978,.T.);
#36401=EDGE_CURVE('',#28628,#28626,#14979,.T.);
#36402=EDGE_CURVE('',#28627,#28628,#14980,.T.);
#36403=EDGE_CURVE('',#28629,#28627,#14981,.T.);
#36404=EDGE_CURVE('',#28630,#28628,#14982,.T.);
#36405=EDGE_CURVE('',#28629,#28630,#14983,.T.);
#36406=EDGE_CURVE('',#28631,#28629,#14984,.T.);
#36407=EDGE_CURVE('',#28632,#28630,#14985,.T.);
#36408=EDGE_CURVE('',#28631,#28632,#14986,.T.);
#36409=EDGE_CURVE('',#28633,#28631,#14987,.T.);
#36410=EDGE_CURVE('',#28634,#28632,#14988,.T.);
#36411=EDGE_CURVE('',#28633,#28634,#14989,.T.);
#36412=EDGE_CURVE('',#28635,#28633,#14990,.T.);
#36413=EDGE_CURVE('',#28636,#28634,#14991,.T.);
#36414=EDGE_CURVE('',#28635,#28636,#14992,.T.);
#36415=EDGE_CURVE('',#28637,#28635,#14993,.T.);
#36416=EDGE_CURVE('',#28638,#28636,#14994,.T.);
#36417=EDGE_CURVE('',#28637,#28638,#14995,.T.);
#36418=EDGE_CURVE('',#28639,#28637,#14996,.T.);
#36419=EDGE_CURVE('',#28640,#28638,#14997,.T.);
#36420=EDGE_CURVE('',#28639,#28640,#14998,.T.);
#36421=EDGE_CURVE('',#28641,#28639,#14999,.T.);
#36422=EDGE_CURVE('',#28642,#28640,#15000,.T.);
#36423=EDGE_CURVE('',#28641,#28642,#15001,.T.);
#36424=EDGE_CURVE('',#28643,#28641,#15002,.T.);
#36425=EDGE_CURVE('',#28644,#28642,#15003,.T.);
#36426=EDGE_CURVE('',#28643,#28644,#15004,.T.);
#36427=EDGE_CURVE('',#28645,#28643,#15005,.T.);
#36428=EDGE_CURVE('',#28646,#28644,#15006,.T.);
#36429=EDGE_CURVE('',#28645,#28646,#15007,.T.);
#36430=EDGE_CURVE('',#28647,#28645,#15008,.T.);
#36431=EDGE_CURVE('',#28648,#28646,#15009,.T.);
#36432=EDGE_CURVE('',#28647,#28648,#15010,.T.);
#36433=EDGE_CURVE('',#28649,#28647,#15011,.T.);
#36434=EDGE_CURVE('',#28650,#28648,#15012,.T.);
#36435=EDGE_CURVE('',#28649,#28650,#15013,.T.);
#36436=EDGE_CURVE('',#28651,#28649,#15014,.T.);
#36437=EDGE_CURVE('',#28652,#28650,#15015,.T.);
#36438=EDGE_CURVE('',#28651,#28652,#15016,.T.);
#36439=EDGE_CURVE('',#28653,#28651,#15017,.T.);
#36440=EDGE_CURVE('',#28654,#28652,#15018,.T.);
#36441=EDGE_CURVE('',#28653,#28654,#15019,.T.);
#36442=EDGE_CURVE('',#28655,#28653,#15020,.T.);
#36443=EDGE_CURVE('',#28656,#28654,#15021,.T.);
#36444=EDGE_CURVE('',#28655,#28656,#15022,.T.);
#36445=EDGE_CURVE('',#28657,#28655,#15023,.T.);
#36446=EDGE_CURVE('',#28658,#28656,#15024,.T.);
#36447=EDGE_CURVE('',#28657,#28658,#15025,.T.);
#36448=EDGE_CURVE('',#28659,#28657,#15026,.T.);
#36449=EDGE_CURVE('',#28660,#28658,#15027,.T.);
#36450=EDGE_CURVE('',#28659,#28660,#15028,.T.);
#36451=EDGE_CURVE('',#28661,#28659,#15029,.T.);
#36452=EDGE_CURVE('',#28662,#28660,#15030,.T.);
#36453=EDGE_CURVE('',#28661,#28662,#15031,.T.);
#36454=EDGE_CURVE('',#28663,#28661,#15032,.T.);
#36455=EDGE_CURVE('',#28664,#28662,#15033,.T.);
#36456=EDGE_CURVE('',#28663,#28664,#15034,.T.);
#36457=EDGE_CURVE('',#28665,#28663,#15035,.T.);
#36458=EDGE_CURVE('',#28666,#28664,#15036,.T.);
#36459=EDGE_CURVE('',#28665,#28666,#15037,.T.);
#36460=EDGE_CURVE('',#28667,#28665,#15038,.T.);
#36461=EDGE_CURVE('',#28668,#28666,#15039,.T.);
#36462=EDGE_CURVE('',#28667,#28668,#15040,.T.);
#36463=EDGE_CURVE('',#28669,#28667,#15041,.T.);
#36464=EDGE_CURVE('',#28670,#28668,#15042,.T.);
#36465=EDGE_CURVE('',#28669,#28670,#15043,.T.);
#36466=EDGE_CURVE('',#28671,#28669,#15044,.T.);
#36467=EDGE_CURVE('',#28672,#28670,#15045,.T.);
#36468=EDGE_CURVE('',#28671,#28672,#15046,.T.);
#36469=EDGE_CURVE('',#28673,#28671,#15047,.T.);
#36470=EDGE_CURVE('',#28674,#28672,#15048,.T.);
#36471=EDGE_CURVE('',#28673,#28674,#15049,.T.);
#36472=EDGE_CURVE('',#28675,#28673,#15050,.T.);
#36473=EDGE_CURVE('',#28676,#28674,#15051,.T.);
#36474=EDGE_CURVE('',#28675,#28676,#15052,.T.);
#36475=EDGE_CURVE('',#28677,#28675,#15053,.T.);
#36476=EDGE_CURVE('',#28678,#28676,#15054,.T.);
#36477=EDGE_CURVE('',#28677,#28678,#15055,.T.);
#36478=EDGE_CURVE('',#28679,#28677,#15056,.T.);
#36479=EDGE_CURVE('',#28680,#28678,#15057,.T.);
#36480=EDGE_CURVE('',#28679,#28680,#15058,.T.);
#36481=EDGE_CURVE('',#28681,#28679,#15059,.T.);
#36482=EDGE_CURVE('',#28682,#28680,#15060,.T.);
#36483=EDGE_CURVE('',#28681,#28682,#15061,.T.);
#36484=EDGE_CURVE('',#28683,#28681,#15062,.T.);
#36485=EDGE_CURVE('',#28684,#28682,#15063,.T.);
#36486=EDGE_CURVE('',#28683,#28684,#15064,.T.);
#36487=EDGE_CURVE('',#28685,#28683,#15065,.T.);
#36488=EDGE_CURVE('',#28686,#28684,#15066,.T.);
#36489=EDGE_CURVE('',#28685,#28686,#15067,.T.);
#36490=EDGE_CURVE('',#28687,#28685,#15068,.T.);
#36491=EDGE_CURVE('',#28688,#28686,#15069,.T.);
#36492=EDGE_CURVE('',#28687,#28688,#15070,.T.);
#36493=EDGE_CURVE('',#28689,#28687,#15071,.T.);
#36494=EDGE_CURVE('',#28690,#28688,#15072,.T.);
#36495=EDGE_CURVE('',#28689,#28690,#15073,.T.);
#36496=EDGE_CURVE('',#28691,#28689,#15074,.T.);
#36497=EDGE_CURVE('',#28692,#28690,#15075,.T.);
#36498=EDGE_CURVE('',#28691,#28692,#15076,.T.);
#36499=EDGE_CURVE('',#28693,#28691,#15077,.T.);
#36500=EDGE_CURVE('',#28694,#28692,#15078,.T.);
#36501=EDGE_CURVE('',#28693,#28694,#15079,.T.);
#36502=EDGE_CURVE('',#28695,#28693,#15080,.T.);
#36503=EDGE_CURVE('',#28696,#28694,#15081,.T.);
#36504=EDGE_CURVE('',#28695,#28696,#15082,.T.);
#36505=EDGE_CURVE('',#28697,#28695,#15083,.T.);
#36506=EDGE_CURVE('',#28698,#28696,#15084,.T.);
#36507=EDGE_CURVE('',#28697,#28698,#15085,.T.);
#36508=EDGE_CURVE('',#28699,#28697,#15086,.T.);
#36509=EDGE_CURVE('',#28700,#28698,#15087,.T.);
#36510=EDGE_CURVE('',#28699,#28700,#15088,.T.);
#36511=EDGE_CURVE('',#28701,#28699,#15089,.T.);
#36512=EDGE_CURVE('',#28702,#28700,#15090,.T.);
#36513=EDGE_CURVE('',#28701,#28702,#15091,.T.);
#36514=EDGE_CURVE('',#28703,#28701,#15092,.T.);
#36515=EDGE_CURVE('',#28704,#28702,#15093,.T.);
#36516=EDGE_CURVE('',#28703,#28704,#15094,.T.);
#36517=EDGE_CURVE('',#28705,#28703,#15095,.T.);
#36518=EDGE_CURVE('',#28706,#28704,#15096,.T.);
#36519=EDGE_CURVE('',#28705,#28706,#15097,.T.);
#36520=EDGE_CURVE('',#28707,#28705,#15098,.T.);
#36521=EDGE_CURVE('',#28708,#28706,#15099,.T.);
#36522=EDGE_CURVE('',#28707,#28708,#15100,.T.);
#36523=EDGE_CURVE('',#28709,#28707,#15101,.T.);
#36524=EDGE_CURVE('',#28710,#28708,#15102,.T.);
#36525=EDGE_CURVE('',#28709,#28710,#15103,.T.);
#36526=EDGE_CURVE('',#28711,#28709,#15104,.T.);
#36527=EDGE_CURVE('',#28712,#28710,#15105,.T.);
#36528=EDGE_CURVE('',#28711,#28712,#15106,.T.);
#36529=EDGE_CURVE('',#28713,#28711,#15107,.T.);
#36530=EDGE_CURVE('',#28714,#28712,#15108,.T.);
#36531=EDGE_CURVE('',#28713,#28714,#15109,.T.);
#36532=EDGE_CURVE('',#28715,#28713,#15110,.T.);
#36533=EDGE_CURVE('',#28716,#28714,#15111,.T.);
#36534=EDGE_CURVE('',#28715,#28716,#15112,.T.);
#36535=EDGE_CURVE('',#28717,#28715,#15113,.T.);
#36536=EDGE_CURVE('',#28718,#28716,#15114,.T.);
#36537=EDGE_CURVE('',#28717,#28718,#15115,.T.);
#36538=EDGE_CURVE('',#28719,#28717,#15116,.T.);
#36539=EDGE_CURVE('',#28720,#28718,#15117,.T.);
#36540=EDGE_CURVE('',#28719,#28720,#15118,.T.);
#36541=EDGE_CURVE('',#28721,#28719,#15119,.T.);
#36542=EDGE_CURVE('',#28722,#28720,#15120,.T.);
#36543=EDGE_CURVE('',#28721,#28722,#15121,.T.);
#36544=EDGE_CURVE('',#28723,#28721,#15122,.T.);
#36545=EDGE_CURVE('',#28724,#28722,#15123,.T.);
#36546=EDGE_CURVE('',#28723,#28724,#15124,.T.);
#36547=EDGE_CURVE('',#28725,#28723,#15125,.T.);
#36548=EDGE_CURVE('',#28726,#28724,#15126,.T.);
#36549=EDGE_CURVE('',#28725,#28726,#15127,.T.);
#36550=EDGE_CURVE('',#28727,#28725,#15128,.T.);
#36551=EDGE_CURVE('',#28728,#28726,#15129,.T.);
#36552=EDGE_CURVE('',#28727,#28728,#15130,.T.);
#36553=EDGE_CURVE('',#28729,#28727,#15131,.T.);
#36554=EDGE_CURVE('',#28730,#28728,#15132,.T.);
#36555=EDGE_CURVE('',#28729,#28730,#15133,.T.);
#36556=EDGE_CURVE('',#28731,#28729,#15134,.T.);
#36557=EDGE_CURVE('',#28732,#28730,#15135,.T.);
#36558=EDGE_CURVE('',#28731,#28732,#15136,.T.);
#36559=EDGE_CURVE('',#28733,#28731,#15137,.T.);
#36560=EDGE_CURVE('',#28734,#28732,#15138,.T.);
#36561=EDGE_CURVE('',#28733,#28734,#15139,.T.);
#36562=EDGE_CURVE('',#28735,#28733,#15140,.T.);
#36563=EDGE_CURVE('',#28736,#28734,#15141,.T.);
#36564=EDGE_CURVE('',#28735,#28736,#15142,.T.);
#36565=EDGE_CURVE('',#28737,#28735,#15143,.T.);
#36566=EDGE_CURVE('',#28738,#28736,#15144,.T.);
#36567=EDGE_CURVE('',#28737,#28738,#15145,.T.);
#36568=EDGE_CURVE('',#28739,#28737,#15146,.T.);
#36569=EDGE_CURVE('',#28740,#28738,#15147,.T.);
#36570=EDGE_CURVE('',#28739,#28740,#15148,.T.);
#36571=EDGE_CURVE('',#28741,#28739,#15149,.T.);
#36572=EDGE_CURVE('',#28742,#28740,#15150,.T.);
#36573=EDGE_CURVE('',#28741,#28742,#15151,.T.);
#36574=EDGE_CURVE('',#28743,#28741,#15152,.T.);
#36575=EDGE_CURVE('',#28744,#28742,#15153,.T.);
#36576=EDGE_CURVE('',#28743,#28744,#15154,.T.);
#36577=EDGE_CURVE('',#28745,#28743,#15155,.T.);
#36578=EDGE_CURVE('',#28746,#28744,#15156,.T.);
#36579=EDGE_CURVE('',#28745,#28746,#15157,.T.);
#36580=EDGE_CURVE('',#28747,#28745,#15158,.T.);
#36581=EDGE_CURVE('',#28748,#28746,#15159,.T.);
#36582=EDGE_CURVE('',#28747,#28748,#15160,.T.);
#36583=EDGE_CURVE('',#28749,#28747,#15161,.T.);
#36584=EDGE_CURVE('',#28750,#28748,#15162,.T.);
#36585=EDGE_CURVE('',#28749,#28750,#15163,.T.);
#36586=EDGE_CURVE('',#28751,#28749,#15164,.T.);
#36587=EDGE_CURVE('',#28752,#28750,#15165,.T.);
#36588=EDGE_CURVE('',#28751,#28752,#15166,.T.);
#36589=EDGE_CURVE('',#28753,#28751,#15167,.T.);
#36590=EDGE_CURVE('',#28754,#28752,#15168,.T.);
#36591=EDGE_CURVE('',#28753,#28754,#15169,.T.);
#36592=EDGE_CURVE('',#28755,#28753,#15170,.T.);
#36593=EDGE_CURVE('',#28756,#28754,#15171,.T.);
#36594=EDGE_CURVE('',#28755,#28756,#15172,.T.);
#36595=EDGE_CURVE('',#28757,#28755,#15173,.T.);
#36596=EDGE_CURVE('',#28758,#28756,#15174,.T.);
#36597=EDGE_CURVE('',#28757,#28758,#15175,.T.);
#36598=EDGE_CURVE('',#28759,#28757,#15176,.T.);
#36599=EDGE_CURVE('',#28760,#28758,#15177,.T.);
#36600=EDGE_CURVE('',#28759,#28760,#15178,.T.);
#36601=EDGE_CURVE('',#28761,#28759,#15179,.T.);
#36602=EDGE_CURVE('',#28762,#28760,#15180,.T.);
#36603=EDGE_CURVE('',#28761,#28762,#15181,.T.);
#36604=EDGE_CURVE('',#28763,#28761,#15182,.T.);
#36605=EDGE_CURVE('',#28764,#28762,#15183,.T.);
#36606=EDGE_CURVE('',#28763,#28764,#15184,.T.);
#36607=EDGE_CURVE('',#28765,#28763,#15185,.T.);
#36608=EDGE_CURVE('',#28766,#28764,#15186,.T.);
#36609=EDGE_CURVE('',#28765,#28766,#15187,.T.);
#36610=EDGE_CURVE('',#28767,#28765,#15188,.T.);
#36611=EDGE_CURVE('',#28768,#28766,#15189,.T.);
#36612=EDGE_CURVE('',#28767,#28768,#15190,.T.);
#36613=EDGE_CURVE('',#28769,#28767,#15191,.T.);
#36614=EDGE_CURVE('',#28770,#28768,#15192,.T.);
#36615=EDGE_CURVE('',#28769,#28770,#15193,.T.);
#36616=EDGE_CURVE('',#28771,#28769,#15194,.T.);
#36617=EDGE_CURVE('',#28772,#28770,#15195,.T.);
#36618=EDGE_CURVE('',#28771,#28772,#15196,.T.);
#36619=EDGE_CURVE('',#28773,#28771,#15197,.T.);
#36620=EDGE_CURVE('',#28774,#28772,#15198,.T.);
#36621=EDGE_CURVE('',#28773,#28774,#15199,.T.);
#36622=EDGE_CURVE('',#28775,#28773,#15200,.T.);
#36623=EDGE_CURVE('',#28776,#28774,#15201,.T.);
#36624=EDGE_CURVE('',#28775,#28776,#15202,.T.);
#36625=EDGE_CURVE('',#28777,#28775,#15203,.T.);
#36626=EDGE_CURVE('',#28778,#28776,#15204,.T.);
#36627=EDGE_CURVE('',#28777,#28778,#15205,.T.);
#36628=EDGE_CURVE('',#28779,#28777,#15206,.T.);
#36629=EDGE_CURVE('',#28780,#28778,#15207,.T.);
#36630=EDGE_CURVE('',#28779,#28780,#15208,.T.);
#36631=EDGE_CURVE('',#28781,#28779,#15209,.T.);
#36632=EDGE_CURVE('',#28782,#28780,#15210,.T.);
#36633=EDGE_CURVE('',#28781,#28782,#15211,.T.);
#36634=EDGE_CURVE('',#28783,#28781,#15212,.T.);
#36635=EDGE_CURVE('',#28784,#28782,#15213,.T.);
#36636=EDGE_CURVE('',#28783,#28784,#15214,.T.);
#36637=EDGE_CURVE('',#28785,#28783,#15215,.T.);
#36638=EDGE_CURVE('',#28786,#28784,#15216,.T.);
#36639=EDGE_CURVE('',#28785,#28786,#15217,.T.);
#36640=EDGE_CURVE('',#28787,#28785,#15218,.T.);
#36641=EDGE_CURVE('',#28788,#28786,#15219,.T.);
#36642=EDGE_CURVE('',#28787,#28788,#15220,.T.);
#36643=EDGE_CURVE('',#28789,#28787,#15221,.T.);
#36644=EDGE_CURVE('',#28790,#28788,#15222,.T.);
#36645=EDGE_CURVE('',#28789,#28790,#15223,.T.);
#36646=EDGE_CURVE('',#28791,#28789,#15224,.T.);
#36647=EDGE_CURVE('',#28792,#28790,#15225,.T.);
#36648=EDGE_CURVE('',#28791,#28792,#15226,.T.);
#36649=EDGE_CURVE('',#28793,#28791,#15227,.T.);
#36650=EDGE_CURVE('',#28794,#28792,#15228,.T.);
#36651=EDGE_CURVE('',#28793,#28794,#15229,.T.);
#36652=EDGE_CURVE('',#28795,#28793,#15230,.T.);
#36653=EDGE_CURVE('',#28796,#28794,#15231,.T.);
#36654=EDGE_CURVE('',#28795,#28796,#15232,.T.);
#36655=EDGE_CURVE('',#28797,#28795,#15233,.T.);
#36656=EDGE_CURVE('',#28798,#28796,#15234,.T.);
#36657=EDGE_CURVE('',#28797,#28798,#15235,.T.);
#36658=EDGE_CURVE('',#28799,#28797,#15236,.T.);
#36659=EDGE_CURVE('',#28800,#28798,#15237,.T.);
#36660=EDGE_CURVE('',#28799,#28800,#15238,.T.);
#36661=EDGE_CURVE('',#28801,#28799,#15239,.T.);
#36662=EDGE_CURVE('',#28802,#28800,#15240,.T.);
#36663=EDGE_CURVE('',#28801,#28802,#15241,.T.);
#36664=EDGE_CURVE('',#28803,#28801,#15242,.T.);
#36665=EDGE_CURVE('',#28804,#28802,#15243,.T.);
#36666=EDGE_CURVE('',#28803,#28804,#15244,.T.);
#36667=EDGE_CURVE('',#28805,#28803,#15245,.T.);
#36668=EDGE_CURVE('',#28806,#28804,#15246,.T.);
#36669=EDGE_CURVE('',#28805,#28806,#15247,.T.);
#36670=EDGE_CURVE('',#28807,#28805,#15248,.T.);
#36671=EDGE_CURVE('',#28808,#28806,#15249,.T.);
#36672=EDGE_CURVE('',#28807,#28808,#15250,.T.);
#36673=EDGE_CURVE('',#28809,#28807,#15251,.T.);
#36674=EDGE_CURVE('',#28810,#28808,#15252,.T.);
#36675=EDGE_CURVE('',#28809,#28810,#15253,.T.);
#36676=EDGE_CURVE('',#28811,#28809,#15254,.T.);
#36677=EDGE_CURVE('',#28812,#28810,#15255,.T.);
#36678=EDGE_CURVE('',#28811,#28812,#15256,.T.);
#36679=EDGE_CURVE('',#28813,#28811,#15257,.T.);
#36680=EDGE_CURVE('',#28814,#28812,#15258,.T.);
#36681=EDGE_CURVE('',#28813,#28814,#15259,.T.);
#36682=EDGE_CURVE('',#28815,#28813,#15260,.T.);
#36683=EDGE_CURVE('',#28816,#28814,#15261,.T.);
#36684=EDGE_CURVE('',#28815,#28816,#15262,.T.);
#36685=EDGE_CURVE('',#28817,#28815,#15263,.T.);
#36686=EDGE_CURVE('',#28818,#28816,#15264,.T.);
#36687=EDGE_CURVE('',#28817,#28818,#15265,.T.);
#36688=EDGE_CURVE('',#28819,#28817,#15266,.T.);
#36689=EDGE_CURVE('',#28820,#28818,#15267,.T.);
#36690=EDGE_CURVE('',#28819,#28820,#15268,.T.);
#36691=EDGE_CURVE('',#28821,#28819,#15269,.T.);
#36692=EDGE_CURVE('',#28822,#28820,#15270,.T.);
#36693=EDGE_CURVE('',#28821,#28822,#15271,.T.);
#36694=EDGE_CURVE('',#28823,#28821,#15272,.T.);
#36695=EDGE_CURVE('',#28824,#28822,#15273,.T.);
#36696=EDGE_CURVE('',#28823,#28824,#15274,.T.);
#36697=EDGE_CURVE('',#28825,#28823,#15275,.T.);
#36698=EDGE_CURVE('',#28826,#28824,#15276,.T.);
#36699=EDGE_CURVE('',#28825,#28826,#15277,.T.);
#36700=EDGE_CURVE('',#28827,#28825,#15278,.T.);
#36701=EDGE_CURVE('',#28828,#28826,#15279,.T.);
#36702=EDGE_CURVE('',#28827,#28828,#15280,.T.);
#36703=EDGE_CURVE('',#28829,#28827,#15281,.T.);
#36704=EDGE_CURVE('',#28830,#28828,#15282,.T.);
#36705=EDGE_CURVE('',#28829,#28830,#15283,.T.);
#36706=EDGE_CURVE('',#28831,#28829,#15284,.T.);
#36707=EDGE_CURVE('',#28832,#28830,#15285,.T.);
#36708=EDGE_CURVE('',#28831,#28832,#15286,.T.);
#36709=EDGE_CURVE('',#28833,#28831,#15287,.T.);
#36710=EDGE_CURVE('',#28834,#28832,#15288,.T.);
#36711=EDGE_CURVE('',#28833,#28834,#15289,.T.);
#36712=EDGE_CURVE('',#28835,#28833,#15290,.T.);
#36713=EDGE_CURVE('',#28836,#28834,#15291,.T.);
#36714=EDGE_CURVE('',#28835,#28836,#15292,.T.);
#36715=EDGE_CURVE('',#28837,#28835,#15293,.T.);
#36716=EDGE_CURVE('',#28838,#28836,#15294,.T.);
#36717=EDGE_CURVE('',#28837,#28838,#15295,.T.);
#36718=EDGE_CURVE('',#28839,#28837,#15296,.T.);
#36719=EDGE_CURVE('',#28840,#28838,#15297,.T.);
#36720=EDGE_CURVE('',#28839,#28840,#15298,.T.);
#36721=EDGE_CURVE('',#28841,#28839,#15299,.T.);
#36722=EDGE_CURVE('',#28842,#28840,#15300,.T.);
#36723=EDGE_CURVE('',#28841,#28842,#15301,.T.);
#36724=EDGE_CURVE('',#28843,#28841,#15302,.T.);
#36725=EDGE_CURVE('',#28844,#28842,#15303,.T.);
#36726=EDGE_CURVE('',#28843,#28844,#15304,.T.);
#36727=EDGE_CURVE('',#28845,#28843,#15305,.T.);
#36728=EDGE_CURVE('',#28846,#28844,#15306,.T.);
#36729=EDGE_CURVE('',#28845,#28846,#15307,.T.);
#36730=EDGE_CURVE('',#28847,#28845,#15308,.T.);
#36731=EDGE_CURVE('',#28848,#28846,#15309,.T.);
#36732=EDGE_CURVE('',#28847,#28848,#15310,.T.);
#36733=EDGE_CURVE('',#28849,#28847,#15311,.T.);
#36734=EDGE_CURVE('',#28850,#28848,#15312,.T.);
#36735=EDGE_CURVE('',#28849,#28850,#15313,.T.);
#36736=EDGE_CURVE('',#28851,#28849,#15314,.T.);
#36737=EDGE_CURVE('',#28852,#28850,#15315,.T.);
#36738=EDGE_CURVE('',#28851,#28852,#15316,.T.);
#36739=EDGE_CURVE('',#28853,#28851,#15317,.T.);
#36740=EDGE_CURVE('',#28854,#28852,#15318,.T.);
#36741=EDGE_CURVE('',#28853,#28854,#15319,.T.);
#36742=EDGE_CURVE('',#28855,#28853,#15320,.T.);
#36743=EDGE_CURVE('',#28856,#28854,#15321,.T.);
#36744=EDGE_CURVE('',#28855,#28856,#15322,.T.);
#36745=EDGE_CURVE('',#28857,#28855,#15323,.T.);
#36746=EDGE_CURVE('',#28858,#28856,#15324,.T.);
#36747=EDGE_CURVE('',#28857,#28858,#15325,.T.);
#36748=EDGE_CURVE('',#28859,#28857,#15326,.T.);
#36749=EDGE_CURVE('',#28860,#28858,#15327,.T.);
#36750=EDGE_CURVE('',#28859,#28860,#15328,.T.);
#36751=EDGE_CURVE('',#28861,#28859,#15329,.T.);
#36752=EDGE_CURVE('',#28862,#28860,#15330,.T.);
#36753=EDGE_CURVE('',#28861,#28862,#15331,.T.);
#36754=EDGE_CURVE('',#28863,#28861,#15332,.T.);
#36755=EDGE_CURVE('',#28864,#28862,#15333,.T.);
#36756=EDGE_CURVE('',#28863,#28864,#15334,.T.);
#36757=EDGE_CURVE('',#28865,#28863,#15335,.T.);
#36758=EDGE_CURVE('',#28866,#28864,#15336,.T.);
#36759=EDGE_CURVE('',#28865,#28866,#15337,.T.);
#36760=EDGE_CURVE('',#28867,#28865,#15338,.T.);
#36761=EDGE_CURVE('',#28868,#28866,#15339,.T.);
#36762=EDGE_CURVE('',#28867,#28868,#15340,.T.);
#36763=EDGE_CURVE('',#28869,#28867,#15341,.T.);
#36764=EDGE_CURVE('',#28870,#28868,#15342,.T.);
#36765=EDGE_CURVE('',#28869,#28870,#15343,.T.);
#36766=EDGE_CURVE('',#28871,#28869,#15344,.T.);
#36767=EDGE_CURVE('',#28872,#28870,#15345,.T.);
#36768=EDGE_CURVE('',#28871,#28872,#15346,.T.);
#36769=EDGE_CURVE('',#28873,#28871,#15347,.T.);
#36770=EDGE_CURVE('',#28874,#28872,#15348,.T.);
#36771=EDGE_CURVE('',#28873,#28874,#15349,.T.);
#36772=EDGE_CURVE('',#28875,#28873,#15350,.T.);
#36773=EDGE_CURVE('',#28876,#28874,#15351,.T.);
#36774=EDGE_CURVE('',#28875,#28876,#15352,.T.);
#36775=EDGE_CURVE('',#28877,#28875,#15353,.T.);
#36776=EDGE_CURVE('',#28878,#28876,#15354,.T.);
#36777=EDGE_CURVE('',#28877,#28878,#15355,.T.);
#36778=EDGE_CURVE('',#28879,#28877,#15356,.T.);
#36779=EDGE_CURVE('',#28880,#28878,#15357,.T.);
#36780=EDGE_CURVE('',#28879,#28880,#15358,.T.);
#36781=EDGE_CURVE('',#28881,#28879,#15359,.T.);
#36782=EDGE_CURVE('',#28882,#28880,#15360,.T.);
#36783=EDGE_CURVE('',#28881,#28882,#15361,.T.);
#36784=EDGE_CURVE('',#28883,#28881,#15362,.T.);
#36785=EDGE_CURVE('',#28884,#28882,#15363,.T.);
#36786=EDGE_CURVE('',#28883,#28884,#15364,.T.);
#36787=EDGE_CURVE('',#28885,#28883,#15365,.T.);
#36788=EDGE_CURVE('',#28886,#28884,#15366,.T.);
#36789=EDGE_CURVE('',#28885,#28886,#15367,.T.);
#36790=EDGE_CURVE('',#28887,#28885,#15368,.T.);
#36791=EDGE_CURVE('',#28888,#28886,#15369,.T.);
#36792=EDGE_CURVE('',#28887,#28888,#15370,.T.);
#36793=EDGE_CURVE('',#28889,#28887,#15371,.T.);
#36794=EDGE_CURVE('',#28890,#28888,#15372,.T.);
#36795=EDGE_CURVE('',#28889,#28890,#15373,.T.);
#36796=EDGE_CURVE('',#28891,#28889,#15374,.T.);
#36797=EDGE_CURVE('',#28892,#28890,#15375,.T.);
#36798=EDGE_CURVE('',#28891,#28892,#15376,.T.);
#36799=EDGE_CURVE('',#28893,#28891,#15377,.T.);
#36800=EDGE_CURVE('',#28894,#28892,#15378,.T.);
#36801=EDGE_CURVE('',#28893,#28894,#15379,.T.);
#36802=EDGE_CURVE('',#28895,#28893,#15380,.T.);
#36803=EDGE_CURVE('',#28896,#28894,#15381,.T.);
#36804=EDGE_CURVE('',#28895,#28896,#15382,.T.);
#36805=EDGE_CURVE('',#28897,#28895,#15383,.T.);
#36806=EDGE_CURVE('',#28898,#28896,#15384,.T.);
#36807=EDGE_CURVE('',#28897,#28898,#15385,.T.);
#36808=EDGE_CURVE('',#28899,#28897,#15386,.T.);
#36809=EDGE_CURVE('',#28900,#28898,#15387,.T.);
#36810=EDGE_CURVE('',#28899,#28900,#15388,.T.);
#36811=EDGE_CURVE('',#28901,#28899,#15389,.T.);
#36812=EDGE_CURVE('',#28902,#28900,#15390,.T.);
#36813=EDGE_CURVE('',#28901,#28902,#15391,.T.);
#36814=EDGE_CURVE('',#28903,#28901,#15392,.T.);
#36815=EDGE_CURVE('',#28904,#28902,#15393,.T.);
#36816=EDGE_CURVE('',#28903,#28904,#15394,.T.);
#36817=EDGE_CURVE('',#28905,#28903,#15395,.T.);
#36818=EDGE_CURVE('',#28906,#28904,#15396,.T.);
#36819=EDGE_CURVE('',#28905,#28906,#15397,.T.);
#36820=EDGE_CURVE('',#28907,#28905,#15398,.T.);
#36821=EDGE_CURVE('',#28908,#28906,#15399,.T.);
#36822=EDGE_CURVE('',#28907,#28908,#15400,.T.);
#36823=EDGE_CURVE('',#28909,#28907,#15401,.T.);
#36824=EDGE_CURVE('',#28910,#28908,#15402,.T.);
#36825=EDGE_CURVE('',#28909,#28910,#15403,.T.);
#36826=EDGE_CURVE('',#28911,#28909,#15404,.T.);
#36827=EDGE_CURVE('',#28912,#28910,#15405,.T.);
#36828=EDGE_CURVE('',#28911,#28912,#15406,.T.);
#36829=EDGE_CURVE('',#28913,#28911,#15407,.T.);
#36830=EDGE_CURVE('',#28914,#28912,#15408,.T.);
#36831=EDGE_CURVE('',#28913,#28914,#15409,.T.);
#36832=EDGE_CURVE('',#28915,#28913,#15410,.T.);
#36833=EDGE_CURVE('',#28916,#28914,#15411,.T.);
#36834=EDGE_CURVE('',#28915,#28916,#15412,.T.);
#36835=EDGE_CURVE('',#28917,#28915,#15413,.T.);
#36836=EDGE_CURVE('',#28918,#28916,#15414,.T.);
#36837=EDGE_CURVE('',#28917,#28918,#15415,.T.);
#36838=EDGE_CURVE('',#28919,#28917,#15416,.T.);
#36839=EDGE_CURVE('',#28920,#28918,#15417,.T.);
#36840=EDGE_CURVE('',#28919,#28920,#15418,.T.);
#36841=EDGE_CURVE('',#28921,#28919,#15419,.T.);
#36842=EDGE_CURVE('',#28922,#28920,#15420,.T.);
#36843=EDGE_CURVE('',#28921,#28922,#15421,.T.);
#36844=EDGE_CURVE('',#28923,#28921,#15422,.T.);
#36845=EDGE_CURVE('',#28924,#28922,#15423,.T.);
#36846=EDGE_CURVE('',#28923,#28924,#15424,.T.);
#36847=EDGE_CURVE('',#28925,#28923,#15425,.T.);
#36848=EDGE_CURVE('',#28926,#28924,#15426,.T.);
#36849=EDGE_CURVE('',#28925,#28926,#15427,.T.);
#36850=EDGE_CURVE('',#28927,#28925,#15428,.T.);
#36851=EDGE_CURVE('',#28928,#28926,#15429,.T.);
#36852=EDGE_CURVE('',#28927,#28928,#15430,.T.);
#36853=EDGE_CURVE('',#28929,#28927,#15431,.T.);
#36854=EDGE_CURVE('',#28930,#28928,#15432,.T.);
#36855=EDGE_CURVE('',#28929,#28930,#15433,.T.);
#36856=EDGE_CURVE('',#28931,#28929,#15434,.T.);
#36857=EDGE_CURVE('',#28932,#28930,#15435,.T.);
#36858=EDGE_CURVE('',#28931,#28932,#15436,.T.);
#36859=EDGE_CURVE('',#28933,#28931,#15437,.T.);
#36860=EDGE_CURVE('',#28934,#28932,#15438,.T.);
#36861=EDGE_CURVE('',#28933,#28934,#15439,.T.);
#36862=EDGE_CURVE('',#28935,#28933,#15440,.T.);
#36863=EDGE_CURVE('',#28936,#28934,#15441,.T.);
#36864=EDGE_CURVE('',#28935,#28936,#15442,.T.);
#36865=EDGE_CURVE('',#28937,#28935,#15443,.T.);
#36866=EDGE_CURVE('',#28938,#28936,#15444,.T.);
#36867=EDGE_CURVE('',#28937,#28938,#15445,.T.);
#36868=EDGE_CURVE('',#28939,#28937,#15446,.T.);
#36869=EDGE_CURVE('',#28940,#28938,#15447,.T.);
#36870=EDGE_CURVE('',#28939,#28940,#15448,.T.);
#36871=EDGE_CURVE('',#28941,#28939,#15449,.T.);
#36872=EDGE_CURVE('',#28942,#28940,#15450,.T.);
#36873=EDGE_CURVE('',#28941,#28942,#15451,.T.);
#36874=EDGE_CURVE('',#28943,#28941,#15452,.T.);
#36875=EDGE_CURVE('',#28944,#28942,#15453,.T.);
#36876=EDGE_CURVE('',#28943,#28944,#15454,.T.);
#36877=EDGE_CURVE('',#28945,#28943,#15455,.T.);
#36878=EDGE_CURVE('',#28946,#28944,#15456,.T.);
#36879=EDGE_CURVE('',#28945,#28946,#15457,.T.);
#36880=EDGE_CURVE('',#28947,#28945,#15458,.T.);
#36881=EDGE_CURVE('',#28948,#28946,#15459,.T.);
#36882=EDGE_CURVE('',#28947,#28948,#15460,.T.);
#36883=EDGE_CURVE('',#28949,#28947,#15461,.T.);
#36884=EDGE_CURVE('',#28950,#28948,#15462,.T.);
#36885=EDGE_CURVE('',#28949,#28950,#15463,.T.);
#36886=EDGE_CURVE('',#28951,#28949,#15464,.T.);
#36887=EDGE_CURVE('',#28952,#28950,#15465,.T.);
#36888=EDGE_CURVE('',#28951,#28952,#15466,.T.);
#36889=EDGE_CURVE('',#28953,#28951,#15467,.T.);
#36890=EDGE_CURVE('',#28954,#28952,#15468,.T.);
#36891=EDGE_CURVE('',#28953,#28954,#15469,.T.);
#36892=EDGE_CURVE('',#28955,#28953,#15470,.T.);
#36893=EDGE_CURVE('',#28956,#28954,#15471,.T.);
#36894=EDGE_CURVE('',#28955,#28956,#15472,.T.);
#36895=EDGE_CURVE('',#28957,#28955,#15473,.T.);
#36896=EDGE_CURVE('',#28958,#28956,#15474,.T.);
#36897=EDGE_CURVE('',#28957,#28958,#15475,.T.);
#36898=EDGE_CURVE('',#28959,#28957,#15476,.T.);
#36899=EDGE_CURVE('',#28960,#28958,#15477,.T.);
#36900=EDGE_CURVE('',#28959,#28960,#15478,.T.);
#36901=EDGE_CURVE('',#28961,#28959,#15479,.T.);
#36902=EDGE_CURVE('',#28962,#28960,#15480,.T.);
#36903=EDGE_CURVE('',#28961,#28962,#15481,.T.);
#36904=EDGE_CURVE('',#28963,#28961,#15482,.T.);
#36905=EDGE_CURVE('',#28964,#28962,#15483,.T.);
#36906=EDGE_CURVE('',#28963,#28964,#15484,.T.);
#36907=EDGE_CURVE('',#28965,#28963,#15485,.T.);
#36908=EDGE_CURVE('',#28966,#28964,#15486,.T.);
#36909=EDGE_CURVE('',#28965,#28966,#15487,.T.);
#36910=EDGE_CURVE('',#28967,#28965,#15488,.T.);
#36911=EDGE_CURVE('',#28968,#28966,#15489,.T.);
#36912=EDGE_CURVE('',#28967,#28968,#15490,.T.);
#36913=EDGE_CURVE('',#28969,#28967,#15491,.T.);
#36914=EDGE_CURVE('',#28970,#28968,#15492,.T.);
#36915=EDGE_CURVE('',#28969,#28970,#15493,.T.);
#36916=EDGE_CURVE('',#28971,#28969,#15494,.T.);
#36917=EDGE_CURVE('',#28972,#28970,#15495,.T.);
#36918=EDGE_CURVE('',#28971,#28972,#15496,.T.);
#36919=EDGE_CURVE('',#28973,#28971,#15497,.T.);
#36920=EDGE_CURVE('',#28974,#28972,#15498,.T.);
#36921=EDGE_CURVE('',#28973,#28974,#15499,.T.);
#36922=EDGE_CURVE('',#28975,#28973,#15500,.T.);
#36923=EDGE_CURVE('',#28976,#28974,#15501,.T.);
#36924=EDGE_CURVE('',#28975,#28976,#15502,.T.);
#36925=EDGE_CURVE('',#28977,#28975,#15503,.T.);
#36926=EDGE_CURVE('',#28978,#28976,#15504,.T.);
#36927=EDGE_CURVE('',#28977,#28978,#15505,.T.);
#36928=EDGE_CURVE('',#28979,#28977,#15506,.T.);
#36929=EDGE_CURVE('',#28980,#28978,#15507,.T.);
#36930=EDGE_CURVE('',#28979,#28980,#15508,.T.);
#36931=EDGE_CURVE('',#28981,#28979,#15509,.T.);
#36932=EDGE_CURVE('',#28982,#28980,#15510,.T.);
#36933=EDGE_CURVE('',#28981,#28982,#15511,.T.);
#36934=EDGE_CURVE('',#28983,#28981,#15512,.T.);
#36935=EDGE_CURVE('',#28984,#28982,#15513,.T.);
#36936=EDGE_CURVE('',#28983,#28984,#15514,.T.);
#36937=EDGE_CURVE('',#28985,#28983,#15515,.T.);
#36938=EDGE_CURVE('',#28986,#28984,#15516,.T.);
#36939=EDGE_CURVE('',#28985,#28986,#15517,.T.);
#36940=EDGE_CURVE('',#28987,#28985,#15518,.T.);
#36941=EDGE_CURVE('',#28988,#28986,#15519,.T.);
#36942=EDGE_CURVE('',#28987,#28988,#15520,.T.);
#36943=EDGE_CURVE('',#28989,#28987,#15521,.T.);
#36944=EDGE_CURVE('',#28990,#28988,#15522,.T.);
#36945=EDGE_CURVE('',#28989,#28990,#15523,.T.);
#36946=EDGE_CURVE('',#28991,#28989,#15524,.T.);
#36947=EDGE_CURVE('',#28992,#28990,#15525,.T.);
#36948=EDGE_CURVE('',#28991,#28992,#15526,.T.);
#36949=EDGE_CURVE('',#28993,#28991,#15527,.T.);
#36950=EDGE_CURVE('',#28994,#28992,#15528,.T.);
#36951=EDGE_CURVE('',#28993,#28994,#15529,.T.);
#36952=EDGE_CURVE('',#28995,#28993,#15530,.T.);
#36953=EDGE_CURVE('',#28996,#28994,#15531,.T.);
#36954=EDGE_CURVE('',#28995,#28996,#15532,.T.);
#36955=EDGE_CURVE('',#28997,#28995,#15533,.T.);
#36956=EDGE_CURVE('',#28998,#28996,#15534,.T.);
#36957=EDGE_CURVE('',#28997,#28998,#15535,.T.);
#36958=EDGE_CURVE('',#28999,#28997,#15536,.T.);
#36959=EDGE_CURVE('',#29000,#28998,#15537,.T.);
#36960=EDGE_CURVE('',#28999,#29000,#15538,.T.);
#36961=EDGE_CURVE('',#29001,#28999,#15539,.T.);
#36962=EDGE_CURVE('',#29002,#29000,#15540,.T.);
#36963=EDGE_CURVE('',#29001,#29002,#15541,.T.);
#36964=EDGE_CURVE('',#29003,#29001,#15542,.T.);
#36965=EDGE_CURVE('',#29004,#29002,#15543,.T.);
#36966=EDGE_CURVE('',#29003,#29004,#15544,.T.);
#36967=EDGE_CURVE('',#29005,#29003,#15545,.T.);
#36968=EDGE_CURVE('',#29006,#29004,#15546,.T.);
#36969=EDGE_CURVE('',#29005,#29006,#15547,.T.);
#36970=EDGE_CURVE('',#29007,#29005,#15548,.T.);
#36971=EDGE_CURVE('',#29008,#29006,#15549,.T.);
#36972=EDGE_CURVE('',#29007,#29008,#15550,.T.);
#36973=EDGE_CURVE('',#29009,#29007,#15551,.T.);
#36974=EDGE_CURVE('',#29010,#29008,#15552,.T.);
#36975=EDGE_CURVE('',#29009,#29010,#15553,.T.);
#36976=EDGE_CURVE('',#29011,#29009,#15554,.T.);
#36977=EDGE_CURVE('',#29012,#29010,#15555,.T.);
#36978=EDGE_CURVE('',#29011,#29012,#15556,.T.);
#36979=EDGE_CURVE('',#29013,#29011,#15557,.T.);
#36980=EDGE_CURVE('',#29014,#29012,#15558,.T.);
#36981=EDGE_CURVE('',#29013,#29014,#15559,.T.);
#36982=EDGE_CURVE('',#29015,#29013,#15560,.T.);
#36983=EDGE_CURVE('',#29016,#29014,#15561,.T.);
#36984=EDGE_CURVE('',#29015,#29016,#15562,.T.);
#36985=EDGE_CURVE('',#29017,#29015,#15563,.T.);
#36986=EDGE_CURVE('',#29018,#29016,#15564,.T.);
#36987=EDGE_CURVE('',#29017,#29018,#15565,.T.);
#36988=EDGE_CURVE('',#29019,#29017,#15566,.T.);
#36989=EDGE_CURVE('',#29020,#29018,#15567,.T.);
#36990=EDGE_CURVE('',#29019,#29020,#15568,.T.);
#36991=EDGE_CURVE('',#29021,#29019,#15569,.T.);
#36992=EDGE_CURVE('',#29022,#29020,#15570,.T.);
#36993=EDGE_CURVE('',#29021,#29022,#15571,.T.);
#36994=EDGE_CURVE('',#29023,#29021,#15572,.T.);
#36995=EDGE_CURVE('',#29024,#29022,#15573,.T.);
#36996=EDGE_CURVE('',#29023,#29024,#15574,.T.);
#36997=EDGE_CURVE('',#29025,#29023,#15575,.T.);
#36998=EDGE_CURVE('',#29026,#29024,#15576,.T.);
#36999=EDGE_CURVE('',#29025,#29026,#15577,.T.);
#37000=EDGE_CURVE('',#29027,#29025,#15578,.T.);
#37001=EDGE_CURVE('',#29028,#29026,#15579,.T.);
#37002=EDGE_CURVE('',#29027,#29028,#15580,.T.);
#37003=EDGE_CURVE('',#29029,#29027,#15581,.T.);
#37004=EDGE_CURVE('',#29030,#29028,#15582,.T.);
#37005=EDGE_CURVE('',#29029,#29030,#15583,.T.);
#37006=EDGE_CURVE('',#29031,#29029,#15584,.T.);
#37007=EDGE_CURVE('',#29032,#29030,#15585,.T.);
#37008=EDGE_CURVE('',#29031,#29032,#15586,.T.);
#37009=EDGE_CURVE('',#29033,#29031,#15587,.T.);
#37010=EDGE_CURVE('',#29034,#29032,#15588,.T.);
#37011=EDGE_CURVE('',#29033,#29034,#15589,.T.);
#37012=EDGE_CURVE('',#29035,#29033,#15590,.T.);
#37013=EDGE_CURVE('',#29036,#29034,#15591,.T.);
#37014=EDGE_CURVE('',#29035,#29036,#15592,.T.);
#37015=EDGE_CURVE('',#29037,#29035,#15593,.T.);
#37016=EDGE_CURVE('',#29038,#29036,#15594,.T.);
#37017=EDGE_CURVE('',#29037,#29038,#15595,.T.);
#37018=EDGE_CURVE('',#29039,#29037,#15596,.T.);
#37019=EDGE_CURVE('',#29040,#29038,#15597,.T.);
#37020=EDGE_CURVE('',#29039,#29040,#15598,.T.);
#37021=EDGE_CURVE('',#29041,#29039,#15599,.T.);
#37022=EDGE_CURVE('',#29042,#29040,#15600,.T.);
#37023=EDGE_CURVE('',#29041,#29042,#15601,.T.);
#37024=EDGE_CURVE('',#29043,#29041,#15602,.T.);
#37025=EDGE_CURVE('',#29044,#29042,#15603,.T.);
#37026=EDGE_CURVE('',#29043,#29044,#15604,.T.);
#37027=EDGE_CURVE('',#29045,#29043,#15605,.T.);
#37028=EDGE_CURVE('',#29046,#29044,#15606,.T.);
#37029=EDGE_CURVE('',#29045,#29046,#15607,.T.);
#37030=EDGE_CURVE('',#29047,#29045,#15608,.T.);
#37031=EDGE_CURVE('',#29048,#29046,#15609,.T.);
#37032=EDGE_CURVE('',#29047,#29048,#15610,.T.);
#37033=EDGE_CURVE('',#29049,#29047,#15611,.T.);
#37034=EDGE_CURVE('',#29050,#29048,#15612,.T.);
#37035=EDGE_CURVE('',#29049,#29050,#15613,.T.);
#37036=EDGE_CURVE('',#29051,#29049,#15614,.T.);
#37037=EDGE_CURVE('',#29052,#29050,#15615,.T.);
#37038=EDGE_CURVE('',#29051,#29052,#15616,.T.);
#37039=EDGE_CURVE('',#29053,#29051,#15617,.T.);
#37040=EDGE_CURVE('',#29054,#29052,#15618,.T.);
#37041=EDGE_CURVE('',#29053,#29054,#15619,.T.);
#37042=EDGE_CURVE('',#29055,#29053,#15620,.T.);
#37043=EDGE_CURVE('',#29056,#29054,#15621,.T.);
#37044=EDGE_CURVE('',#29055,#29056,#15622,.T.);
#37045=EDGE_CURVE('',#29057,#29055,#15623,.T.);
#37046=EDGE_CURVE('',#29058,#29056,#15624,.T.);
#37047=EDGE_CURVE('',#29057,#29058,#15625,.T.);
#37048=EDGE_CURVE('',#29059,#29057,#15626,.T.);
#37049=EDGE_CURVE('',#29060,#29058,#15627,.T.);
#37050=EDGE_CURVE('',#29059,#29060,#15628,.T.);
#37051=EDGE_CURVE('',#29061,#29059,#15629,.T.);
#37052=EDGE_CURVE('',#29062,#29060,#15630,.T.);
#37053=EDGE_CURVE('',#29061,#29062,#15631,.T.);
#37054=EDGE_CURVE('',#29063,#29061,#15632,.T.);
#37055=EDGE_CURVE('',#29064,#29062,#15633,.T.);
#37056=EDGE_CURVE('',#29063,#29064,#15634,.T.);
#37057=EDGE_CURVE('',#29065,#29063,#15635,.T.);
#37058=EDGE_CURVE('',#29066,#29064,#15636,.T.);
#37059=EDGE_CURVE('',#29065,#29066,#15637,.T.);
#37060=EDGE_CURVE('',#29067,#29065,#15638,.T.);
#37061=EDGE_CURVE('',#29068,#29066,#15639,.T.);
#37062=EDGE_CURVE('',#29067,#29068,#15640,.T.);
#37063=EDGE_CURVE('',#29069,#29067,#15641,.T.);
#37064=EDGE_CURVE('',#29070,#29068,#15642,.T.);
#37065=EDGE_CURVE('',#29069,#29070,#15643,.T.);
#37066=EDGE_CURVE('',#29071,#29069,#15644,.T.);
#37067=EDGE_CURVE('',#29072,#29070,#15645,.T.);
#37068=EDGE_CURVE('',#29071,#29072,#15646,.T.);
#37069=EDGE_CURVE('',#29073,#29071,#15647,.T.);
#37070=EDGE_CURVE('',#29074,#29072,#15648,.T.);
#37071=EDGE_CURVE('',#29073,#29074,#15649,.T.);
#37072=EDGE_CURVE('',#29075,#29073,#15650,.T.);
#37073=EDGE_CURVE('',#29076,#29074,#15651,.T.);
#37074=EDGE_CURVE('',#29075,#29076,#15652,.T.);
#37075=EDGE_CURVE('',#29077,#29075,#15653,.T.);
#37076=EDGE_CURVE('',#29078,#29076,#15654,.T.);
#37077=EDGE_CURVE('',#29077,#29078,#15655,.T.);
#37078=EDGE_CURVE('',#29079,#29077,#15656,.T.);
#37079=EDGE_CURVE('',#29080,#29078,#15657,.T.);
#37080=EDGE_CURVE('',#29079,#29080,#15658,.T.);
#37081=EDGE_CURVE('',#29081,#29079,#15659,.T.);
#37082=EDGE_CURVE('',#29082,#29080,#15660,.T.);
#37083=EDGE_CURVE('',#29081,#29082,#15661,.T.);
#37084=EDGE_CURVE('',#29083,#29081,#15662,.T.);
#37085=EDGE_CURVE('',#29084,#29082,#15663,.T.);
#37086=EDGE_CURVE('',#29083,#29084,#15664,.T.);
#37087=EDGE_CURVE('',#29085,#29083,#15665,.T.);
#37088=EDGE_CURVE('',#29086,#29084,#15666,.T.);
#37089=EDGE_CURVE('',#29085,#29086,#15667,.T.);
#37090=EDGE_CURVE('',#29087,#29085,#15668,.T.);
#37091=EDGE_CURVE('',#29088,#29086,#15669,.T.);
#37092=EDGE_CURVE('',#29087,#29088,#15670,.T.);
#37093=EDGE_CURVE('',#29089,#29087,#15671,.T.);
#37094=EDGE_CURVE('',#29090,#29088,#15672,.T.);
#37095=EDGE_CURVE('',#29089,#29090,#15673,.T.);
#37096=EDGE_CURVE('',#29091,#29089,#15674,.T.);
#37097=EDGE_CURVE('',#29092,#29090,#15675,.T.);
#37098=EDGE_CURVE('',#29091,#29092,#15676,.T.);
#37099=EDGE_CURVE('',#29093,#29091,#15677,.T.);
#37100=EDGE_CURVE('',#29094,#29092,#15678,.T.);
#37101=EDGE_CURVE('',#29093,#29094,#15679,.T.);
#37102=EDGE_CURVE('',#29095,#29093,#15680,.T.);
#37103=EDGE_CURVE('',#29096,#29094,#15681,.T.);
#37104=EDGE_CURVE('',#29095,#29096,#15682,.T.);
#37105=EDGE_CURVE('',#29097,#29095,#15683,.T.);
#37106=EDGE_CURVE('',#29098,#29096,#15684,.T.);
#37107=EDGE_CURVE('',#29097,#29098,#15685,.T.);
#37108=EDGE_CURVE('',#29099,#29097,#15686,.T.);
#37109=EDGE_CURVE('',#29100,#29098,#15687,.T.);
#37110=EDGE_CURVE('',#29099,#29100,#15688,.T.);
#37111=EDGE_CURVE('',#29101,#29099,#15689,.T.);
#37112=EDGE_CURVE('',#29102,#29100,#15690,.T.);
#37113=EDGE_CURVE('',#29101,#29102,#15691,.T.);
#37114=EDGE_CURVE('',#29103,#29101,#15692,.T.);
#37115=EDGE_CURVE('',#29104,#29102,#15693,.T.);
#37116=EDGE_CURVE('',#29103,#29104,#15694,.T.);
#37117=EDGE_CURVE('',#29105,#29103,#15695,.T.);
#37118=EDGE_CURVE('',#29106,#29104,#15696,.T.);
#37119=EDGE_CURVE('',#29105,#29106,#15697,.T.);
#37120=EDGE_CURVE('',#29107,#29105,#15698,.T.);
#37121=EDGE_CURVE('',#29108,#29106,#15699,.T.);
#37122=EDGE_CURVE('',#29107,#29108,#15700,.T.);
#37123=EDGE_CURVE('',#29109,#29107,#15701,.T.);
#37124=EDGE_CURVE('',#29110,#29108,#15702,.T.);
#37125=EDGE_CURVE('',#29109,#29110,#15703,.T.);
#37126=EDGE_CURVE('',#29111,#29109,#15704,.T.);
#37127=EDGE_CURVE('',#29112,#29110,#15705,.T.);
#37128=EDGE_CURVE('',#29111,#29112,#15706,.T.);
#37129=EDGE_CURVE('',#29113,#29111,#15707,.T.);
#37130=EDGE_CURVE('',#29114,#29112,#15708,.T.);
#37131=EDGE_CURVE('',#29113,#29114,#15709,.T.);
#37132=EDGE_CURVE('',#29115,#29113,#15710,.T.);
#37133=EDGE_CURVE('',#29116,#29114,#15711,.T.);
#37134=EDGE_CURVE('',#29115,#29116,#15712,.T.);
#37135=EDGE_CURVE('',#29117,#29115,#15713,.T.);
#37136=EDGE_CURVE('',#29118,#29116,#15714,.T.);
#37137=EDGE_CURVE('',#29117,#29118,#15715,.T.);
#37138=EDGE_CURVE('',#29119,#29117,#15716,.T.);
#37139=EDGE_CURVE('',#29120,#29118,#15717,.T.);
#37140=EDGE_CURVE('',#29119,#29120,#15718,.T.);
#37141=EDGE_CURVE('',#29121,#29119,#15719,.T.);
#37142=EDGE_CURVE('',#29122,#29120,#15720,.T.);
#37143=EDGE_CURVE('',#29121,#29122,#15721,.T.);
#37144=EDGE_CURVE('',#29123,#29121,#15722,.T.);
#37145=EDGE_CURVE('',#29124,#29122,#15723,.T.);
#37146=EDGE_CURVE('',#29123,#29124,#15724,.T.);
#37147=EDGE_CURVE('',#29125,#29123,#15725,.T.);
#37148=EDGE_CURVE('',#29126,#29124,#15726,.T.);
#37149=EDGE_CURVE('',#29125,#29126,#15727,.T.);
#37150=EDGE_CURVE('',#29127,#29125,#15728,.T.);
#37151=EDGE_CURVE('',#29128,#29126,#15729,.T.);
#37152=EDGE_CURVE('',#29127,#29128,#15730,.T.);
#37153=EDGE_CURVE('',#29129,#29127,#15731,.T.);
#37154=EDGE_CURVE('',#29130,#29128,#15732,.T.);
#37155=EDGE_CURVE('',#29129,#29130,#15733,.T.);
#37156=EDGE_CURVE('',#29131,#29129,#15734,.T.);
#37157=EDGE_CURVE('',#29132,#29130,#15735,.T.);
#37158=EDGE_CURVE('',#29131,#29132,#15736,.T.);
#37159=EDGE_CURVE('',#29133,#29131,#15737,.T.);
#37160=EDGE_CURVE('',#29134,#29132,#15738,.T.);
#37161=EDGE_CURVE('',#29133,#29134,#15739,.T.);
#37162=EDGE_CURVE('',#29135,#29133,#15740,.T.);
#37163=EDGE_CURVE('',#29136,#29134,#15741,.T.);
#37164=EDGE_CURVE('',#29135,#29136,#15742,.T.);
#37165=EDGE_CURVE('',#29137,#29135,#15743,.T.);
#37166=EDGE_CURVE('',#29138,#29136,#15744,.T.);
#37167=EDGE_CURVE('',#29137,#29138,#15745,.T.);
#37168=EDGE_CURVE('',#29139,#29137,#15746,.T.);
#37169=EDGE_CURVE('',#29140,#29138,#15747,.T.);
#37170=EDGE_CURVE('',#29139,#29140,#15748,.T.);
#37171=EDGE_CURVE('',#29141,#29139,#15749,.T.);
#37172=EDGE_CURVE('',#29142,#29140,#15750,.T.);
#37173=EDGE_CURVE('',#29141,#29142,#15751,.T.);
#37174=EDGE_CURVE('',#29143,#29141,#15752,.T.);
#37175=EDGE_CURVE('',#29144,#29142,#15753,.T.);
#37176=EDGE_CURVE('',#29143,#29144,#15754,.T.);
#37177=EDGE_CURVE('',#29145,#29143,#15755,.T.);
#37178=EDGE_CURVE('',#29146,#29144,#15756,.T.);
#37179=EDGE_CURVE('',#29145,#29146,#15757,.T.);
#37180=EDGE_CURVE('',#29147,#29145,#15758,.T.);
#37181=EDGE_CURVE('',#29148,#29146,#15759,.T.);
#37182=EDGE_CURVE('',#29147,#29148,#15760,.T.);
#37183=EDGE_CURVE('',#29149,#29147,#15761,.T.);
#37184=EDGE_CURVE('',#29150,#29148,#15762,.T.);
#37185=EDGE_CURVE('',#29149,#29150,#15763,.T.);
#37186=EDGE_CURVE('',#29151,#29149,#15764,.T.);
#37187=EDGE_CURVE('',#29152,#29150,#15765,.T.);
#37188=EDGE_CURVE('',#29151,#29152,#15766,.T.);
#37189=EDGE_CURVE('',#29153,#29151,#15767,.T.);
#37190=EDGE_CURVE('',#29154,#29152,#15768,.T.);
#37191=EDGE_CURVE('',#29153,#29154,#15769,.T.);
#37192=EDGE_CURVE('',#29155,#29153,#15770,.T.);
#37193=EDGE_CURVE('',#29156,#29154,#15771,.T.);
#37194=EDGE_CURVE('',#29155,#29156,#15772,.T.);
#37195=EDGE_CURVE('',#29157,#29155,#15773,.T.);
#37196=EDGE_CURVE('',#29158,#29156,#15774,.T.);
#37197=EDGE_CURVE('',#29157,#29158,#15775,.T.);
#37198=EDGE_CURVE('',#29159,#29157,#15776,.T.);
#37199=EDGE_CURVE('',#29160,#29158,#15777,.T.);
#37200=EDGE_CURVE('',#29159,#29160,#15778,.T.);
#37201=EDGE_CURVE('',#29161,#29159,#15779,.T.);
#37202=EDGE_CURVE('',#29162,#29160,#15780,.T.);
#37203=EDGE_CURVE('',#29161,#29162,#15781,.T.);
#37204=EDGE_CURVE('',#29163,#29161,#15782,.T.);
#37205=EDGE_CURVE('',#29164,#29162,#15783,.T.);
#37206=EDGE_CURVE('',#29163,#29164,#15784,.T.);
#37207=EDGE_CURVE('',#29165,#29163,#15785,.T.);
#37208=EDGE_CURVE('',#29166,#29164,#15786,.T.);
#37209=EDGE_CURVE('',#29165,#29166,#15787,.T.);
#37210=EDGE_CURVE('',#29167,#29165,#15788,.T.);
#37211=EDGE_CURVE('',#29168,#29166,#15789,.T.);
#37212=EDGE_CURVE('',#29167,#29168,#15790,.T.);
#37213=EDGE_CURVE('',#29169,#29167,#15791,.T.);
#37214=EDGE_CURVE('',#29170,#29168,#15792,.T.);
#37215=EDGE_CURVE('',#29169,#29170,#15793,.T.);
#37216=EDGE_CURVE('',#29171,#29169,#15794,.T.);
#37217=EDGE_CURVE('',#29172,#29170,#15795,.T.);
#37218=EDGE_CURVE('',#29171,#29172,#15796,.T.);
#37219=EDGE_CURVE('',#29173,#29171,#15797,.T.);
#37220=EDGE_CURVE('',#29174,#29172,#15798,.T.);
#37221=EDGE_CURVE('',#29173,#29174,#15799,.T.);
#37222=EDGE_CURVE('',#29175,#29173,#15800,.T.);
#37223=EDGE_CURVE('',#29176,#29174,#15801,.T.);
#37224=EDGE_CURVE('',#29175,#29176,#15802,.T.);
#37225=EDGE_CURVE('',#29177,#29175,#15803,.T.);
#37226=EDGE_CURVE('',#29178,#29176,#15804,.T.);
#37227=EDGE_CURVE('',#29177,#29178,#15805,.T.);
#37228=EDGE_CURVE('',#29179,#29177,#15806,.T.);
#37229=EDGE_CURVE('',#29180,#29178,#15807,.T.);
#37230=EDGE_CURVE('',#29179,#29180,#15808,.T.);
#37231=EDGE_CURVE('',#29181,#29179,#15809,.T.);
#37232=EDGE_CURVE('',#29182,#29180,#15810,.T.);
#37233=EDGE_CURVE('',#29181,#29182,#15811,.T.);
#37234=EDGE_CURVE('',#29183,#29181,#15812,.T.);
#37235=EDGE_CURVE('',#29184,#29182,#15813,.T.);
#37236=EDGE_CURVE('',#29183,#29184,#15814,.T.);
#37237=EDGE_CURVE('',#29185,#29183,#15815,.T.);
#37238=EDGE_CURVE('',#29186,#29184,#15816,.T.);
#37239=EDGE_CURVE('',#29185,#29186,#15817,.T.);
#37240=EDGE_CURVE('',#29187,#29185,#15818,.T.);
#37241=EDGE_CURVE('',#29188,#29186,#15819,.T.);
#37242=EDGE_CURVE('',#29187,#29188,#15820,.T.);
#37243=EDGE_CURVE('',#29189,#29187,#15821,.T.);
#37244=EDGE_CURVE('',#29190,#29188,#15822,.T.);
#37245=EDGE_CURVE('',#29189,#29190,#15823,.T.);
#37246=EDGE_CURVE('',#29191,#29189,#15824,.T.);
#37247=EDGE_CURVE('',#29192,#29190,#15825,.T.);
#37248=EDGE_CURVE('',#29191,#29192,#15826,.T.);
#37249=EDGE_CURVE('',#29193,#29191,#15827,.T.);
#37250=EDGE_CURVE('',#29194,#29192,#15828,.T.);
#37251=EDGE_CURVE('',#29193,#29194,#15829,.T.);
#37252=EDGE_CURVE('',#29195,#29193,#15830,.T.);
#37253=EDGE_CURVE('',#29196,#29194,#15831,.T.);
#37254=EDGE_CURVE('',#29195,#29196,#15832,.T.);
#37255=EDGE_CURVE('',#29197,#29195,#15833,.T.);
#37256=EDGE_CURVE('',#29198,#29196,#15834,.T.);
#37257=EDGE_CURVE('',#29197,#29198,#15835,.T.);
#37258=EDGE_CURVE('',#29199,#29197,#15836,.T.);
#37259=EDGE_CURVE('',#29200,#29198,#15837,.T.);
#37260=EDGE_CURVE('',#29199,#29200,#15838,.T.);
#37261=EDGE_CURVE('',#29201,#29199,#15839,.T.);
#37262=EDGE_CURVE('',#29202,#29200,#15840,.T.);
#37263=EDGE_CURVE('',#29201,#29202,#15841,.T.);
#37264=EDGE_CURVE('',#29203,#29201,#15842,.T.);
#37265=EDGE_CURVE('',#29204,#29202,#15843,.T.);
#37266=EDGE_CURVE('',#29203,#29204,#15844,.T.);
#37267=EDGE_CURVE('',#29205,#29203,#15845,.T.);
#37268=EDGE_CURVE('',#29206,#29204,#15846,.T.);
#37269=EDGE_CURVE('',#29205,#29206,#15847,.T.);
#37270=EDGE_CURVE('',#29207,#29205,#15848,.T.);
#37271=EDGE_CURVE('',#29208,#29206,#15849,.T.);
#37272=EDGE_CURVE('',#29207,#29208,#15850,.T.);
#37273=EDGE_CURVE('',#29209,#29207,#15851,.T.);
#37274=EDGE_CURVE('',#29210,#29208,#15852,.T.);
#37275=EDGE_CURVE('',#29209,#29210,#15853,.T.);
#37276=EDGE_CURVE('',#29211,#29209,#15854,.T.);
#37277=EDGE_CURVE('',#29212,#29210,#15855,.T.);
#37278=EDGE_CURVE('',#29211,#29212,#15856,.T.);
#37279=EDGE_CURVE('',#29213,#29211,#15857,.T.);
#37280=EDGE_CURVE('',#29214,#29212,#15858,.T.);
#37281=EDGE_CURVE('',#29213,#29214,#15859,.T.);
#37282=EDGE_CURVE('',#29215,#29213,#15860,.T.);
#37283=EDGE_CURVE('',#29216,#29214,#15861,.T.);
#37284=EDGE_CURVE('',#29215,#29216,#15862,.T.);
#37285=EDGE_CURVE('',#29217,#29215,#15863,.T.);
#37286=EDGE_CURVE('',#29218,#29216,#15864,.T.);
#37287=EDGE_CURVE('',#29217,#29218,#15865,.T.);
#37288=EDGE_CURVE('',#29219,#29217,#15866,.T.);
#37289=EDGE_CURVE('',#29220,#29218,#15867,.T.);
#37290=EDGE_CURVE('',#29219,#29220,#15868,.T.);
#37291=EDGE_CURVE('',#29221,#29219,#15869,.T.);
#37292=EDGE_CURVE('',#29222,#29220,#15870,.T.);
#37293=EDGE_CURVE('',#29221,#29222,#15871,.T.);
#37294=EDGE_CURVE('',#29223,#29221,#15872,.T.);
#37295=EDGE_CURVE('',#29224,#29222,#15873,.T.);
#37296=EDGE_CURVE('',#29223,#29224,#15874,.T.);
#37297=EDGE_CURVE('',#29225,#29223,#15875,.T.);
#37298=EDGE_CURVE('',#29226,#29224,#15876,.T.);
#37299=EDGE_CURVE('',#29225,#29226,#15877,.T.);
#37300=EDGE_CURVE('',#29227,#29225,#15878,.T.);
#37301=EDGE_CURVE('',#29228,#29226,#15879,.T.);
#37302=EDGE_CURVE('',#29227,#29228,#15880,.T.);
#37303=EDGE_CURVE('',#29229,#29227,#15881,.T.);
#37304=EDGE_CURVE('',#29230,#29228,#15882,.T.);
#37305=EDGE_CURVE('',#29229,#29230,#15883,.T.);
#37306=EDGE_CURVE('',#29231,#29229,#15884,.T.);
#37307=EDGE_CURVE('',#29232,#29230,#15885,.T.);
#37308=EDGE_CURVE('',#29231,#29232,#15886,.T.);
#37309=EDGE_CURVE('',#29233,#29231,#15887,.T.);
#37310=EDGE_CURVE('',#29234,#29232,#15888,.T.);
#37311=EDGE_CURVE('',#29233,#29234,#15889,.T.);
#37312=EDGE_CURVE('',#29235,#29233,#15890,.T.);
#37313=EDGE_CURVE('',#29236,#29234,#15891,.T.);
#37314=EDGE_CURVE('',#29235,#29236,#15892,.T.);
#37315=EDGE_CURVE('',#29237,#29235,#15893,.T.);
#37316=EDGE_CURVE('',#29238,#29236,#15894,.T.);
#37317=EDGE_CURVE('',#29237,#29238,#15895,.T.);
#37318=EDGE_CURVE('',#29239,#29237,#15896,.T.);
#37319=EDGE_CURVE('',#29240,#29238,#15897,.T.);
#37320=EDGE_CURVE('',#29239,#29240,#15898,.T.);
#37321=EDGE_CURVE('',#29241,#29239,#15899,.T.);
#37322=EDGE_CURVE('',#29242,#29240,#15900,.T.);
#37323=EDGE_CURVE('',#29241,#29242,#15901,.T.);
#37324=EDGE_CURVE('',#29243,#29241,#15902,.T.);
#37325=EDGE_CURVE('',#29244,#29242,#15903,.T.);
#37326=EDGE_CURVE('',#29243,#29244,#15904,.T.);
#37327=EDGE_CURVE('',#29245,#29243,#15905,.T.);
#37328=EDGE_CURVE('',#29246,#29244,#15906,.T.);
#37329=EDGE_CURVE('',#29245,#29246,#15907,.T.);
#37330=EDGE_CURVE('',#29247,#29245,#15908,.T.);
#37331=EDGE_CURVE('',#29248,#29246,#15909,.T.);
#37332=EDGE_CURVE('',#29247,#29248,#15910,.T.);
#37333=EDGE_CURVE('',#29249,#29247,#15911,.T.);
#37334=EDGE_CURVE('',#29250,#29248,#15912,.T.);
#37335=EDGE_CURVE('',#29249,#29250,#15913,.T.);
#37336=EDGE_CURVE('',#29251,#29249,#15914,.T.);
#37337=EDGE_CURVE('',#29252,#29250,#15915,.T.);
#37338=EDGE_CURVE('',#29251,#29252,#15916,.T.);
#37339=EDGE_CURVE('',#29253,#29251,#15917,.T.);
#37340=EDGE_CURVE('',#29254,#29252,#15918,.T.);
#37341=EDGE_CURVE('',#29253,#29254,#15919,.T.);
#37342=EDGE_CURVE('',#29255,#29253,#15920,.T.);
#37343=EDGE_CURVE('',#29256,#29254,#15921,.T.);
#37344=EDGE_CURVE('',#29255,#29256,#15922,.T.);
#37345=EDGE_CURVE('',#29257,#29255,#15923,.T.);
#37346=EDGE_CURVE('',#29258,#29256,#15924,.T.);
#37347=EDGE_CURVE('',#29257,#29258,#15925,.T.);
#37348=EDGE_CURVE('',#29259,#29257,#15926,.T.);
#37349=EDGE_CURVE('',#29260,#29258,#15927,.T.);
#37350=EDGE_CURVE('',#29259,#29260,#15928,.T.);
#37351=EDGE_CURVE('',#29261,#29259,#15929,.T.);
#37352=EDGE_CURVE('',#29262,#29260,#15930,.T.);
#37353=EDGE_CURVE('',#29261,#29262,#15931,.T.);
#37354=EDGE_CURVE('',#29263,#29261,#15932,.T.);
#37355=EDGE_CURVE('',#29264,#29262,#15933,.T.);
#37356=EDGE_CURVE('',#29263,#29264,#15934,.T.);
#37357=EDGE_CURVE('',#29265,#29263,#15935,.T.);
#37358=EDGE_CURVE('',#29266,#29264,#15936,.T.);
#37359=EDGE_CURVE('',#29265,#29266,#15937,.T.);
#37360=EDGE_CURVE('',#29267,#29265,#15938,.T.);
#37361=EDGE_CURVE('',#29268,#29266,#15939,.T.);
#37362=EDGE_CURVE('',#29267,#29268,#15940,.T.);
#37363=EDGE_CURVE('',#29269,#29267,#15941,.T.);
#37364=EDGE_CURVE('',#29270,#29268,#15942,.T.);
#37365=EDGE_CURVE('',#29269,#29270,#15943,.T.);
#37366=EDGE_CURVE('',#29271,#29269,#15944,.T.);
#37367=EDGE_CURVE('',#29272,#29270,#15945,.T.);
#37368=EDGE_CURVE('',#29271,#29272,#15946,.T.);
#37369=EDGE_CURVE('',#29273,#29271,#15947,.T.);
#37370=EDGE_CURVE('',#29274,#29272,#15948,.T.);
#37371=EDGE_CURVE('',#29273,#29274,#15949,.T.);
#37372=EDGE_CURVE('',#29275,#29273,#15950,.T.);
#37373=EDGE_CURVE('',#29276,#29274,#15951,.T.);
#37374=EDGE_CURVE('',#29275,#29276,#15952,.T.);
#37375=EDGE_CURVE('',#29277,#29275,#15953,.T.);
#37376=EDGE_CURVE('',#29278,#29276,#15954,.T.);
#37377=EDGE_CURVE('',#29277,#29278,#15955,.T.);
#37378=EDGE_CURVE('',#29279,#29277,#15956,.T.);
#37379=EDGE_CURVE('',#29280,#29278,#15957,.T.);
#37380=EDGE_CURVE('',#29279,#29280,#15958,.T.);
#37381=EDGE_CURVE('',#29281,#29279,#15959,.T.);
#37382=EDGE_CURVE('',#29282,#29280,#15960,.T.);
#37383=EDGE_CURVE('',#29281,#29282,#15961,.T.);
#37384=EDGE_CURVE('',#29283,#29281,#15962,.T.);
#37385=EDGE_CURVE('',#29284,#29282,#15963,.T.);
#37386=EDGE_CURVE('',#29283,#29284,#15964,.T.);
#37387=EDGE_CURVE('',#29285,#29283,#15965,.T.);
#37388=EDGE_CURVE('',#29286,#29284,#15966,.T.);
#37389=EDGE_CURVE('',#29285,#29286,#15967,.T.);
#37390=EDGE_CURVE('',#29287,#29285,#15968,.T.);
#37391=EDGE_CURVE('',#29288,#29286,#15969,.T.);
#37392=EDGE_CURVE('',#29287,#29288,#15970,.T.);
#37393=EDGE_CURVE('',#29289,#29287,#15971,.T.);
#37394=EDGE_CURVE('',#29290,#29288,#15972,.T.);
#37395=EDGE_CURVE('',#29289,#29290,#15973,.T.);
#37396=EDGE_CURVE('',#29291,#29289,#15974,.T.);
#37397=EDGE_CURVE('',#29292,#29290,#15975,.T.);
#37398=EDGE_CURVE('',#29291,#29292,#15976,.T.);
#37399=EDGE_CURVE('',#29293,#29291,#15977,.T.);
#37400=EDGE_CURVE('',#29294,#29292,#15978,.T.);
#37401=EDGE_CURVE('',#29293,#29294,#15979,.T.);
#37402=EDGE_CURVE('',#29295,#29293,#15980,.T.);
#37403=EDGE_CURVE('',#29296,#29294,#15981,.T.);
#37404=EDGE_CURVE('',#29295,#29296,#15982,.T.);
#37405=EDGE_CURVE('',#29297,#29295,#15983,.T.);
#37406=EDGE_CURVE('',#29298,#29296,#15984,.T.);
#37407=EDGE_CURVE('',#29297,#29298,#15985,.T.);
#37408=EDGE_CURVE('',#29299,#29297,#15986,.T.);
#37409=EDGE_CURVE('',#29300,#29298,#15987,.T.);
#37410=EDGE_CURVE('',#29299,#29300,#15988,.T.);
#37411=EDGE_CURVE('',#29301,#29299,#15989,.T.);
#37412=EDGE_CURVE('',#29302,#29300,#15990,.T.);
#37413=EDGE_CURVE('',#29301,#29302,#15991,.T.);
#37414=EDGE_CURVE('',#29303,#29301,#15992,.T.);
#37415=EDGE_CURVE('',#29304,#29302,#15993,.T.);
#37416=EDGE_CURVE('',#29303,#29304,#15994,.T.);
#37417=EDGE_CURVE('',#29305,#29303,#15995,.T.);
#37418=EDGE_CURVE('',#29306,#29304,#15996,.T.);
#37419=EDGE_CURVE('',#29305,#29306,#15997,.T.);
#37420=EDGE_CURVE('',#29307,#29305,#15998,.T.);
#37421=EDGE_CURVE('',#29308,#29306,#15999,.T.);
#37422=EDGE_CURVE('',#29307,#29308,#16000,.T.);
#37423=EDGE_CURVE('',#29309,#29307,#16001,.T.);
#37424=EDGE_CURVE('',#29310,#29308,#16002,.T.);
#37425=EDGE_CURVE('',#29309,#29310,#16003,.T.);
#37426=EDGE_CURVE('',#29311,#29309,#16004,.T.);
#37427=EDGE_CURVE('',#29312,#29310,#16005,.T.);
#37428=EDGE_CURVE('',#29311,#29312,#16006,.T.);
#37429=EDGE_CURVE('',#29313,#29311,#16007,.T.);
#37430=EDGE_CURVE('',#29314,#29312,#16008,.T.);
#37431=EDGE_CURVE('',#29313,#29314,#16009,.T.);
#37432=EDGE_CURVE('',#29315,#29313,#16010,.T.);
#37433=EDGE_CURVE('',#29316,#29314,#16011,.T.);
#37434=EDGE_CURVE('',#29315,#29316,#16012,.T.);
#37435=EDGE_CURVE('',#29317,#29315,#16013,.T.);
#37436=EDGE_CURVE('',#29318,#29316,#16014,.T.);
#37437=EDGE_CURVE('',#29317,#29318,#16015,.T.);
#37438=EDGE_CURVE('',#29319,#29317,#16016,.T.);
#37439=EDGE_CURVE('',#29320,#29318,#16017,.T.);
#37440=EDGE_CURVE('',#29319,#29320,#16018,.T.);
#37441=EDGE_CURVE('',#29321,#29319,#16019,.T.);
#37442=EDGE_CURVE('',#29322,#29320,#16020,.T.);
#37443=EDGE_CURVE('',#29321,#29322,#16021,.T.);
#37444=EDGE_CURVE('',#29323,#29321,#16022,.T.);
#37445=EDGE_CURVE('',#29324,#29322,#16023,.T.);
#37446=EDGE_CURVE('',#29323,#29324,#16024,.T.);
#37447=EDGE_CURVE('',#29325,#29323,#16025,.T.);
#37448=EDGE_CURVE('',#29326,#29324,#16026,.T.);
#37449=EDGE_CURVE('',#29325,#29326,#16027,.T.);
#37450=EDGE_CURVE('',#29327,#29325,#16028,.T.);
#37451=EDGE_CURVE('',#29328,#29326,#16029,.T.);
#37452=EDGE_CURVE('',#29327,#29328,#16030,.T.);
#37453=EDGE_CURVE('',#29329,#29327,#16031,.T.);
#37454=EDGE_CURVE('',#29330,#29328,#16032,.T.);
#37455=EDGE_CURVE('',#29329,#29330,#16033,.T.);
#37456=EDGE_CURVE('',#29331,#29329,#16034,.T.);
#37457=EDGE_CURVE('',#29332,#29330,#16035,.T.);
#37458=EDGE_CURVE('',#29331,#29332,#16036,.T.);
#37459=EDGE_CURVE('',#29333,#29331,#16037,.T.);
#37460=EDGE_CURVE('',#29334,#29332,#16038,.T.);
#37461=EDGE_CURVE('',#29333,#29334,#16039,.T.);
#37462=EDGE_CURVE('',#29335,#29333,#16040,.T.);
#37463=EDGE_CURVE('',#29336,#29334,#16041,.T.);
#37464=EDGE_CURVE('',#29335,#29336,#16042,.T.);
#37465=EDGE_CURVE('',#29337,#29335,#16043,.T.);
#37466=EDGE_CURVE('',#29338,#29336,#16044,.T.);
#37467=EDGE_CURVE('',#29337,#29338,#16045,.T.);
#37468=EDGE_CURVE('',#29339,#29337,#16046,.T.);
#37469=EDGE_CURVE('',#29340,#29338,#16047,.T.);
#37470=EDGE_CURVE('',#29339,#29340,#16048,.T.);
#37471=EDGE_CURVE('',#29341,#29339,#16049,.T.);
#37472=EDGE_CURVE('',#29342,#29340,#16050,.T.);
#37473=EDGE_CURVE('',#29341,#29342,#16051,.T.);
#37474=EDGE_CURVE('',#29343,#29341,#16052,.T.);
#37475=EDGE_CURVE('',#29344,#29342,#16053,.T.);
#37476=EDGE_CURVE('',#29343,#29344,#16054,.T.);
#37477=EDGE_CURVE('',#29345,#29343,#16055,.T.);
#37478=EDGE_CURVE('',#29346,#29344,#16056,.T.);
#37479=EDGE_CURVE('',#29345,#29346,#16057,.T.);
#37480=EDGE_CURVE('',#29347,#29345,#16058,.T.);
#37481=EDGE_CURVE('',#29348,#29346,#16059,.T.);
#37482=EDGE_CURVE('',#29347,#29348,#16060,.T.);
#37483=EDGE_CURVE('',#29349,#29347,#16061,.T.);
#37484=EDGE_CURVE('',#29350,#29348,#16062,.T.);
#37485=EDGE_CURVE('',#29349,#29350,#16063,.T.);
#37486=EDGE_CURVE('',#29351,#29349,#16064,.T.);
#37487=EDGE_CURVE('',#29352,#29350,#16065,.T.);
#37488=EDGE_CURVE('',#29351,#29352,#16066,.T.);
#37489=EDGE_CURVE('',#29353,#29351,#16067,.T.);
#37490=EDGE_CURVE('',#29354,#29352,#16068,.T.);
#37491=EDGE_CURVE('',#29353,#29354,#16069,.T.);
#37492=EDGE_CURVE('',#29355,#29353,#16070,.T.);
#37493=EDGE_CURVE('',#29356,#29354,#16071,.T.);
#37494=EDGE_CURVE('',#29355,#29356,#16072,.T.);
#37495=EDGE_CURVE('',#29357,#29355,#16073,.T.);
#37496=EDGE_CURVE('',#29358,#29356,#16074,.T.);
#37497=EDGE_CURVE('',#29357,#29358,#16075,.T.);
#37498=EDGE_CURVE('',#29359,#29357,#16076,.T.);
#37499=EDGE_CURVE('',#29360,#29358,#16077,.T.);
#37500=EDGE_CURVE('',#29359,#29360,#16078,.T.);
#37501=EDGE_CURVE('',#29361,#29359,#16079,.T.);
#37502=EDGE_CURVE('',#29362,#29360,#16080,.T.);
#37503=EDGE_CURVE('',#29361,#29362,#16081,.T.);
#37504=EDGE_CURVE('',#29363,#29361,#16082,.T.);
#37505=EDGE_CURVE('',#29364,#29362,#16083,.T.);
#37506=EDGE_CURVE('',#29363,#29364,#16084,.T.);
#37507=EDGE_CURVE('',#29365,#29363,#16085,.T.);
#37508=EDGE_CURVE('',#29366,#29364,#16086,.T.);
#37509=EDGE_CURVE('',#29365,#29366,#16087,.T.);
#37510=EDGE_CURVE('',#29367,#29365,#16088,.T.);
#37511=EDGE_CURVE('',#29368,#29366,#16089,.T.);
#37512=EDGE_CURVE('',#29367,#29368,#16090,.T.);
#37513=EDGE_CURVE('',#29369,#29367,#16091,.T.);
#37514=EDGE_CURVE('',#29370,#29368,#16092,.T.);
#37515=EDGE_CURVE('',#29369,#29370,#16093,.T.);
#37516=EDGE_CURVE('',#29371,#29369,#16094,.T.);
#37517=EDGE_CURVE('',#29372,#29370,#16095,.T.);
#37518=EDGE_CURVE('',#29371,#29372,#16096,.T.);
#37519=EDGE_CURVE('',#29373,#29371,#16097,.T.);
#37520=EDGE_CURVE('',#29374,#29372,#16098,.T.);
#37521=EDGE_CURVE('',#29373,#29374,#16099,.T.);
#37522=EDGE_CURVE('',#29375,#29373,#16100,.T.);
#37523=EDGE_CURVE('',#29376,#29374,#16101,.T.);
#37524=EDGE_CURVE('',#29375,#29376,#16102,.T.);
#37525=EDGE_CURVE('',#29377,#29375,#16103,.T.);
#37526=EDGE_CURVE('',#29378,#29376,#16104,.T.);
#37527=EDGE_CURVE('',#29377,#29378,#16105,.T.);
#37528=EDGE_CURVE('',#29379,#29377,#16106,.T.);
#37529=EDGE_CURVE('',#29380,#29378,#16107,.T.);
#37530=EDGE_CURVE('',#29379,#29380,#16108,.T.);
#37531=EDGE_CURVE('',#29381,#29379,#16109,.T.);
#37532=EDGE_CURVE('',#29382,#29380,#16110,.T.);
#37533=EDGE_CURVE('',#29381,#29382,#16111,.T.);
#37534=EDGE_CURVE('',#29383,#29381,#16112,.T.);
#37535=EDGE_CURVE('',#29384,#29382,#16113,.T.);
#37536=EDGE_CURVE('',#29383,#29384,#16114,.T.);
#37537=EDGE_CURVE('',#29385,#29383,#16115,.T.);
#37538=EDGE_CURVE('',#29386,#29384,#16116,.T.);
#37539=EDGE_CURVE('',#29385,#29386,#16117,.T.);
#37540=EDGE_CURVE('',#29387,#29385,#16118,.T.);
#37541=EDGE_CURVE('',#29388,#29386,#16119,.T.);
#37542=EDGE_CURVE('',#29387,#29388,#16120,.T.);
#37543=EDGE_CURVE('',#29389,#29387,#16121,.T.);
#37544=EDGE_CURVE('',#29390,#29388,#16122,.T.);
#37545=EDGE_CURVE('',#29389,#29390,#16123,.T.);
#37546=EDGE_CURVE('',#29391,#29389,#16124,.T.);
#37547=EDGE_CURVE('',#29392,#29390,#16125,.T.);
#37548=EDGE_CURVE('',#29391,#29392,#16126,.T.);
#37549=EDGE_CURVE('',#29393,#29391,#16127,.T.);
#37550=EDGE_CURVE('',#29394,#29392,#16128,.T.);
#37551=EDGE_CURVE('',#29393,#29394,#16129,.T.);
#37552=EDGE_CURVE('',#29395,#29393,#16130,.T.);
#37553=EDGE_CURVE('',#29396,#29394,#16131,.T.);
#37554=EDGE_CURVE('',#29395,#29396,#16132,.T.);
#37555=EDGE_CURVE('',#29397,#29395,#16133,.T.);
#37556=EDGE_CURVE('',#29398,#29396,#16134,.T.);
#37557=EDGE_CURVE('',#29397,#29398,#16135,.T.);
#37558=EDGE_CURVE('',#29399,#29397,#16136,.T.);
#37559=EDGE_CURVE('',#29400,#29398,#16137,.T.);
#37560=EDGE_CURVE('',#29399,#29400,#16138,.T.);
#37561=EDGE_CURVE('',#29401,#29399,#16139,.T.);
#37562=EDGE_CURVE('',#29402,#29400,#16140,.T.);
#37563=EDGE_CURVE('',#29401,#29402,#16141,.T.);
#37564=EDGE_CURVE('',#29403,#29401,#16142,.T.);
#37565=EDGE_CURVE('',#29404,#29402,#16143,.T.);
#37566=EDGE_CURVE('',#29403,#29404,#16144,.T.);
#37567=EDGE_CURVE('',#29405,#29403,#16145,.T.);
#37568=EDGE_CURVE('',#29406,#29404,#16146,.T.);
#37569=EDGE_CURVE('',#29405,#29406,#16147,.T.);
#37570=EDGE_CURVE('',#29407,#29405,#16148,.T.);
#37571=EDGE_CURVE('',#29408,#29406,#16149,.T.);
#37572=EDGE_CURVE('',#29407,#29408,#16150,.T.);
#37573=EDGE_CURVE('',#29409,#29407,#16151,.T.);
#37574=EDGE_CURVE('',#29410,#29408,#16152,.T.);
#37575=EDGE_CURVE('',#29409,#29410,#16153,.T.);
#37576=EDGE_CURVE('',#29411,#29409,#16154,.T.);
#37577=EDGE_CURVE('',#29412,#29410,#16155,.T.);
#37578=EDGE_CURVE('',#29411,#29412,#16156,.T.);
#37579=EDGE_CURVE('',#28395,#29411,#16157,.T.);
#37580=EDGE_CURVE('',#28396,#29412,#16158,.T.);
#37581=EDGE_CURVE('',#28403,#28411,#16159,.T.);
#37582=EDGE_CURVE('',#28402,#28416,#16160,.T.);
#50433=ORIENTED_EDGE('',*,*,#36049,.T.);
#50434=ORIENTED_EDGE('',*,*,#36050,.T.);
#50435=ORIENTED_EDGE('',*,*,#36051,.T.);
#50436=ORIENTED_EDGE('',*,*,#36050,.F.);
#50437=ORIENTED_EDGE('',*,*,#36051,.F.);
#50438=ORIENTED_EDGE('',*,*,#36052,.T.);
#50439=ORIENTED_EDGE('',*,*,#36053,.T.);
#50440=ORIENTED_EDGE('',*,*,#36052,.F.);
#50441=ORIENTED_EDGE('',*,*,#36054,.T.);
#50442=ORIENTED_EDGE('',*,*,#36055,.T.);
#50443=ORIENTED_EDGE('',*,*,#36056,.F.);
#50444=ORIENTED_EDGE('',*,*,#36057,.F.);
#50445=ORIENTED_EDGE('',*,*,#36049,.F.);
#50446=ORIENTED_EDGE('',*,*,#36058,.T.);
#50447=ORIENTED_EDGE('',*,*,#36059,.T.);
#50448=ORIENTED_EDGE('',*,*,#36060,.T.);
#50449=ORIENTED_EDGE('',*,*,#36059,.F.);
#50450=ORIENTED_EDGE('',*,*,#36060,.F.);
#50451=ORIENTED_EDGE('',*,*,#36061,.T.);
#50452=ORIENTED_EDGE('',*,*,#36062,.T.);
#50453=ORIENTED_EDGE('',*,*,#36061,.F.);
#50454=ORIENTED_EDGE('',*,*,#36063,.T.);
#50455=ORIENTED_EDGE('',*,*,#36064,.T.);
#50456=ORIENTED_EDGE('',*,*,#36065,.F.);
#50457=ORIENTED_EDGE('',*,*,#36066,.F.);
#50458=ORIENTED_EDGE('',*,*,#36058,.F.);
#50459=ORIENTED_EDGE('',*,*,#36062,.F.);
#50460=ORIENTED_EDGE('',*,*,#36067,.F.);
#50461=ORIENTED_EDGE('',*,*,#36053,.F.);
#50462=ORIENTED_EDGE('',*,*,#36068,.F.);
#50463=ORIENTED_EDGE('',*,*,#36067,.T.);
#50464=ORIENTED_EDGE('',*,*,#36069,.T.);
#50465=ORIENTED_EDGE('',*,*,#36070,.F.);
#50466=ORIENTED_EDGE('',*,*,#36069,.F.);
#50467=ORIENTED_EDGE('',*,*,#36068,.T.);
#50468=ORIENTED_EDGE('',*,*,#36071,.T.);
#50469=ORIENTED_EDGE('',*,*,#36072,.F.);
#50470=ORIENTED_EDGE('',*,*,#36071,.F.);
#50471=ORIENTED_EDGE('',*,*,#36073,.T.);
#50472=ORIENTED_EDGE('',*,*,#36074,.T.);
#50473=ORIENTED_EDGE('',*,*,#36075,.T.);
#50474=ORIENTED_EDGE('',*,*,#36076,.T.);
#50475=ORIENTED_EDGE('',*,*,#36073,.F.);
#50476=ORIENTED_EDGE('',*,*,#36077,.F.);
#50477=ORIENTED_EDGE('',*,*,#36078,.F.);
#50478=ORIENTED_EDGE('',*,*,#36079,.T.);
#50479=ORIENTED_EDGE('',*,*,#36057,.T.);
#50480=ORIENTED_EDGE('',*,*,#36080,.F.);
#50481=ORIENTED_EDGE('',*,*,#36076,.F.);
#50482=ORIENTED_EDGE('',*,*,#36081,.F.);
#50483=ORIENTED_EDGE('',*,*,#36082,.F.);
#50484=ORIENTED_EDGE('',*,*,#36077,.T.);
#50485=ORIENTED_EDGE('',*,*,#36070,.T.);
#50486=ORIENTED_EDGE('',*,*,#36072,.T.);
#50487=ORIENTED_EDGE('',*,*,#36078,.T.);
#50488=ORIENTED_EDGE('',*,*,#36082,.T.);
#50489=ORIENTED_EDGE('',*,*,#36083,.T.);
#50490=ORIENTED_EDGE('',*,*,#36084,.T.);
#50491=ORIENTED_EDGE('',*,*,#36085,.T.);
#50492=ORIENTED_EDGE('',*,*,#36066,.T.);
#50493=ORIENTED_EDGE('',*,*,#36086,.F.);
#50494=ORIENTED_EDGE('',*,*,#36087,.F.);
#50495=ORIENTED_EDGE('',*,*,#36088,.T.);
#50496=ORIENTED_EDGE('',*,*,#36087,.T.);
#50497=ORIENTED_EDGE('',*,*,#36089,.F.);
#50498=ORIENTED_EDGE('',*,*,#36090,.F.);
#50499=ORIENTED_EDGE('',*,*,#36091,.T.);
#50500=ORIENTED_EDGE('',*,*,#36090,.T.);
#50501=ORIENTED_EDGE('',*,*,#36092,.F.);
#50502=ORIENTED_EDGE('',*,*,#36093,.F.);
#50503=ORIENTED_EDGE('',*,*,#36094,.T.);
#50504=ORIENTED_EDGE('',*,*,#36093,.T.);
#50505=ORIENTED_EDGE('',*,*,#36095,.F.);
#50506=ORIENTED_EDGE('',*,*,#36096,.F.);
#50507=ORIENTED_EDGE('',*,*,#36097,.T.);
#50508=ORIENTED_EDGE('',*,*,#36096,.T.);
#50509=ORIENTED_EDGE('',*,*,#36098,.F.);
#50510=ORIENTED_EDGE('',*,*,#36099,.F.);
#50511=ORIENTED_EDGE('',*,*,#36100,.T.);
#50512=ORIENTED_EDGE('',*,*,#36099,.T.);
#50513=ORIENTED_EDGE('',*,*,#36101,.F.);
#50514=ORIENTED_EDGE('',*,*,#36102,.F.);
#50515=ORIENTED_EDGE('',*,*,#36103,.T.);
#50516=ORIENTED_EDGE('',*,*,#36102,.T.);
#50517=ORIENTED_EDGE('',*,*,#36104,.F.);
#50518=ORIENTED_EDGE('',*,*,#36105,.F.);
#50519=ORIENTED_EDGE('',*,*,#36106,.T.);
#50520=ORIENTED_EDGE('',*,*,#36105,.T.);
#50521=ORIENTED_EDGE('',*,*,#36107,.F.);
#50522=ORIENTED_EDGE('',*,*,#36108,.F.);
#50523=ORIENTED_EDGE('',*,*,#36109,.T.);
#50524=ORIENTED_EDGE('',*,*,#36108,.T.);
#50525=ORIENTED_EDGE('',*,*,#36110,.F.);
#50526=ORIENTED_EDGE('',*,*,#36111,.F.);
#50527=ORIENTED_EDGE('',*,*,#36112,.T.);
#50528=ORIENTED_EDGE('',*,*,#36111,.T.);
#50529=ORIENTED_EDGE('',*,*,#36113,.F.);
#50530=ORIENTED_EDGE('',*,*,#36114,.F.);
#50531=ORIENTED_EDGE('',*,*,#36115,.T.);
#50532=ORIENTED_EDGE('',*,*,#36114,.T.);
#50533=ORIENTED_EDGE('',*,*,#36116,.F.);
#50534=ORIENTED_EDGE('',*,*,#36117,.F.);
#50535=ORIENTED_EDGE('',*,*,#36118,.T.);
#50536=ORIENTED_EDGE('',*,*,#36117,.T.);
#50537=ORIENTED_EDGE('',*,*,#36119,.F.);
#50538=ORIENTED_EDGE('',*,*,#36120,.F.);
#50539=ORIENTED_EDGE('',*,*,#36121,.T.);
#50540=ORIENTED_EDGE('',*,*,#36120,.T.);
#50541=ORIENTED_EDGE('',*,*,#36122,.F.);
#50542=ORIENTED_EDGE('',*,*,#36123,.F.);
#50543=ORIENTED_EDGE('',*,*,#36124,.T.);
#50544=ORIENTED_EDGE('',*,*,#36123,.T.);
#50545=ORIENTED_EDGE('',*,*,#36125,.F.);
#50546=ORIENTED_EDGE('',*,*,#36126,.F.);
#50547=ORIENTED_EDGE('',*,*,#36127,.T.);
#50548=ORIENTED_EDGE('',*,*,#36126,.T.);
#50549=ORIENTED_EDGE('',*,*,#36128,.F.);
#50550=ORIENTED_EDGE('',*,*,#36129,.F.);
#50551=ORIENTED_EDGE('',*,*,#36130,.T.);
#50552=ORIENTED_EDGE('',*,*,#36129,.T.);
#50553=ORIENTED_EDGE('',*,*,#36131,.F.);
#50554=ORIENTED_EDGE('',*,*,#36132,.F.);
#50555=ORIENTED_EDGE('',*,*,#36133,.T.);
#50556=ORIENTED_EDGE('',*,*,#36132,.T.);
#50557=ORIENTED_EDGE('',*,*,#36134,.F.);
#50558=ORIENTED_EDGE('',*,*,#36135,.F.);
#50559=ORIENTED_EDGE('',*,*,#36136,.T.);
#50560=ORIENTED_EDGE('',*,*,#36135,.T.);
#50561=ORIENTED_EDGE('',*,*,#36137,.F.);
#50562=ORIENTED_EDGE('',*,*,#36138,.F.);
#50563=ORIENTED_EDGE('',*,*,#36139,.T.);
#50564=ORIENTED_EDGE('',*,*,#36138,.T.);
#50565=ORIENTED_EDGE('',*,*,#36140,.F.);
#50566=ORIENTED_EDGE('',*,*,#36141,.F.);
#50567=ORIENTED_EDGE('',*,*,#36142,.T.);
#50568=ORIENTED_EDGE('',*,*,#36141,.T.);
#50569=ORIENTED_EDGE('',*,*,#36143,.F.);
#50570=ORIENTED_EDGE('',*,*,#36144,.F.);
#50571=ORIENTED_EDGE('',*,*,#36145,.T.);
#50572=ORIENTED_EDGE('',*,*,#36144,.T.);
#50573=ORIENTED_EDGE('',*,*,#36146,.F.);
#50574=ORIENTED_EDGE('',*,*,#36147,.F.);
#50575=ORIENTED_EDGE('',*,*,#36148,.T.);
#50576=ORIENTED_EDGE('',*,*,#36147,.T.);
#50577=ORIENTED_EDGE('',*,*,#36149,.F.);
#50578=ORIENTED_EDGE('',*,*,#36150,.F.);
#50579=ORIENTED_EDGE('',*,*,#36151,.T.);
#50580=ORIENTED_EDGE('',*,*,#36150,.T.);
#50581=ORIENTED_EDGE('',*,*,#36152,.F.);
#50582=ORIENTED_EDGE('',*,*,#36153,.F.);
#50583=ORIENTED_EDGE('',*,*,#36154,.T.);
#50584=ORIENTED_EDGE('',*,*,#36153,.T.);
#50585=ORIENTED_EDGE('',*,*,#36155,.F.);
#50586=ORIENTED_EDGE('',*,*,#36156,.F.);
#50587=ORIENTED_EDGE('',*,*,#36157,.T.);
#50588=ORIENTED_EDGE('',*,*,#36156,.T.);
#50589=ORIENTED_EDGE('',*,*,#36158,.F.);
#50590=ORIENTED_EDGE('',*,*,#36159,.F.);
#50591=ORIENTED_EDGE('',*,*,#36160,.T.);
#50592=ORIENTED_EDGE('',*,*,#36159,.T.);
#50593=ORIENTED_EDGE('',*,*,#36161,.F.);
#50594=ORIENTED_EDGE('',*,*,#36162,.F.);
#50595=ORIENTED_EDGE('',*,*,#36163,.T.);
#50596=ORIENTED_EDGE('',*,*,#36162,.T.);
#50597=ORIENTED_EDGE('',*,*,#36164,.F.);
#50598=ORIENTED_EDGE('',*,*,#36165,.F.);
#50599=ORIENTED_EDGE('',*,*,#36166,.T.);
#50600=ORIENTED_EDGE('',*,*,#36165,.T.);
#50601=ORIENTED_EDGE('',*,*,#36167,.F.);
#50602=ORIENTED_EDGE('',*,*,#36168,.F.);
#50603=ORIENTED_EDGE('',*,*,#36169,.T.);
#50604=ORIENTED_EDGE('',*,*,#36168,.T.);
#50605=ORIENTED_EDGE('',*,*,#36170,.F.);
#50606=ORIENTED_EDGE('',*,*,#36171,.F.);
#50607=ORIENTED_EDGE('',*,*,#36172,.T.);
#50608=ORIENTED_EDGE('',*,*,#36171,.T.);
#50609=ORIENTED_EDGE('',*,*,#36173,.F.);
#50610=ORIENTED_EDGE('',*,*,#36174,.F.);
#50611=ORIENTED_EDGE('',*,*,#36175,.T.);
#50612=ORIENTED_EDGE('',*,*,#36174,.T.);
#50613=ORIENTED_EDGE('',*,*,#36176,.F.);
#50614=ORIENTED_EDGE('',*,*,#36177,.F.);
#50615=ORIENTED_EDGE('',*,*,#36178,.T.);
#50616=ORIENTED_EDGE('',*,*,#36177,.T.);
#50617=ORIENTED_EDGE('',*,*,#36179,.F.);
#50618=ORIENTED_EDGE('',*,*,#36180,.F.);
#50619=ORIENTED_EDGE('',*,*,#36181,.T.);
#50620=ORIENTED_EDGE('',*,*,#36180,.T.);
#50621=ORIENTED_EDGE('',*,*,#36182,.F.);
#50622=ORIENTED_EDGE('',*,*,#36183,.F.);
#50623=ORIENTED_EDGE('',*,*,#36184,.T.);
#50624=ORIENTED_EDGE('',*,*,#36183,.T.);
#50625=ORIENTED_EDGE('',*,*,#36185,.F.);
#50626=ORIENTED_EDGE('',*,*,#36186,.F.);
#50627=ORIENTED_EDGE('',*,*,#36187,.T.);
#50628=ORIENTED_EDGE('',*,*,#36186,.T.);
#50629=ORIENTED_EDGE('',*,*,#36188,.F.);
#50630=ORIENTED_EDGE('',*,*,#36189,.F.);
#50631=ORIENTED_EDGE('',*,*,#36190,.T.);
#50632=ORIENTED_EDGE('',*,*,#36189,.T.);
#50633=ORIENTED_EDGE('',*,*,#36191,.F.);
#50634=ORIENTED_EDGE('',*,*,#36192,.F.);
#50635=ORIENTED_EDGE('',*,*,#36193,.T.);
#50636=ORIENTED_EDGE('',*,*,#36192,.T.);
#50637=ORIENTED_EDGE('',*,*,#36194,.F.);
#50638=ORIENTED_EDGE('',*,*,#36195,.F.);
#50639=ORIENTED_EDGE('',*,*,#36196,.T.);
#50640=ORIENTED_EDGE('',*,*,#36195,.T.);
#50641=ORIENTED_EDGE('',*,*,#36197,.F.);
#50642=ORIENTED_EDGE('',*,*,#36198,.F.);
#50643=ORIENTED_EDGE('',*,*,#36199,.T.);
#50644=ORIENTED_EDGE('',*,*,#36198,.T.);
#50645=ORIENTED_EDGE('',*,*,#36200,.F.);
#50646=ORIENTED_EDGE('',*,*,#36201,.F.);
#50647=ORIENTED_EDGE('',*,*,#36202,.T.);
#50648=ORIENTED_EDGE('',*,*,#36201,.T.);
#50649=ORIENTED_EDGE('',*,*,#36203,.F.);
#50650=ORIENTED_EDGE('',*,*,#36204,.F.);
#50651=ORIENTED_EDGE('',*,*,#36205,.T.);
#50652=ORIENTED_EDGE('',*,*,#36204,.T.);
#50653=ORIENTED_EDGE('',*,*,#36206,.F.);
#50654=ORIENTED_EDGE('',*,*,#36207,.F.);
#50655=ORIENTED_EDGE('',*,*,#36208,.T.);
#50656=ORIENTED_EDGE('',*,*,#36207,.T.);
#50657=ORIENTED_EDGE('',*,*,#36209,.F.);
#50658=ORIENTED_EDGE('',*,*,#36210,.F.);
#50659=ORIENTED_EDGE('',*,*,#36211,.T.);
#50660=ORIENTED_EDGE('',*,*,#36210,.T.);
#50661=ORIENTED_EDGE('',*,*,#36212,.F.);
#50662=ORIENTED_EDGE('',*,*,#36213,.F.);
#50663=ORIENTED_EDGE('',*,*,#36214,.T.);
#50664=ORIENTED_EDGE('',*,*,#36213,.T.);
#50665=ORIENTED_EDGE('',*,*,#36215,.F.);
#50666=ORIENTED_EDGE('',*,*,#36216,.F.);
#50667=ORIENTED_EDGE('',*,*,#36217,.T.);
#50668=ORIENTED_EDGE('',*,*,#36216,.T.);
#50669=ORIENTED_EDGE('',*,*,#36218,.F.);
#50670=ORIENTED_EDGE('',*,*,#36219,.F.);
#50671=ORIENTED_EDGE('',*,*,#36220,.T.);
#50672=ORIENTED_EDGE('',*,*,#36219,.T.);
#50673=ORIENTED_EDGE('',*,*,#36221,.F.);
#50674=ORIENTED_EDGE('',*,*,#36222,.F.);
#50675=ORIENTED_EDGE('',*,*,#36223,.T.);
#50676=ORIENTED_EDGE('',*,*,#36222,.T.);
#50677=ORIENTED_EDGE('',*,*,#36224,.F.);
#50678=ORIENTED_EDGE('',*,*,#36225,.F.);
#50679=ORIENTED_EDGE('',*,*,#36226,.T.);
#50680=ORIENTED_EDGE('',*,*,#36225,.T.);
#50681=ORIENTED_EDGE('',*,*,#36227,.F.);
#50682=ORIENTED_EDGE('',*,*,#36228,.F.);
#50683=ORIENTED_EDGE('',*,*,#36229,.T.);
#50684=ORIENTED_EDGE('',*,*,#36228,.T.);
#50685=ORIENTED_EDGE('',*,*,#36230,.F.);
#50686=ORIENTED_EDGE('',*,*,#36231,.F.);
#50687=ORIENTED_EDGE('',*,*,#36232,.T.);
#50688=ORIENTED_EDGE('',*,*,#36231,.T.);
#50689=ORIENTED_EDGE('',*,*,#36233,.F.);
#50690=ORIENTED_EDGE('',*,*,#36234,.F.);
#50691=ORIENTED_EDGE('',*,*,#36235,.T.);
#50692=ORIENTED_EDGE('',*,*,#36234,.T.);
#50693=ORIENTED_EDGE('',*,*,#36236,.F.);
#50694=ORIENTED_EDGE('',*,*,#36237,.F.);
#50695=ORIENTED_EDGE('',*,*,#36238,.T.);
#50696=ORIENTED_EDGE('',*,*,#36237,.T.);
#50697=ORIENTED_EDGE('',*,*,#36239,.F.);
#50698=ORIENTED_EDGE('',*,*,#36240,.F.);
#50699=ORIENTED_EDGE('',*,*,#36241,.T.);
#50700=ORIENTED_EDGE('',*,*,#36240,.T.);
#50701=ORIENTED_EDGE('',*,*,#36242,.F.);
#50702=ORIENTED_EDGE('',*,*,#36243,.F.);
#50703=ORIENTED_EDGE('',*,*,#36244,.T.);
#50704=ORIENTED_EDGE('',*,*,#36243,.T.);
#50705=ORIENTED_EDGE('',*,*,#36245,.F.);
#50706=ORIENTED_EDGE('',*,*,#36246,.F.);
#50707=ORIENTED_EDGE('',*,*,#36247,.T.);
#50708=ORIENTED_EDGE('',*,*,#36246,.T.);
#50709=ORIENTED_EDGE('',*,*,#36248,.F.);
#50710=ORIENTED_EDGE('',*,*,#36249,.F.);
#50711=ORIENTED_EDGE('',*,*,#36250,.T.);
#50712=ORIENTED_EDGE('',*,*,#36249,.T.);
#50713=ORIENTED_EDGE('',*,*,#36251,.F.);
#50714=ORIENTED_EDGE('',*,*,#36252,.F.);
#50715=ORIENTED_EDGE('',*,*,#36253,.T.);
#50716=ORIENTED_EDGE('',*,*,#36252,.T.);
#50717=ORIENTED_EDGE('',*,*,#36254,.F.);
#50718=ORIENTED_EDGE('',*,*,#36255,.F.);
#50719=ORIENTED_EDGE('',*,*,#36256,.T.);
#50720=ORIENTED_EDGE('',*,*,#36255,.T.);
#50721=ORIENTED_EDGE('',*,*,#36257,.F.);
#50722=ORIENTED_EDGE('',*,*,#36258,.F.);
#50723=ORIENTED_EDGE('',*,*,#36259,.T.);
#50724=ORIENTED_EDGE('',*,*,#36258,.T.);
#50725=ORIENTED_EDGE('',*,*,#36260,.F.);
#50726=ORIENTED_EDGE('',*,*,#36261,.F.);
#50727=ORIENTED_EDGE('',*,*,#36262,.T.);
#50728=ORIENTED_EDGE('',*,*,#36261,.T.);
#50729=ORIENTED_EDGE('',*,*,#36263,.F.);
#50730=ORIENTED_EDGE('',*,*,#36264,.F.);
#50731=ORIENTED_EDGE('',*,*,#36265,.T.);
#50732=ORIENTED_EDGE('',*,*,#36264,.T.);
#50733=ORIENTED_EDGE('',*,*,#36266,.F.);
#50734=ORIENTED_EDGE('',*,*,#36267,.F.);
#50735=ORIENTED_EDGE('',*,*,#36268,.T.);
#50736=ORIENTED_EDGE('',*,*,#36267,.T.);
#50737=ORIENTED_EDGE('',*,*,#36269,.F.);
#50738=ORIENTED_EDGE('',*,*,#36270,.F.);
#50739=ORIENTED_EDGE('',*,*,#36271,.T.);
#50740=ORIENTED_EDGE('',*,*,#36270,.T.);
#50741=ORIENTED_EDGE('',*,*,#36272,.F.);
#50742=ORIENTED_EDGE('',*,*,#36273,.F.);
#50743=ORIENTED_EDGE('',*,*,#36274,.T.);
#50744=ORIENTED_EDGE('',*,*,#36273,.T.);
#50745=ORIENTED_EDGE('',*,*,#36275,.F.);
#50746=ORIENTED_EDGE('',*,*,#36276,.F.);
#50747=ORIENTED_EDGE('',*,*,#36277,.T.);
#50748=ORIENTED_EDGE('',*,*,#36276,.T.);
#50749=ORIENTED_EDGE('',*,*,#36278,.F.);
#50750=ORIENTED_EDGE('',*,*,#36279,.F.);
#50751=ORIENTED_EDGE('',*,*,#36280,.T.);
#50752=ORIENTED_EDGE('',*,*,#36279,.T.);
#50753=ORIENTED_EDGE('',*,*,#36281,.F.);
#50754=ORIENTED_EDGE('',*,*,#36282,.F.);
#50755=ORIENTED_EDGE('',*,*,#36283,.T.);
#50756=ORIENTED_EDGE('',*,*,#36282,.T.);
#50757=ORIENTED_EDGE('',*,*,#36284,.F.);
#50758=ORIENTED_EDGE('',*,*,#36285,.F.);
#50759=ORIENTED_EDGE('',*,*,#36286,.T.);
#50760=ORIENTED_EDGE('',*,*,#36285,.T.);
#50761=ORIENTED_EDGE('',*,*,#36287,.F.);
#50762=ORIENTED_EDGE('',*,*,#36288,.F.);
#50763=ORIENTED_EDGE('',*,*,#36289,.T.);
#50764=ORIENTED_EDGE('',*,*,#36288,.T.);
#50765=ORIENTED_EDGE('',*,*,#36290,.F.);
#50766=ORIENTED_EDGE('',*,*,#36291,.F.);
#50767=ORIENTED_EDGE('',*,*,#36292,.T.);
#50768=ORIENTED_EDGE('',*,*,#36291,.T.);
#50769=ORIENTED_EDGE('',*,*,#36293,.F.);
#50770=ORIENTED_EDGE('',*,*,#36294,.F.);
#50771=ORIENTED_EDGE('',*,*,#36295,.T.);
#50772=ORIENTED_EDGE('',*,*,#36294,.T.);
#50773=ORIENTED_EDGE('',*,*,#36296,.F.);
#50774=ORIENTED_EDGE('',*,*,#36297,.F.);
#50775=ORIENTED_EDGE('',*,*,#36298,.T.);
#50776=ORIENTED_EDGE('',*,*,#36297,.T.);
#50777=ORIENTED_EDGE('',*,*,#36299,.F.);
#50778=ORIENTED_EDGE('',*,*,#36300,.F.);
#50779=ORIENTED_EDGE('',*,*,#36301,.T.);
#50780=ORIENTED_EDGE('',*,*,#36300,.T.);
#50781=ORIENTED_EDGE('',*,*,#36302,.F.);
#50782=ORIENTED_EDGE('',*,*,#36303,.F.);
#50783=ORIENTED_EDGE('',*,*,#36304,.T.);
#50784=ORIENTED_EDGE('',*,*,#36303,.T.);
#50785=ORIENTED_EDGE('',*,*,#36305,.F.);
#50786=ORIENTED_EDGE('',*,*,#36306,.F.);
#50787=ORIENTED_EDGE('',*,*,#36307,.T.);
#50788=ORIENTED_EDGE('',*,*,#36306,.T.);
#50789=ORIENTED_EDGE('',*,*,#36308,.F.);
#50790=ORIENTED_EDGE('',*,*,#36309,.F.);
#50791=ORIENTED_EDGE('',*,*,#36310,.T.);
#50792=ORIENTED_EDGE('',*,*,#36309,.T.);
#50793=ORIENTED_EDGE('',*,*,#36311,.F.);
#50794=ORIENTED_EDGE('',*,*,#36312,.F.);
#50795=ORIENTED_EDGE('',*,*,#36313,.T.);
#50796=ORIENTED_EDGE('',*,*,#36312,.T.);
#50797=ORIENTED_EDGE('',*,*,#36314,.F.);
#50798=ORIENTED_EDGE('',*,*,#36315,.F.);
#50799=ORIENTED_EDGE('',*,*,#36316,.T.);
#50800=ORIENTED_EDGE('',*,*,#36315,.T.);
#50801=ORIENTED_EDGE('',*,*,#36317,.F.);
#50802=ORIENTED_EDGE('',*,*,#36318,.F.);
#50803=ORIENTED_EDGE('',*,*,#36319,.T.);
#50804=ORIENTED_EDGE('',*,*,#36318,.T.);
#50805=ORIENTED_EDGE('',*,*,#36320,.F.);
#50806=ORIENTED_EDGE('',*,*,#36321,.F.);
#50807=ORIENTED_EDGE('',*,*,#36322,.T.);
#50808=ORIENTED_EDGE('',*,*,#36321,.T.);
#50809=ORIENTED_EDGE('',*,*,#36323,.F.);
#50810=ORIENTED_EDGE('',*,*,#36324,.F.);
#50811=ORIENTED_EDGE('',*,*,#36325,.T.);
#50812=ORIENTED_EDGE('',*,*,#36324,.T.);
#50813=ORIENTED_EDGE('',*,*,#36326,.F.);
#50814=ORIENTED_EDGE('',*,*,#36327,.F.);
#50815=ORIENTED_EDGE('',*,*,#36328,.T.);
#50816=ORIENTED_EDGE('',*,*,#36327,.T.);
#50817=ORIENTED_EDGE('',*,*,#36329,.F.);
#50818=ORIENTED_EDGE('',*,*,#36330,.F.);
#50819=ORIENTED_EDGE('',*,*,#36331,.T.);
#50820=ORIENTED_EDGE('',*,*,#36330,.T.);
#50821=ORIENTED_EDGE('',*,*,#36332,.F.);
#50822=ORIENTED_EDGE('',*,*,#36333,.F.);
#50823=ORIENTED_EDGE('',*,*,#36334,.T.);
#50824=ORIENTED_EDGE('',*,*,#36333,.T.);
#50825=ORIENTED_EDGE('',*,*,#36335,.F.);
#50826=ORIENTED_EDGE('',*,*,#36336,.F.);
#50827=ORIENTED_EDGE('',*,*,#36337,.T.);
#50828=ORIENTED_EDGE('',*,*,#36336,.T.);
#50829=ORIENTED_EDGE('',*,*,#36338,.F.);
#50830=ORIENTED_EDGE('',*,*,#36339,.F.);
#50831=ORIENTED_EDGE('',*,*,#36340,.T.);
#50832=ORIENTED_EDGE('',*,*,#36339,.T.);
#50833=ORIENTED_EDGE('',*,*,#36341,.F.);
#50834=ORIENTED_EDGE('',*,*,#36342,.F.);
#50835=ORIENTED_EDGE('',*,*,#36343,.T.);
#50836=ORIENTED_EDGE('',*,*,#36342,.T.);
#50837=ORIENTED_EDGE('',*,*,#36344,.F.);
#50838=ORIENTED_EDGE('',*,*,#36345,.F.);
#50839=ORIENTED_EDGE('',*,*,#36346,.T.);
#50840=ORIENTED_EDGE('',*,*,#36345,.T.);
#50841=ORIENTED_EDGE('',*,*,#36347,.F.);
#50842=ORIENTED_EDGE('',*,*,#36348,.F.);
#50843=ORIENTED_EDGE('',*,*,#36349,.T.);
#50844=ORIENTED_EDGE('',*,*,#36348,.T.);
#50845=ORIENTED_EDGE('',*,*,#36350,.F.);
#50846=ORIENTED_EDGE('',*,*,#36351,.F.);
#50847=ORIENTED_EDGE('',*,*,#36352,.T.);
#50848=ORIENTED_EDGE('',*,*,#36351,.T.);
#50849=ORIENTED_EDGE('',*,*,#36353,.F.);
#50850=ORIENTED_EDGE('',*,*,#36354,.F.);
#50851=ORIENTED_EDGE('',*,*,#36355,.T.);
#50852=ORIENTED_EDGE('',*,*,#36354,.T.);
#50853=ORIENTED_EDGE('',*,*,#36356,.F.);
#50854=ORIENTED_EDGE('',*,*,#36357,.F.);
#50855=ORIENTED_EDGE('',*,*,#36358,.T.);
#50856=ORIENTED_EDGE('',*,*,#36357,.T.);
#50857=ORIENTED_EDGE('',*,*,#36359,.F.);
#50858=ORIENTED_EDGE('',*,*,#36360,.F.);
#50859=ORIENTED_EDGE('',*,*,#36361,.T.);
#50860=ORIENTED_EDGE('',*,*,#36360,.T.);
#50861=ORIENTED_EDGE('',*,*,#36362,.F.);
#50862=ORIENTED_EDGE('',*,*,#36363,.F.);
#50863=ORIENTED_EDGE('',*,*,#36364,.T.);
#50864=ORIENTED_EDGE('',*,*,#36363,.T.);
#50865=ORIENTED_EDGE('',*,*,#36365,.F.);
#50866=ORIENTED_EDGE('',*,*,#36366,.F.);
#50867=ORIENTED_EDGE('',*,*,#36367,.T.);
#50868=ORIENTED_EDGE('',*,*,#36366,.T.);
#50869=ORIENTED_EDGE('',*,*,#36368,.F.);
#50870=ORIENTED_EDGE('',*,*,#36369,.F.);
#50871=ORIENTED_EDGE('',*,*,#36370,.T.);
#50872=ORIENTED_EDGE('',*,*,#36369,.T.);
#50873=ORIENTED_EDGE('',*,*,#36371,.F.);
#50874=ORIENTED_EDGE('',*,*,#36372,.F.);
#50875=ORIENTED_EDGE('',*,*,#36373,.T.);
#50876=ORIENTED_EDGE('',*,*,#36372,.T.);
#50877=ORIENTED_EDGE('',*,*,#36374,.F.);
#50878=ORIENTED_EDGE('',*,*,#36375,.F.);
#50879=ORIENTED_EDGE('',*,*,#36376,.T.);
#50880=ORIENTED_EDGE('',*,*,#36375,.T.);
#50881=ORIENTED_EDGE('',*,*,#36377,.F.);
#50882=ORIENTED_EDGE('',*,*,#36378,.F.);
#50883=ORIENTED_EDGE('',*,*,#36379,.T.);
#50884=ORIENTED_EDGE('',*,*,#36378,.T.);
#50885=ORIENTED_EDGE('',*,*,#36380,.F.);
#50886=ORIENTED_EDGE('',*,*,#36381,.F.);
#50887=ORIENTED_EDGE('',*,*,#36382,.T.);
#50888=ORIENTED_EDGE('',*,*,#36381,.T.);
#50889=ORIENTED_EDGE('',*,*,#36383,.F.);
#50890=ORIENTED_EDGE('',*,*,#36384,.F.);
#50891=ORIENTED_EDGE('',*,*,#36385,.T.);
#50892=ORIENTED_EDGE('',*,*,#36384,.T.);
#50893=ORIENTED_EDGE('',*,*,#36386,.F.);
#50894=ORIENTED_EDGE('',*,*,#36387,.F.);
#50895=ORIENTED_EDGE('',*,*,#36388,.T.);
#50896=ORIENTED_EDGE('',*,*,#36387,.T.);
#50897=ORIENTED_EDGE('',*,*,#36389,.F.);
#50898=ORIENTED_EDGE('',*,*,#36390,.F.);
#50899=ORIENTED_EDGE('',*,*,#36391,.T.);
#50900=ORIENTED_EDGE('',*,*,#36390,.T.);
#50901=ORIENTED_EDGE('',*,*,#36392,.F.);
#50902=ORIENTED_EDGE('',*,*,#36393,.F.);
#50903=ORIENTED_EDGE('',*,*,#36394,.T.);
#50904=ORIENTED_EDGE('',*,*,#36393,.T.);
#50905=ORIENTED_EDGE('',*,*,#36395,.F.);
#50906=ORIENTED_EDGE('',*,*,#36396,.F.);
#50907=ORIENTED_EDGE('',*,*,#36397,.T.);
#50908=ORIENTED_EDGE('',*,*,#36396,.T.);
#50909=ORIENTED_EDGE('',*,*,#36398,.F.);
#50910=ORIENTED_EDGE('',*,*,#36399,.F.);
#50911=ORIENTED_EDGE('',*,*,#36400,.T.);
#50912=ORIENTED_EDGE('',*,*,#36399,.T.);
#50913=ORIENTED_EDGE('',*,*,#36401,.F.);
#50914=ORIENTED_EDGE('',*,*,#36402,.F.);
#50915=ORIENTED_EDGE('',*,*,#36403,.T.);
#50916=ORIENTED_EDGE('',*,*,#36402,.T.);
#50917=ORIENTED_EDGE('',*,*,#36404,.F.);
#50918=ORIENTED_EDGE('',*,*,#36405,.F.);
#50919=ORIENTED_EDGE('',*,*,#36406,.T.);
#50920=ORIENTED_EDGE('',*,*,#36405,.T.);
#50921=ORIENTED_EDGE('',*,*,#36407,.F.);
#50922=ORIENTED_EDGE('',*,*,#36408,.F.);
#50923=ORIENTED_EDGE('',*,*,#36409,.T.);
#50924=ORIENTED_EDGE('',*,*,#36408,.T.);
#50925=ORIENTED_EDGE('',*,*,#36410,.F.);
#50926=ORIENTED_EDGE('',*,*,#36411,.F.);
#50927=ORIENTED_EDGE('',*,*,#36412,.T.);
#50928=ORIENTED_EDGE('',*,*,#36411,.T.);
#50929=ORIENTED_EDGE('',*,*,#36413,.F.);
#50930=ORIENTED_EDGE('',*,*,#36414,.F.);
#50931=ORIENTED_EDGE('',*,*,#36415,.T.);
#50932=ORIENTED_EDGE('',*,*,#36414,.T.);
#50933=ORIENTED_EDGE('',*,*,#36416,.F.);
#50934=ORIENTED_EDGE('',*,*,#36417,.F.);
#50935=ORIENTED_EDGE('',*,*,#36418,.T.);
#50936=ORIENTED_EDGE('',*,*,#36417,.T.);
#50937=ORIENTED_EDGE('',*,*,#36419,.F.);
#50938=ORIENTED_EDGE('',*,*,#36420,.F.);
#50939=ORIENTED_EDGE('',*,*,#36421,.T.);
#50940=ORIENTED_EDGE('',*,*,#36420,.T.);
#50941=ORIENTED_EDGE('',*,*,#36422,.F.);
#50942=ORIENTED_EDGE('',*,*,#36423,.F.);
#50943=ORIENTED_EDGE('',*,*,#36424,.T.);
#50944=ORIENTED_EDGE('',*,*,#36423,.T.);
#50945=ORIENTED_EDGE('',*,*,#36425,.F.);
#50946=ORIENTED_EDGE('',*,*,#36426,.F.);
#50947=ORIENTED_EDGE('',*,*,#36427,.T.);
#50948=ORIENTED_EDGE('',*,*,#36426,.T.);
#50949=ORIENTED_EDGE('',*,*,#36428,.F.);
#50950=ORIENTED_EDGE('',*,*,#36429,.F.);
#50951=ORIENTED_EDGE('',*,*,#36430,.T.);
#50952=ORIENTED_EDGE('',*,*,#36429,.T.);
#50953=ORIENTED_EDGE('',*,*,#36431,.F.);
#50954=ORIENTED_EDGE('',*,*,#36432,.F.);
#50955=ORIENTED_EDGE('',*,*,#36433,.T.);
#50956=ORIENTED_EDGE('',*,*,#36432,.T.);
#50957=ORIENTED_EDGE('',*,*,#36434,.F.);
#50958=ORIENTED_EDGE('',*,*,#36435,.F.);
#50959=ORIENTED_EDGE('',*,*,#36436,.T.);
#50960=ORIENTED_EDGE('',*,*,#36435,.T.);
#50961=ORIENTED_EDGE('',*,*,#36437,.F.);
#50962=ORIENTED_EDGE('',*,*,#36438,.F.);
#50963=ORIENTED_EDGE('',*,*,#36439,.T.);
#50964=ORIENTED_EDGE('',*,*,#36438,.T.);
#50965=ORIENTED_EDGE('',*,*,#36440,.F.);
#50966=ORIENTED_EDGE('',*,*,#36441,.F.);
#50967=ORIENTED_EDGE('',*,*,#36442,.T.);
#50968=ORIENTED_EDGE('',*,*,#36441,.T.);
#50969=ORIENTED_EDGE('',*,*,#36443,.F.);
#50970=ORIENTED_EDGE('',*,*,#36444,.F.);
#50971=ORIENTED_EDGE('',*,*,#36445,.T.);
#50972=ORIENTED_EDGE('',*,*,#36444,.T.);
#50973=ORIENTED_EDGE('',*,*,#36446,.F.);
#50974=ORIENTED_EDGE('',*,*,#36447,.F.);
#50975=ORIENTED_EDGE('',*,*,#36448,.T.);
#50976=ORIENTED_EDGE('',*,*,#36447,.T.);
#50977=ORIENTED_EDGE('',*,*,#36449,.F.);
#50978=ORIENTED_EDGE('',*,*,#36450,.F.);
#50979=ORIENTED_EDGE('',*,*,#36451,.T.);
#50980=ORIENTED_EDGE('',*,*,#36450,.T.);
#50981=ORIENTED_EDGE('',*,*,#36452,.F.);
#50982=ORIENTED_EDGE('',*,*,#36453,.F.);
#50983=ORIENTED_EDGE('',*,*,#36454,.T.);
#50984=ORIENTED_EDGE('',*,*,#36453,.T.);
#50985=ORIENTED_EDGE('',*,*,#36455,.F.);
#50986=ORIENTED_EDGE('',*,*,#36456,.F.);
#50987=ORIENTED_EDGE('',*,*,#36457,.T.);
#50988=ORIENTED_EDGE('',*,*,#36456,.T.);
#50989=ORIENTED_EDGE('',*,*,#36458,.F.);
#50990=ORIENTED_EDGE('',*,*,#36459,.F.);
#50991=ORIENTED_EDGE('',*,*,#36460,.T.);
#50992=ORIENTED_EDGE('',*,*,#36459,.T.);
#50993=ORIENTED_EDGE('',*,*,#36461,.F.);
#50994=ORIENTED_EDGE('',*,*,#36462,.F.);
#50995=ORIENTED_EDGE('',*,*,#36463,.T.);
#50996=ORIENTED_EDGE('',*,*,#36462,.T.);
#50997=ORIENTED_EDGE('',*,*,#36464,.F.);
#50998=ORIENTED_EDGE('',*,*,#36465,.F.);
#50999=ORIENTED_EDGE('',*,*,#36466,.T.);
#51000=ORIENTED_EDGE('',*,*,#36465,.T.);
#51001=ORIENTED_EDGE('',*,*,#36467,.F.);
#51002=ORIENTED_EDGE('',*,*,#36468,.F.);
#51003=ORIENTED_EDGE('',*,*,#36469,.T.);
#51004=ORIENTED_EDGE('',*,*,#36468,.T.);
#51005=ORIENTED_EDGE('',*,*,#36470,.F.);
#51006=ORIENTED_EDGE('',*,*,#36471,.F.);
#51007=ORIENTED_EDGE('',*,*,#36472,.T.);
#51008=ORIENTED_EDGE('',*,*,#36471,.T.);
#51009=ORIENTED_EDGE('',*,*,#36473,.F.);
#51010=ORIENTED_EDGE('',*,*,#36474,.F.);
#51011=ORIENTED_EDGE('',*,*,#36475,.T.);
#51012=ORIENTED_EDGE('',*,*,#36474,.T.);
#51013=ORIENTED_EDGE('',*,*,#36476,.F.);
#51014=ORIENTED_EDGE('',*,*,#36477,.F.);
#51015=ORIENTED_EDGE('',*,*,#36478,.T.);
#51016=ORIENTED_EDGE('',*,*,#36477,.T.);
#51017=ORIENTED_EDGE('',*,*,#36479,.F.);
#51018=ORIENTED_EDGE('',*,*,#36480,.F.);
#51019=ORIENTED_EDGE('',*,*,#36481,.T.);
#51020=ORIENTED_EDGE('',*,*,#36480,.T.);
#51021=ORIENTED_EDGE('',*,*,#36482,.F.);
#51022=ORIENTED_EDGE('',*,*,#36483,.F.);
#51023=ORIENTED_EDGE('',*,*,#36484,.T.);
#51024=ORIENTED_EDGE('',*,*,#36483,.T.);
#51025=ORIENTED_EDGE('',*,*,#36485,.F.);
#51026=ORIENTED_EDGE('',*,*,#36486,.F.);
#51027=ORIENTED_EDGE('',*,*,#36487,.T.);
#51028=ORIENTED_EDGE('',*,*,#36486,.T.);
#51029=ORIENTED_EDGE('',*,*,#36488,.F.);
#51030=ORIENTED_EDGE('',*,*,#36489,.F.);
#51031=ORIENTED_EDGE('',*,*,#36490,.T.);
#51032=ORIENTED_EDGE('',*,*,#36489,.T.);
#51033=ORIENTED_EDGE('',*,*,#36491,.F.);
#51034=ORIENTED_EDGE('',*,*,#36492,.F.);
#51035=ORIENTED_EDGE('',*,*,#36493,.T.);
#51036=ORIENTED_EDGE('',*,*,#36492,.T.);
#51037=ORIENTED_EDGE('',*,*,#36494,.F.);
#51038=ORIENTED_EDGE('',*,*,#36495,.F.);
#51039=ORIENTED_EDGE('',*,*,#36496,.T.);
#51040=ORIENTED_EDGE('',*,*,#36495,.T.);
#51041=ORIENTED_EDGE('',*,*,#36497,.F.);
#51042=ORIENTED_EDGE('',*,*,#36498,.F.);
#51043=ORIENTED_EDGE('',*,*,#36499,.T.);
#51044=ORIENTED_EDGE('',*,*,#36498,.T.);
#51045=ORIENTED_EDGE('',*,*,#36500,.F.);
#51046=ORIENTED_EDGE('',*,*,#36501,.F.);
#51047=ORIENTED_EDGE('',*,*,#36502,.T.);
#51048=ORIENTED_EDGE('',*,*,#36501,.T.);
#51049=ORIENTED_EDGE('',*,*,#36503,.F.);
#51050=ORIENTED_EDGE('',*,*,#36504,.F.);
#51051=ORIENTED_EDGE('',*,*,#36505,.T.);
#51052=ORIENTED_EDGE('',*,*,#36504,.T.);
#51053=ORIENTED_EDGE('',*,*,#36506,.F.);
#51054=ORIENTED_EDGE('',*,*,#36507,.F.);
#51055=ORIENTED_EDGE('',*,*,#36508,.T.);
#51056=ORIENTED_EDGE('',*,*,#36507,.T.);
#51057=ORIENTED_EDGE('',*,*,#36509,.F.);
#51058=ORIENTED_EDGE('',*,*,#36510,.F.);
#51059=ORIENTED_EDGE('',*,*,#36511,.T.);
#51060=ORIENTED_EDGE('',*,*,#36510,.T.);
#51061=ORIENTED_EDGE('',*,*,#36512,.F.);
#51062=ORIENTED_EDGE('',*,*,#36513,.F.);
#51063=ORIENTED_EDGE('',*,*,#36514,.T.);
#51064=ORIENTED_EDGE('',*,*,#36513,.T.);
#51065=ORIENTED_EDGE('',*,*,#36515,.F.);
#51066=ORIENTED_EDGE('',*,*,#36516,.F.);
#51067=ORIENTED_EDGE('',*,*,#36517,.T.);
#51068=ORIENTED_EDGE('',*,*,#36516,.T.);
#51069=ORIENTED_EDGE('',*,*,#36518,.F.);
#51070=ORIENTED_EDGE('',*,*,#36519,.F.);
#51071=ORIENTED_EDGE('',*,*,#36520,.T.);
#51072=ORIENTED_EDGE('',*,*,#36519,.T.);
#51073=ORIENTED_EDGE('',*,*,#36521,.F.);
#51074=ORIENTED_EDGE('',*,*,#36522,.F.);
#51075=ORIENTED_EDGE('',*,*,#36523,.T.);
#51076=ORIENTED_EDGE('',*,*,#36522,.T.);
#51077=ORIENTED_EDGE('',*,*,#36524,.F.);
#51078=ORIENTED_EDGE('',*,*,#36525,.F.);
#51079=ORIENTED_EDGE('',*,*,#36526,.T.);
#51080=ORIENTED_EDGE('',*,*,#36525,.T.);
#51081=ORIENTED_EDGE('',*,*,#36527,.F.);
#51082=ORIENTED_EDGE('',*,*,#36528,.F.);
#51083=ORIENTED_EDGE('',*,*,#36529,.T.);
#51084=ORIENTED_EDGE('',*,*,#36528,.T.);
#51085=ORIENTED_EDGE('',*,*,#36530,.F.);
#51086=ORIENTED_EDGE('',*,*,#36531,.F.);
#51087=ORIENTED_EDGE('',*,*,#36532,.T.);
#51088=ORIENTED_EDGE('',*,*,#36531,.T.);
#51089=ORIENTED_EDGE('',*,*,#36533,.F.);
#51090=ORIENTED_EDGE('',*,*,#36534,.F.);
#51091=ORIENTED_EDGE('',*,*,#36535,.T.);
#51092=ORIENTED_EDGE('',*,*,#36534,.T.);
#51093=ORIENTED_EDGE('',*,*,#36536,.F.);
#51094=ORIENTED_EDGE('',*,*,#36537,.F.);
#51095=ORIENTED_EDGE('',*,*,#36538,.T.);
#51096=ORIENTED_EDGE('',*,*,#36537,.T.);
#51097=ORIENTED_EDGE('',*,*,#36539,.F.);
#51098=ORIENTED_EDGE('',*,*,#36540,.F.);
#51099=ORIENTED_EDGE('',*,*,#36541,.T.);
#51100=ORIENTED_EDGE('',*,*,#36540,.T.);
#51101=ORIENTED_EDGE('',*,*,#36542,.F.);
#51102=ORIENTED_EDGE('',*,*,#36543,.F.);
#51103=ORIENTED_EDGE('',*,*,#36544,.T.);
#51104=ORIENTED_EDGE('',*,*,#36543,.T.);
#51105=ORIENTED_EDGE('',*,*,#36545,.F.);
#51106=ORIENTED_EDGE('',*,*,#36546,.F.);
#51107=ORIENTED_EDGE('',*,*,#36547,.T.);
#51108=ORIENTED_EDGE('',*,*,#36546,.T.);
#51109=ORIENTED_EDGE('',*,*,#36548,.F.);
#51110=ORIENTED_EDGE('',*,*,#36549,.F.);
#51111=ORIENTED_EDGE('',*,*,#36550,.T.);
#51112=ORIENTED_EDGE('',*,*,#36549,.T.);
#51113=ORIENTED_EDGE('',*,*,#36551,.F.);
#51114=ORIENTED_EDGE('',*,*,#36552,.F.);
#51115=ORIENTED_EDGE('',*,*,#36553,.T.);
#51116=ORIENTED_EDGE('',*,*,#36552,.T.);
#51117=ORIENTED_EDGE('',*,*,#36554,.F.);
#51118=ORIENTED_EDGE('',*,*,#36555,.F.);
#51119=ORIENTED_EDGE('',*,*,#36556,.T.);
#51120=ORIENTED_EDGE('',*,*,#36555,.T.);
#51121=ORIENTED_EDGE('',*,*,#36557,.F.);
#51122=ORIENTED_EDGE('',*,*,#36558,.F.);
#51123=ORIENTED_EDGE('',*,*,#36559,.T.);
#51124=ORIENTED_EDGE('',*,*,#36558,.T.);
#51125=ORIENTED_EDGE('',*,*,#36560,.F.);
#51126=ORIENTED_EDGE('',*,*,#36561,.F.);
#51127=ORIENTED_EDGE('',*,*,#36562,.T.);
#51128=ORIENTED_EDGE('',*,*,#36561,.T.);
#51129=ORIENTED_EDGE('',*,*,#36563,.F.);
#51130=ORIENTED_EDGE('',*,*,#36564,.F.);
#51131=ORIENTED_EDGE('',*,*,#36565,.T.);
#51132=ORIENTED_EDGE('',*,*,#36564,.T.);
#51133=ORIENTED_EDGE('',*,*,#36566,.F.);
#51134=ORIENTED_EDGE('',*,*,#36567,.F.);
#51135=ORIENTED_EDGE('',*,*,#36568,.T.);
#51136=ORIENTED_EDGE('',*,*,#36567,.T.);
#51137=ORIENTED_EDGE('',*,*,#36569,.F.);
#51138=ORIENTED_EDGE('',*,*,#36570,.F.);
#51139=ORIENTED_EDGE('',*,*,#36571,.T.);
#51140=ORIENTED_EDGE('',*,*,#36570,.T.);
#51141=ORIENTED_EDGE('',*,*,#36572,.F.);
#51142=ORIENTED_EDGE('',*,*,#36573,.F.);
#51143=ORIENTED_EDGE('',*,*,#36574,.T.);
#51144=ORIENTED_EDGE('',*,*,#36573,.T.);
#51145=ORIENTED_EDGE('',*,*,#36575,.F.);
#51146=ORIENTED_EDGE('',*,*,#36576,.F.);
#51147=ORIENTED_EDGE('',*,*,#36577,.T.);
#51148=ORIENTED_EDGE('',*,*,#36576,.T.);
#51149=ORIENTED_EDGE('',*,*,#36578,.F.);
#51150=ORIENTED_EDGE('',*,*,#36579,.F.);
#51151=ORIENTED_EDGE('',*,*,#36580,.T.);
#51152=ORIENTED_EDGE('',*,*,#36579,.T.);
#51153=ORIENTED_EDGE('',*,*,#36581,.F.);
#51154=ORIENTED_EDGE('',*,*,#36582,.F.);
#51155=ORIENTED_EDGE('',*,*,#36583,.T.);
#51156=ORIENTED_EDGE('',*,*,#36582,.T.);
#51157=ORIENTED_EDGE('',*,*,#36584,.F.);
#51158=ORIENTED_EDGE('',*,*,#36585,.F.);
#51159=ORIENTED_EDGE('',*,*,#36586,.T.);
#51160=ORIENTED_EDGE('',*,*,#36585,.T.);
#51161=ORIENTED_EDGE('',*,*,#36587,.F.);
#51162=ORIENTED_EDGE('',*,*,#36588,.F.);
#51163=ORIENTED_EDGE('',*,*,#36589,.T.);
#51164=ORIENTED_EDGE('',*,*,#36588,.T.);
#51165=ORIENTED_EDGE('',*,*,#36590,.F.);
#51166=ORIENTED_EDGE('',*,*,#36591,.F.);
#51167=ORIENTED_EDGE('',*,*,#36592,.T.);
#51168=ORIENTED_EDGE('',*,*,#36591,.T.);
#51169=ORIENTED_EDGE('',*,*,#36593,.F.);
#51170=ORIENTED_EDGE('',*,*,#36594,.F.);
#51171=ORIENTED_EDGE('',*,*,#36595,.T.);
#51172=ORIENTED_EDGE('',*,*,#36594,.T.);
#51173=ORIENTED_EDGE('',*,*,#36596,.F.);
#51174=ORIENTED_EDGE('',*,*,#36597,.F.);
#51175=ORIENTED_EDGE('',*,*,#36598,.T.);
#51176=ORIENTED_EDGE('',*,*,#36597,.T.);
#51177=ORIENTED_EDGE('',*,*,#36599,.F.);
#51178=ORIENTED_EDGE('',*,*,#36600,.F.);
#51179=ORIENTED_EDGE('',*,*,#36601,.T.);
#51180=ORIENTED_EDGE('',*,*,#36600,.T.);
#51181=ORIENTED_EDGE('',*,*,#36602,.F.);
#51182=ORIENTED_EDGE('',*,*,#36603,.F.);
#51183=ORIENTED_EDGE('',*,*,#36604,.T.);
#51184=ORIENTED_EDGE('',*,*,#36603,.T.);
#51185=ORIENTED_EDGE('',*,*,#36605,.F.);
#51186=ORIENTED_EDGE('',*,*,#36606,.F.);
#51187=ORIENTED_EDGE('',*,*,#36607,.T.);
#51188=ORIENTED_EDGE('',*,*,#36606,.T.);
#51189=ORIENTED_EDGE('',*,*,#36608,.F.);
#51190=ORIENTED_EDGE('',*,*,#36609,.F.);
#51191=ORIENTED_EDGE('',*,*,#36610,.T.);
#51192=ORIENTED_EDGE('',*,*,#36609,.T.);
#51193=ORIENTED_EDGE('',*,*,#36611,.F.);
#51194=ORIENTED_EDGE('',*,*,#36612,.F.);
#51195=ORIENTED_EDGE('',*,*,#36613,.T.);
#51196=ORIENTED_EDGE('',*,*,#36612,.T.);
#51197=ORIENTED_EDGE('',*,*,#36614,.F.);
#51198=ORIENTED_EDGE('',*,*,#36615,.F.);
#51199=ORIENTED_EDGE('',*,*,#36616,.T.);
#51200=ORIENTED_EDGE('',*,*,#36615,.T.);
#51201=ORIENTED_EDGE('',*,*,#36617,.F.);
#51202=ORIENTED_EDGE('',*,*,#36618,.F.);
#51203=ORIENTED_EDGE('',*,*,#36619,.T.);
#51204=ORIENTED_EDGE('',*,*,#36618,.T.);
#51205=ORIENTED_EDGE('',*,*,#36620,.F.);
#51206=ORIENTED_EDGE('',*,*,#36621,.F.);
#51207=ORIENTED_EDGE('',*,*,#36622,.T.);
#51208=ORIENTED_EDGE('',*,*,#36621,.T.);
#51209=ORIENTED_EDGE('',*,*,#36623,.F.);
#51210=ORIENTED_EDGE('',*,*,#36624,.F.);
#51211=ORIENTED_EDGE('',*,*,#36625,.T.);
#51212=ORIENTED_EDGE('',*,*,#36624,.T.);
#51213=ORIENTED_EDGE('',*,*,#36626,.F.);
#51214=ORIENTED_EDGE('',*,*,#36627,.F.);
#51215=ORIENTED_EDGE('',*,*,#36628,.T.);
#51216=ORIENTED_EDGE('',*,*,#36627,.T.);
#51217=ORIENTED_EDGE('',*,*,#36629,.F.);
#51218=ORIENTED_EDGE('',*,*,#36630,.F.);
#51219=ORIENTED_EDGE('',*,*,#36631,.T.);
#51220=ORIENTED_EDGE('',*,*,#36630,.T.);
#51221=ORIENTED_EDGE('',*,*,#36632,.F.);
#51222=ORIENTED_EDGE('',*,*,#36633,.F.);
#51223=ORIENTED_EDGE('',*,*,#36634,.T.);
#51224=ORIENTED_EDGE('',*,*,#36633,.T.);
#51225=ORIENTED_EDGE('',*,*,#36635,.F.);
#51226=ORIENTED_EDGE('',*,*,#36636,.F.);
#51227=ORIENTED_EDGE('',*,*,#36637,.T.);
#51228=ORIENTED_EDGE('',*,*,#36636,.T.);
#51229=ORIENTED_EDGE('',*,*,#36638,.F.);
#51230=ORIENTED_EDGE('',*,*,#36639,.F.);
#51231=ORIENTED_EDGE('',*,*,#36640,.T.);
#51232=ORIENTED_EDGE('',*,*,#36639,.T.);
#51233=ORIENTED_EDGE('',*,*,#36641,.F.);
#51234=ORIENTED_EDGE('',*,*,#36642,.F.);
#51235=ORIENTED_EDGE('',*,*,#36643,.T.);
#51236=ORIENTED_EDGE('',*,*,#36642,.T.);
#51237=ORIENTED_EDGE('',*,*,#36644,.F.);
#51238=ORIENTED_EDGE('',*,*,#36645,.F.);
#51239=ORIENTED_EDGE('',*,*,#36646,.T.);
#51240=ORIENTED_EDGE('',*,*,#36645,.T.);
#51241=ORIENTED_EDGE('',*,*,#36647,.F.);
#51242=ORIENTED_EDGE('',*,*,#36648,.F.);
#51243=ORIENTED_EDGE('',*,*,#36649,.T.);
#51244=ORIENTED_EDGE('',*,*,#36648,.T.);
#51245=ORIENTED_EDGE('',*,*,#36650,.F.);
#51246=ORIENTED_EDGE('',*,*,#36651,.F.);
#51247=ORIENTED_EDGE('',*,*,#36652,.T.);
#51248=ORIENTED_EDGE('',*,*,#36651,.T.);
#51249=ORIENTED_EDGE('',*,*,#36653,.F.);
#51250=ORIENTED_EDGE('',*,*,#36654,.F.);
#51251=ORIENTED_EDGE('',*,*,#36655,.T.);
#51252=ORIENTED_EDGE('',*,*,#36654,.T.);
#51253=ORIENTED_EDGE('',*,*,#36656,.F.);
#51254=ORIENTED_EDGE('',*,*,#36657,.F.);
#51255=ORIENTED_EDGE('',*,*,#36658,.T.);
#51256=ORIENTED_EDGE('',*,*,#36657,.T.);
#51257=ORIENTED_EDGE('',*,*,#36659,.F.);
#51258=ORIENTED_EDGE('',*,*,#36660,.F.);
#51259=ORIENTED_EDGE('',*,*,#36661,.T.);
#51260=ORIENTED_EDGE('',*,*,#36660,.T.);
#51261=ORIENTED_EDGE('',*,*,#36662,.F.);
#51262=ORIENTED_EDGE('',*,*,#36663,.F.);
#51263=ORIENTED_EDGE('',*,*,#36664,.T.);
#51264=ORIENTED_EDGE('',*,*,#36663,.T.);
#51265=ORIENTED_EDGE('',*,*,#36665,.F.);
#51266=ORIENTED_EDGE('',*,*,#36666,.F.);
#51267=ORIENTED_EDGE('',*,*,#36667,.T.);
#51268=ORIENTED_EDGE('',*,*,#36666,.T.);
#51269=ORIENTED_EDGE('',*,*,#36668,.F.);
#51270=ORIENTED_EDGE('',*,*,#36669,.F.);
#51271=ORIENTED_EDGE('',*,*,#36670,.T.);
#51272=ORIENTED_EDGE('',*,*,#36669,.T.);
#51273=ORIENTED_EDGE('',*,*,#36671,.F.);
#51274=ORIENTED_EDGE('',*,*,#36672,.F.);
#51275=ORIENTED_EDGE('',*,*,#36673,.T.);
#51276=ORIENTED_EDGE('',*,*,#36672,.T.);
#51277=ORIENTED_EDGE('',*,*,#36674,.F.);
#51278=ORIENTED_EDGE('',*,*,#36675,.F.);
#51279=ORIENTED_EDGE('',*,*,#36676,.T.);
#51280=ORIENTED_EDGE('',*,*,#36675,.T.);
#51281=ORIENTED_EDGE('',*,*,#36677,.F.);
#51282=ORIENTED_EDGE('',*,*,#36678,.F.);
#51283=ORIENTED_EDGE('',*,*,#36679,.T.);
#51284=ORIENTED_EDGE('',*,*,#36678,.T.);
#51285=ORIENTED_EDGE('',*,*,#36680,.F.);
#51286=ORIENTED_EDGE('',*,*,#36681,.F.);
#51287=ORIENTED_EDGE('',*,*,#36682,.T.);
#51288=ORIENTED_EDGE('',*,*,#36681,.T.);
#51289=ORIENTED_EDGE('',*,*,#36683,.F.);
#51290=ORIENTED_EDGE('',*,*,#36684,.F.);
#51291=ORIENTED_EDGE('',*,*,#36685,.T.);
#51292=ORIENTED_EDGE('',*,*,#36684,.T.);
#51293=ORIENTED_EDGE('',*,*,#36686,.F.);
#51294=ORIENTED_EDGE('',*,*,#36687,.F.);
#51295=ORIENTED_EDGE('',*,*,#36688,.T.);
#51296=ORIENTED_EDGE('',*,*,#36687,.T.);
#51297=ORIENTED_EDGE('',*,*,#36689,.F.);
#51298=ORIENTED_EDGE('',*,*,#36690,.F.);
#51299=ORIENTED_EDGE('',*,*,#36691,.T.);
#51300=ORIENTED_EDGE('',*,*,#36690,.T.);
#51301=ORIENTED_EDGE('',*,*,#36692,.F.);
#51302=ORIENTED_EDGE('',*,*,#36693,.F.);
#51303=ORIENTED_EDGE('',*,*,#36694,.T.);
#51304=ORIENTED_EDGE('',*,*,#36693,.T.);
#51305=ORIENTED_EDGE('',*,*,#36695,.F.);
#51306=ORIENTED_EDGE('',*,*,#36696,.F.);
#51307=ORIENTED_EDGE('',*,*,#36697,.T.);
#51308=ORIENTED_EDGE('',*,*,#36696,.T.);
#51309=ORIENTED_EDGE('',*,*,#36698,.F.);
#51310=ORIENTED_EDGE('',*,*,#36699,.F.);
#51311=ORIENTED_EDGE('',*,*,#36700,.T.);
#51312=ORIENTED_EDGE('',*,*,#36699,.T.);
#51313=ORIENTED_EDGE('',*,*,#36701,.F.);
#51314=ORIENTED_EDGE('',*,*,#36702,.F.);
#51315=ORIENTED_EDGE('',*,*,#36703,.T.);
#51316=ORIENTED_EDGE('',*,*,#36702,.T.);
#51317=ORIENTED_EDGE('',*,*,#36704,.F.);
#51318=ORIENTED_EDGE('',*,*,#36705,.F.);
#51319=ORIENTED_EDGE('',*,*,#36706,.T.);
#51320=ORIENTED_EDGE('',*,*,#36705,.T.);
#51321=ORIENTED_EDGE('',*,*,#36707,.F.);
#51322=ORIENTED_EDGE('',*,*,#36708,.F.);
#51323=ORIENTED_EDGE('',*,*,#36709,.T.);
#51324=ORIENTED_EDGE('',*,*,#36708,.T.);
#51325=ORIENTED_EDGE('',*,*,#36710,.F.);
#51326=ORIENTED_EDGE('',*,*,#36711,.F.);
#51327=ORIENTED_EDGE('',*,*,#36712,.T.);
#51328=ORIENTED_EDGE('',*,*,#36711,.T.);
#51329=ORIENTED_EDGE('',*,*,#36713,.F.);
#51330=ORIENTED_EDGE('',*,*,#36714,.F.);
#51331=ORIENTED_EDGE('',*,*,#36715,.T.);
#51332=ORIENTED_EDGE('',*,*,#36714,.T.);
#51333=ORIENTED_EDGE('',*,*,#36716,.F.);
#51334=ORIENTED_EDGE('',*,*,#36717,.F.);
#51335=ORIENTED_EDGE('',*,*,#36718,.T.);
#51336=ORIENTED_EDGE('',*,*,#36717,.T.);
#51337=ORIENTED_EDGE('',*,*,#36719,.F.);
#51338=ORIENTED_EDGE('',*,*,#36720,.F.);
#51339=ORIENTED_EDGE('',*,*,#36721,.T.);
#51340=ORIENTED_EDGE('',*,*,#36720,.T.);
#51341=ORIENTED_EDGE('',*,*,#36722,.F.);
#51342=ORIENTED_EDGE('',*,*,#36723,.F.);
#51343=ORIENTED_EDGE('',*,*,#36724,.T.);
#51344=ORIENTED_EDGE('',*,*,#36723,.T.);
#51345=ORIENTED_EDGE('',*,*,#36725,.F.);
#51346=ORIENTED_EDGE('',*,*,#36726,.F.);
#51347=ORIENTED_EDGE('',*,*,#36727,.T.);
#51348=ORIENTED_EDGE('',*,*,#36726,.T.);
#51349=ORIENTED_EDGE('',*,*,#36728,.F.);
#51350=ORIENTED_EDGE('',*,*,#36729,.F.);
#51351=ORIENTED_EDGE('',*,*,#36730,.T.);
#51352=ORIENTED_EDGE('',*,*,#36729,.T.);
#51353=ORIENTED_EDGE('',*,*,#36731,.F.);
#51354=ORIENTED_EDGE('',*,*,#36732,.F.);
#51355=ORIENTED_EDGE('',*,*,#36733,.T.);
#51356=ORIENTED_EDGE('',*,*,#36732,.T.);
#51357=ORIENTED_EDGE('',*,*,#36734,.F.);
#51358=ORIENTED_EDGE('',*,*,#36735,.F.);
#51359=ORIENTED_EDGE('',*,*,#36736,.T.);
#51360=ORIENTED_EDGE('',*,*,#36735,.T.);
#51361=ORIENTED_EDGE('',*,*,#36737,.F.);
#51362=ORIENTED_EDGE('',*,*,#36738,.F.);
#51363=ORIENTED_EDGE('',*,*,#36739,.T.);
#51364=ORIENTED_EDGE('',*,*,#36738,.T.);
#51365=ORIENTED_EDGE('',*,*,#36740,.F.);
#51366=ORIENTED_EDGE('',*,*,#36741,.F.);
#51367=ORIENTED_EDGE('',*,*,#36742,.T.);
#51368=ORIENTED_EDGE('',*,*,#36741,.T.);
#51369=ORIENTED_EDGE('',*,*,#36743,.F.);
#51370=ORIENTED_EDGE('',*,*,#36744,.F.);
#51371=ORIENTED_EDGE('',*,*,#36745,.T.);
#51372=ORIENTED_EDGE('',*,*,#36744,.T.);
#51373=ORIENTED_EDGE('',*,*,#36746,.F.);
#51374=ORIENTED_EDGE('',*,*,#36747,.F.);
#51375=ORIENTED_EDGE('',*,*,#36748,.T.);
#51376=ORIENTED_EDGE('',*,*,#36747,.T.);
#51377=ORIENTED_EDGE('',*,*,#36749,.F.);
#51378=ORIENTED_EDGE('',*,*,#36750,.F.);
#51379=ORIENTED_EDGE('',*,*,#36751,.T.);
#51380=ORIENTED_EDGE('',*,*,#36750,.T.);
#51381=ORIENTED_EDGE('',*,*,#36752,.F.);
#51382=ORIENTED_EDGE('',*,*,#36753,.F.);
#51383=ORIENTED_EDGE('',*,*,#36754,.T.);
#51384=ORIENTED_EDGE('',*,*,#36753,.T.);
#51385=ORIENTED_EDGE('',*,*,#36755,.F.);
#51386=ORIENTED_EDGE('',*,*,#36756,.F.);
#51387=ORIENTED_EDGE('',*,*,#36757,.T.);
#51388=ORIENTED_EDGE('',*,*,#36756,.T.);
#51389=ORIENTED_EDGE('',*,*,#36758,.F.);
#51390=ORIENTED_EDGE('',*,*,#36759,.F.);
#51391=ORIENTED_EDGE('',*,*,#36760,.T.);
#51392=ORIENTED_EDGE('',*,*,#36759,.T.);
#51393=ORIENTED_EDGE('',*,*,#36761,.F.);
#51394=ORIENTED_EDGE('',*,*,#36762,.F.);
#51395=ORIENTED_EDGE('',*,*,#36763,.T.);
#51396=ORIENTED_EDGE('',*,*,#36762,.T.);
#51397=ORIENTED_EDGE('',*,*,#36764,.F.);
#51398=ORIENTED_EDGE('',*,*,#36765,.F.);
#51399=ORIENTED_EDGE('',*,*,#36766,.T.);
#51400=ORIENTED_EDGE('',*,*,#36765,.T.);
#51401=ORIENTED_EDGE('',*,*,#36767,.F.);
#51402=ORIENTED_EDGE('',*,*,#36768,.F.);
#51403=ORIENTED_EDGE('',*,*,#36769,.T.);
#51404=ORIENTED_EDGE('',*,*,#36768,.T.);
#51405=ORIENTED_EDGE('',*,*,#36770,.F.);
#51406=ORIENTED_EDGE('',*,*,#36771,.F.);
#51407=ORIENTED_EDGE('',*,*,#36772,.T.);
#51408=ORIENTED_EDGE('',*,*,#36771,.T.);
#51409=ORIENTED_EDGE('',*,*,#36773,.F.);
#51410=ORIENTED_EDGE('',*,*,#36774,.F.);
#51411=ORIENTED_EDGE('',*,*,#36775,.T.);
#51412=ORIENTED_EDGE('',*,*,#36774,.T.);
#51413=ORIENTED_EDGE('',*,*,#36776,.F.);
#51414=ORIENTED_EDGE('',*,*,#36777,.F.);
#51415=ORIENTED_EDGE('',*,*,#36778,.T.);
#51416=ORIENTED_EDGE('',*,*,#36777,.T.);
#51417=ORIENTED_EDGE('',*,*,#36779,.F.);
#51418=ORIENTED_EDGE('',*,*,#36780,.F.);
#51419=ORIENTED_EDGE('',*,*,#36781,.T.);
#51420=ORIENTED_EDGE('',*,*,#36780,.T.);
#51421=ORIENTED_EDGE('',*,*,#36782,.F.);
#51422=ORIENTED_EDGE('',*,*,#36783,.F.);
#51423=ORIENTED_EDGE('',*,*,#36784,.T.);
#51424=ORIENTED_EDGE('',*,*,#36783,.T.);
#51425=ORIENTED_EDGE('',*,*,#36785,.F.);
#51426=ORIENTED_EDGE('',*,*,#36786,.F.);
#51427=ORIENTED_EDGE('',*,*,#36787,.T.);
#51428=ORIENTED_EDGE('',*,*,#36786,.T.);
#51429=ORIENTED_EDGE('',*,*,#36788,.F.);
#51430=ORIENTED_EDGE('',*,*,#36789,.F.);
#51431=ORIENTED_EDGE('',*,*,#36790,.T.);
#51432=ORIENTED_EDGE('',*,*,#36789,.T.);
#51433=ORIENTED_EDGE('',*,*,#36791,.F.);
#51434=ORIENTED_EDGE('',*,*,#36792,.F.);
#51435=ORIENTED_EDGE('',*,*,#36793,.T.);
#51436=ORIENTED_EDGE('',*,*,#36792,.T.);
#51437=ORIENTED_EDGE('',*,*,#36794,.F.);
#51438=ORIENTED_EDGE('',*,*,#36795,.F.);
#51439=ORIENTED_EDGE('',*,*,#36796,.T.);
#51440=ORIENTED_EDGE('',*,*,#36795,.T.);
#51441=ORIENTED_EDGE('',*,*,#36797,.F.);
#51442=ORIENTED_EDGE('',*,*,#36798,.F.);
#51443=ORIENTED_EDGE('',*,*,#36799,.T.);
#51444=ORIENTED_EDGE('',*,*,#36798,.T.);
#51445=ORIENTED_EDGE('',*,*,#36800,.F.);
#51446=ORIENTED_EDGE('',*,*,#36801,.F.);
#51447=ORIENTED_EDGE('',*,*,#36802,.T.);
#51448=ORIENTED_EDGE('',*,*,#36801,.T.);
#51449=ORIENTED_EDGE('',*,*,#36803,.F.);
#51450=ORIENTED_EDGE('',*,*,#36804,.F.);
#51451=ORIENTED_EDGE('',*,*,#36805,.T.);
#51452=ORIENTED_EDGE('',*,*,#36804,.T.);
#51453=ORIENTED_EDGE('',*,*,#36806,.F.);
#51454=ORIENTED_EDGE('',*,*,#36807,.F.);
#51455=ORIENTED_EDGE('',*,*,#36808,.T.);
#51456=ORIENTED_EDGE('',*,*,#36807,.T.);
#51457=ORIENTED_EDGE('',*,*,#36809,.F.);
#51458=ORIENTED_EDGE('',*,*,#36810,.F.);
#51459=ORIENTED_EDGE('',*,*,#36811,.T.);
#51460=ORIENTED_EDGE('',*,*,#36810,.T.);
#51461=ORIENTED_EDGE('',*,*,#36812,.F.);
#51462=ORIENTED_EDGE('',*,*,#36813,.F.);
#51463=ORIENTED_EDGE('',*,*,#36814,.T.);
#51464=ORIENTED_EDGE('',*,*,#36813,.T.);
#51465=ORIENTED_EDGE('',*,*,#36815,.F.);
#51466=ORIENTED_EDGE('',*,*,#36816,.F.);
#51467=ORIENTED_EDGE('',*,*,#36817,.T.);
#51468=ORIENTED_EDGE('',*,*,#36816,.T.);
#51469=ORIENTED_EDGE('',*,*,#36818,.F.);
#51470=ORIENTED_EDGE('',*,*,#36819,.F.);
#51471=ORIENTED_EDGE('',*,*,#36820,.T.);
#51472=ORIENTED_EDGE('',*,*,#36819,.T.);
#51473=ORIENTED_EDGE('',*,*,#36821,.F.);
#51474=ORIENTED_EDGE('',*,*,#36822,.F.);
#51475=ORIENTED_EDGE('',*,*,#36823,.T.);
#51476=ORIENTED_EDGE('',*,*,#36822,.T.);
#51477=ORIENTED_EDGE('',*,*,#36824,.F.);
#51478=ORIENTED_EDGE('',*,*,#36825,.F.);
#51479=ORIENTED_EDGE('',*,*,#36826,.T.);
#51480=ORIENTED_EDGE('',*,*,#36825,.T.);
#51481=ORIENTED_EDGE('',*,*,#36827,.F.);
#51482=ORIENTED_EDGE('',*,*,#36828,.F.);
#51483=ORIENTED_EDGE('',*,*,#36829,.T.);
#51484=ORIENTED_EDGE('',*,*,#36828,.T.);
#51485=ORIENTED_EDGE('',*,*,#36830,.F.);
#51486=ORIENTED_EDGE('',*,*,#36831,.F.);
#51487=ORIENTED_EDGE('',*,*,#36832,.T.);
#51488=ORIENTED_EDGE('',*,*,#36831,.T.);
#51489=ORIENTED_EDGE('',*,*,#36833,.F.);
#51490=ORIENTED_EDGE('',*,*,#36834,.F.);
#51491=ORIENTED_EDGE('',*,*,#36835,.T.);
#51492=ORIENTED_EDGE('',*,*,#36834,.T.);
#51493=ORIENTED_EDGE('',*,*,#36836,.F.);
#51494=ORIENTED_EDGE('',*,*,#36837,.F.);
#51495=ORIENTED_EDGE('',*,*,#36838,.T.);
#51496=ORIENTED_EDGE('',*,*,#36837,.T.);
#51497=ORIENTED_EDGE('',*,*,#36839,.F.);
#51498=ORIENTED_EDGE('',*,*,#36840,.F.);
#51499=ORIENTED_EDGE('',*,*,#36841,.T.);
#51500=ORIENTED_EDGE('',*,*,#36840,.T.);
#51501=ORIENTED_EDGE('',*,*,#36842,.F.);
#51502=ORIENTED_EDGE('',*,*,#36843,.F.);
#51503=ORIENTED_EDGE('',*,*,#36844,.T.);
#51504=ORIENTED_EDGE('',*,*,#36843,.T.);
#51505=ORIENTED_EDGE('',*,*,#36845,.F.);
#51506=ORIENTED_EDGE('',*,*,#36846,.F.);
#51507=ORIENTED_EDGE('',*,*,#36847,.T.);
#51508=ORIENTED_EDGE('',*,*,#36846,.T.);
#51509=ORIENTED_EDGE('',*,*,#36848,.F.);
#51510=ORIENTED_EDGE('',*,*,#36849,.F.);
#51511=ORIENTED_EDGE('',*,*,#36850,.T.);
#51512=ORIENTED_EDGE('',*,*,#36849,.T.);
#51513=ORIENTED_EDGE('',*,*,#36851,.F.);
#51514=ORIENTED_EDGE('',*,*,#36852,.F.);
#51515=ORIENTED_EDGE('',*,*,#36853,.T.);
#51516=ORIENTED_EDGE('',*,*,#36852,.T.);
#51517=ORIENTED_EDGE('',*,*,#36854,.F.);
#51518=ORIENTED_EDGE('',*,*,#36855,.F.);
#51519=ORIENTED_EDGE('',*,*,#36856,.T.);
#51520=ORIENTED_EDGE('',*,*,#36855,.T.);
#51521=ORIENTED_EDGE('',*,*,#36857,.F.);
#51522=ORIENTED_EDGE('',*,*,#36858,.F.);
#51523=ORIENTED_EDGE('',*,*,#36859,.T.);
#51524=ORIENTED_EDGE('',*,*,#36858,.T.);
#51525=ORIENTED_EDGE('',*,*,#36860,.F.);
#51526=ORIENTED_EDGE('',*,*,#36861,.F.);
#51527=ORIENTED_EDGE('',*,*,#36862,.T.);
#51528=ORIENTED_EDGE('',*,*,#36861,.T.);
#51529=ORIENTED_EDGE('',*,*,#36863,.F.);
#51530=ORIENTED_EDGE('',*,*,#36864,.F.);
#51531=ORIENTED_EDGE('',*,*,#36865,.T.);
#51532=ORIENTED_EDGE('',*,*,#36864,.T.);
#51533=ORIENTED_EDGE('',*,*,#36866,.F.);
#51534=ORIENTED_EDGE('',*,*,#36867,.F.);
#51535=ORIENTED_EDGE('',*,*,#36868,.T.);
#51536=ORIENTED_EDGE('',*,*,#36867,.T.);
#51537=ORIENTED_EDGE('',*,*,#36869,.F.);
#51538=ORIENTED_EDGE('',*,*,#36870,.F.);
#51539=ORIENTED_EDGE('',*,*,#36871,.T.);
#51540=ORIENTED_EDGE('',*,*,#36870,.T.);
#51541=ORIENTED_EDGE('',*,*,#36872,.F.);
#51542=ORIENTED_EDGE('',*,*,#36873,.F.);
#51543=ORIENTED_EDGE('',*,*,#36874,.T.);
#51544=ORIENTED_EDGE('',*,*,#36873,.T.);
#51545=ORIENTED_EDGE('',*,*,#36875,.F.);
#51546=ORIENTED_EDGE('',*,*,#36876,.F.);
#51547=ORIENTED_EDGE('',*,*,#36877,.T.);
#51548=ORIENTED_EDGE('',*,*,#36876,.T.);
#51549=ORIENTED_EDGE('',*,*,#36878,.F.);
#51550=ORIENTED_EDGE('',*,*,#36879,.F.);
#51551=ORIENTED_EDGE('',*,*,#36880,.T.);
#51552=ORIENTED_EDGE('',*,*,#36879,.T.);
#51553=ORIENTED_EDGE('',*,*,#36881,.F.);
#51554=ORIENTED_EDGE('',*,*,#36882,.F.);
#51555=ORIENTED_EDGE('',*,*,#36883,.T.);
#51556=ORIENTED_EDGE('',*,*,#36882,.T.);
#51557=ORIENTED_EDGE('',*,*,#36884,.F.);
#51558=ORIENTED_EDGE('',*,*,#36885,.F.);
#51559=ORIENTED_EDGE('',*,*,#36886,.T.);
#51560=ORIENTED_EDGE('',*,*,#36885,.T.);
#51561=ORIENTED_EDGE('',*,*,#36887,.F.);
#51562=ORIENTED_EDGE('',*,*,#36888,.F.);
#51563=ORIENTED_EDGE('',*,*,#36889,.T.);
#51564=ORIENTED_EDGE('',*,*,#36888,.T.);
#51565=ORIENTED_EDGE('',*,*,#36890,.F.);
#51566=ORIENTED_EDGE('',*,*,#36891,.F.);
#51567=ORIENTED_EDGE('',*,*,#36892,.T.);
#51568=ORIENTED_EDGE('',*,*,#36891,.T.);
#51569=ORIENTED_EDGE('',*,*,#36893,.F.);
#51570=ORIENTED_EDGE('',*,*,#36894,.F.);
#51571=ORIENTED_EDGE('',*,*,#36895,.T.);
#51572=ORIENTED_EDGE('',*,*,#36894,.T.);
#51573=ORIENTED_EDGE('',*,*,#36896,.F.);
#51574=ORIENTED_EDGE('',*,*,#36897,.F.);
#51575=ORIENTED_EDGE('',*,*,#36898,.T.);
#51576=ORIENTED_EDGE('',*,*,#36897,.T.);
#51577=ORIENTED_EDGE('',*,*,#36899,.F.);
#51578=ORIENTED_EDGE('',*,*,#36900,.F.);
#51579=ORIENTED_EDGE('',*,*,#36901,.T.);
#51580=ORIENTED_EDGE('',*,*,#36900,.T.);
#51581=ORIENTED_EDGE('',*,*,#36902,.F.);
#51582=ORIENTED_EDGE('',*,*,#36903,.F.);
#51583=ORIENTED_EDGE('',*,*,#36904,.T.);
#51584=ORIENTED_EDGE('',*,*,#36903,.T.);
#51585=ORIENTED_EDGE('',*,*,#36905,.F.);
#51586=ORIENTED_EDGE('',*,*,#36906,.F.);
#51587=ORIENTED_EDGE('',*,*,#36907,.T.);
#51588=ORIENTED_EDGE('',*,*,#36906,.T.);
#51589=ORIENTED_EDGE('',*,*,#36908,.F.);
#51590=ORIENTED_EDGE('',*,*,#36909,.F.);
#51591=ORIENTED_EDGE('',*,*,#36910,.T.);
#51592=ORIENTED_EDGE('',*,*,#36909,.T.);
#51593=ORIENTED_EDGE('',*,*,#36911,.F.);
#51594=ORIENTED_EDGE('',*,*,#36912,.F.);
#51595=ORIENTED_EDGE('',*,*,#36913,.T.);
#51596=ORIENTED_EDGE('',*,*,#36912,.T.);
#51597=ORIENTED_EDGE('',*,*,#36914,.F.);
#51598=ORIENTED_EDGE('',*,*,#36915,.F.);
#51599=ORIENTED_EDGE('',*,*,#36916,.T.);
#51600=ORIENTED_EDGE('',*,*,#36915,.T.);
#51601=ORIENTED_EDGE('',*,*,#36917,.F.);
#51602=ORIENTED_EDGE('',*,*,#36918,.F.);
#51603=ORIENTED_EDGE('',*,*,#36919,.T.);
#51604=ORIENTED_EDGE('',*,*,#36918,.T.);
#51605=ORIENTED_EDGE('',*,*,#36920,.F.);
#51606=ORIENTED_EDGE('',*,*,#36921,.F.);
#51607=ORIENTED_EDGE('',*,*,#36922,.T.);
#51608=ORIENTED_EDGE('',*,*,#36921,.T.);
#51609=ORIENTED_EDGE('',*,*,#36923,.F.);
#51610=ORIENTED_EDGE('',*,*,#36924,.F.);
#51611=ORIENTED_EDGE('',*,*,#36925,.T.);
#51612=ORIENTED_EDGE('',*,*,#36924,.T.);
#51613=ORIENTED_EDGE('',*,*,#36926,.F.);
#51614=ORIENTED_EDGE('',*,*,#36927,.F.);
#51615=ORIENTED_EDGE('',*,*,#36928,.T.);
#51616=ORIENTED_EDGE('',*,*,#36927,.T.);
#51617=ORIENTED_EDGE('',*,*,#36929,.F.);
#51618=ORIENTED_EDGE('',*,*,#36930,.F.);
#51619=ORIENTED_EDGE('',*,*,#36931,.T.);
#51620=ORIENTED_EDGE('',*,*,#36930,.T.);
#51621=ORIENTED_EDGE('',*,*,#36932,.F.);
#51622=ORIENTED_EDGE('',*,*,#36933,.F.);
#51623=ORIENTED_EDGE('',*,*,#36934,.T.);
#51624=ORIENTED_EDGE('',*,*,#36933,.T.);
#51625=ORIENTED_EDGE('',*,*,#36935,.F.);
#51626=ORIENTED_EDGE('',*,*,#36936,.F.);
#51627=ORIENTED_EDGE('',*,*,#36937,.T.);
#51628=ORIENTED_EDGE('',*,*,#36936,.T.);
#51629=ORIENTED_EDGE('',*,*,#36938,.F.);
#51630=ORIENTED_EDGE('',*,*,#36939,.F.);
#51631=ORIENTED_EDGE('',*,*,#36940,.T.);
#51632=ORIENTED_EDGE('',*,*,#36939,.T.);
#51633=ORIENTED_EDGE('',*,*,#36941,.F.);
#51634=ORIENTED_EDGE('',*,*,#36942,.F.);
#51635=ORIENTED_EDGE('',*,*,#36943,.T.);
#51636=ORIENTED_EDGE('',*,*,#36942,.T.);
#51637=ORIENTED_EDGE('',*,*,#36944,.F.);
#51638=ORIENTED_EDGE('',*,*,#36945,.F.);
#51639=ORIENTED_EDGE('',*,*,#36946,.T.);
#51640=ORIENTED_EDGE('',*,*,#36945,.T.);
#51641=ORIENTED_EDGE('',*,*,#36947,.F.);
#51642=ORIENTED_EDGE('',*,*,#36948,.F.);
#51643=ORIENTED_EDGE('',*,*,#36949,.T.);
#51644=ORIENTED_EDGE('',*,*,#36948,.T.);
#51645=ORIENTED_EDGE('',*,*,#36950,.F.);
#51646=ORIENTED_EDGE('',*,*,#36951,.F.);
#51647=ORIENTED_EDGE('',*,*,#36952,.T.);
#51648=ORIENTED_EDGE('',*,*,#36951,.T.);
#51649=ORIENTED_EDGE('',*,*,#36953,.F.);
#51650=ORIENTED_EDGE('',*,*,#36954,.F.);
#51651=ORIENTED_EDGE('',*,*,#36955,.T.);
#51652=ORIENTED_EDGE('',*,*,#36954,.T.);
#51653=ORIENTED_EDGE('',*,*,#36956,.F.);
#51654=ORIENTED_EDGE('',*,*,#36957,.F.);
#51655=ORIENTED_EDGE('',*,*,#36958,.T.);
#51656=ORIENTED_EDGE('',*,*,#36957,.T.);
#51657=ORIENTED_EDGE('',*,*,#36959,.F.);
#51658=ORIENTED_EDGE('',*,*,#36960,.F.);
#51659=ORIENTED_EDGE('',*,*,#36961,.T.);
#51660=ORIENTED_EDGE('',*,*,#36960,.T.);
#51661=ORIENTED_EDGE('',*,*,#36962,.F.);
#51662=ORIENTED_EDGE('',*,*,#36963,.F.);
#51663=ORIENTED_EDGE('',*,*,#36964,.T.);
#51664=ORIENTED_EDGE('',*,*,#36963,.T.);
#51665=ORIENTED_EDGE('',*,*,#36965,.F.);
#51666=ORIENTED_EDGE('',*,*,#36966,.F.);
#51667=ORIENTED_EDGE('',*,*,#36967,.T.);
#51668=ORIENTED_EDGE('',*,*,#36966,.T.);
#51669=ORIENTED_EDGE('',*,*,#36968,.F.);
#51670=ORIENTED_EDGE('',*,*,#36969,.F.);
#51671=ORIENTED_EDGE('',*,*,#36970,.T.);
#51672=ORIENTED_EDGE('',*,*,#36969,.T.);
#51673=ORIENTED_EDGE('',*,*,#36971,.F.);
#51674=ORIENTED_EDGE('',*,*,#36972,.F.);
#51675=ORIENTED_EDGE('',*,*,#36973,.T.);
#51676=ORIENTED_EDGE('',*,*,#36972,.T.);
#51677=ORIENTED_EDGE('',*,*,#36974,.F.);
#51678=ORIENTED_EDGE('',*,*,#36975,.F.);
#51679=ORIENTED_EDGE('',*,*,#36976,.T.);
#51680=ORIENTED_EDGE('',*,*,#36975,.T.);
#51681=ORIENTED_EDGE('',*,*,#36977,.F.);
#51682=ORIENTED_EDGE('',*,*,#36978,.F.);
#51683=ORIENTED_EDGE('',*,*,#36979,.T.);
#51684=ORIENTED_EDGE('',*,*,#36978,.T.);
#51685=ORIENTED_EDGE('',*,*,#36980,.F.);
#51686=ORIENTED_EDGE('',*,*,#36981,.F.);
#51687=ORIENTED_EDGE('',*,*,#36982,.T.);
#51688=ORIENTED_EDGE('',*,*,#36981,.T.);
#51689=ORIENTED_EDGE('',*,*,#36983,.F.);
#51690=ORIENTED_EDGE('',*,*,#36984,.F.);
#51691=ORIENTED_EDGE('',*,*,#36985,.T.);
#51692=ORIENTED_EDGE('',*,*,#36984,.T.);
#51693=ORIENTED_EDGE('',*,*,#36986,.F.);
#51694=ORIENTED_EDGE('',*,*,#36987,.F.);
#51695=ORIENTED_EDGE('',*,*,#36988,.T.);
#51696=ORIENTED_EDGE('',*,*,#36987,.T.);
#51697=ORIENTED_EDGE('',*,*,#36989,.F.);
#51698=ORIENTED_EDGE('',*,*,#36990,.F.);
#51699=ORIENTED_EDGE('',*,*,#36991,.T.);
#51700=ORIENTED_EDGE('',*,*,#36990,.T.);
#51701=ORIENTED_EDGE('',*,*,#36992,.F.);
#51702=ORIENTED_EDGE('',*,*,#36993,.F.);
#51703=ORIENTED_EDGE('',*,*,#36994,.T.);
#51704=ORIENTED_EDGE('',*,*,#36993,.T.);
#51705=ORIENTED_EDGE('',*,*,#36995,.F.);
#51706=ORIENTED_EDGE('',*,*,#36996,.F.);
#51707=ORIENTED_EDGE('',*,*,#36997,.T.);
#51708=ORIENTED_EDGE('',*,*,#36996,.T.);
#51709=ORIENTED_EDGE('',*,*,#36998,.F.);
#51710=ORIENTED_EDGE('',*,*,#36999,.F.);
#51711=ORIENTED_EDGE('',*,*,#37000,.T.);
#51712=ORIENTED_EDGE('',*,*,#36999,.T.);
#51713=ORIENTED_EDGE('',*,*,#37001,.F.);
#51714=ORIENTED_EDGE('',*,*,#37002,.F.);
#51715=ORIENTED_EDGE('',*,*,#37003,.T.);
#51716=ORIENTED_EDGE('',*,*,#37002,.T.);
#51717=ORIENTED_EDGE('',*,*,#37004,.F.);
#51718=ORIENTED_EDGE('',*,*,#37005,.F.);
#51719=ORIENTED_EDGE('',*,*,#37006,.T.);
#51720=ORIENTED_EDGE('',*,*,#37005,.T.);
#51721=ORIENTED_EDGE('',*,*,#37007,.F.);
#51722=ORIENTED_EDGE('',*,*,#37008,.F.);
#51723=ORIENTED_EDGE('',*,*,#37009,.T.);
#51724=ORIENTED_EDGE('',*,*,#37008,.T.);
#51725=ORIENTED_EDGE('',*,*,#37010,.F.);
#51726=ORIENTED_EDGE('',*,*,#37011,.F.);
#51727=ORIENTED_EDGE('',*,*,#37012,.T.);
#51728=ORIENTED_EDGE('',*,*,#37011,.T.);
#51729=ORIENTED_EDGE('',*,*,#37013,.F.);
#51730=ORIENTED_EDGE('',*,*,#37014,.F.);
#51731=ORIENTED_EDGE('',*,*,#37015,.T.);
#51732=ORIENTED_EDGE('',*,*,#37014,.T.);
#51733=ORIENTED_EDGE('',*,*,#37016,.F.);
#51734=ORIENTED_EDGE('',*,*,#37017,.F.);
#51735=ORIENTED_EDGE('',*,*,#37018,.T.);
#51736=ORIENTED_EDGE('',*,*,#37017,.T.);
#51737=ORIENTED_EDGE('',*,*,#37019,.F.);
#51738=ORIENTED_EDGE('',*,*,#37020,.F.);
#51739=ORIENTED_EDGE('',*,*,#37021,.T.);
#51740=ORIENTED_EDGE('',*,*,#37020,.T.);
#51741=ORIENTED_EDGE('',*,*,#37022,.F.);
#51742=ORIENTED_EDGE('',*,*,#37023,.F.);
#51743=ORIENTED_EDGE('',*,*,#37024,.T.);
#51744=ORIENTED_EDGE('',*,*,#37023,.T.);
#51745=ORIENTED_EDGE('',*,*,#37025,.F.);
#51746=ORIENTED_EDGE('',*,*,#37026,.F.);
#51747=ORIENTED_EDGE('',*,*,#37027,.T.);
#51748=ORIENTED_EDGE('',*,*,#37026,.T.);
#51749=ORIENTED_EDGE('',*,*,#37028,.F.);
#51750=ORIENTED_EDGE('',*,*,#37029,.F.);
#51751=ORIENTED_EDGE('',*,*,#37030,.T.);
#51752=ORIENTED_EDGE('',*,*,#37029,.T.);
#51753=ORIENTED_EDGE('',*,*,#37031,.F.);
#51754=ORIENTED_EDGE('',*,*,#37032,.F.);
#51755=ORIENTED_EDGE('',*,*,#37033,.T.);
#51756=ORIENTED_EDGE('',*,*,#37032,.T.);
#51757=ORIENTED_EDGE('',*,*,#37034,.F.);
#51758=ORIENTED_EDGE('',*,*,#37035,.F.);
#51759=ORIENTED_EDGE('',*,*,#37036,.T.);
#51760=ORIENTED_EDGE('',*,*,#37035,.T.);
#51761=ORIENTED_EDGE('',*,*,#37037,.F.);
#51762=ORIENTED_EDGE('',*,*,#37038,.F.);
#51763=ORIENTED_EDGE('',*,*,#37039,.T.);
#51764=ORIENTED_EDGE('',*,*,#37038,.T.);
#51765=ORIENTED_EDGE('',*,*,#37040,.F.);
#51766=ORIENTED_EDGE('',*,*,#37041,.F.);
#51767=ORIENTED_EDGE('',*,*,#37042,.T.);
#51768=ORIENTED_EDGE('',*,*,#37041,.T.);
#51769=ORIENTED_EDGE('',*,*,#37043,.F.);
#51770=ORIENTED_EDGE('',*,*,#37044,.F.);
#51771=ORIENTED_EDGE('',*,*,#37045,.T.);
#51772=ORIENTED_EDGE('',*,*,#37044,.T.);
#51773=ORIENTED_EDGE('',*,*,#37046,.F.);
#51774=ORIENTED_EDGE('',*,*,#37047,.F.);
#51775=ORIENTED_EDGE('',*,*,#37048,.T.);
#51776=ORIENTED_EDGE('',*,*,#37047,.T.);
#51777=ORIENTED_EDGE('',*,*,#37049,.F.);
#51778=ORIENTED_EDGE('',*,*,#37050,.F.);
#51779=ORIENTED_EDGE('',*,*,#37051,.T.);
#51780=ORIENTED_EDGE('',*,*,#37050,.T.);
#51781=ORIENTED_EDGE('',*,*,#37052,.F.);
#51782=ORIENTED_EDGE('',*,*,#37053,.F.);
#51783=ORIENTED_EDGE('',*,*,#37054,.T.);
#51784=ORIENTED_EDGE('',*,*,#37053,.T.);
#51785=ORIENTED_EDGE('',*,*,#37055,.F.);
#51786=ORIENTED_EDGE('',*,*,#37056,.F.);
#51787=ORIENTED_EDGE('',*,*,#37057,.T.);
#51788=ORIENTED_EDGE('',*,*,#37056,.T.);
#51789=ORIENTED_EDGE('',*,*,#37058,.F.);
#51790=ORIENTED_EDGE('',*,*,#37059,.F.);
#51791=ORIENTED_EDGE('',*,*,#37060,.T.);
#51792=ORIENTED_EDGE('',*,*,#37059,.T.);
#51793=ORIENTED_EDGE('',*,*,#37061,.F.);
#51794=ORIENTED_EDGE('',*,*,#37062,.F.);
#51795=ORIENTED_EDGE('',*,*,#37063,.T.);
#51796=ORIENTED_EDGE('',*,*,#37062,.T.);
#51797=ORIENTED_EDGE('',*,*,#37064,.F.);
#51798=ORIENTED_EDGE('',*,*,#37065,.F.);
#51799=ORIENTED_EDGE('',*,*,#37066,.T.);
#51800=ORIENTED_EDGE('',*,*,#37065,.T.);
#51801=ORIENTED_EDGE('',*,*,#37067,.F.);
#51802=ORIENTED_EDGE('',*,*,#37068,.F.);
#51803=ORIENTED_EDGE('',*,*,#37069,.T.);
#51804=ORIENTED_EDGE('',*,*,#37068,.T.);
#51805=ORIENTED_EDGE('',*,*,#37070,.F.);
#51806=ORIENTED_EDGE('',*,*,#37071,.F.);
#51807=ORIENTED_EDGE('',*,*,#37072,.T.);
#51808=ORIENTED_EDGE('',*,*,#37071,.T.);
#51809=ORIENTED_EDGE('',*,*,#37073,.F.);
#51810=ORIENTED_EDGE('',*,*,#37074,.F.);
#51811=ORIENTED_EDGE('',*,*,#37075,.T.);
#51812=ORIENTED_EDGE('',*,*,#37074,.T.);
#51813=ORIENTED_EDGE('',*,*,#37076,.F.);
#51814=ORIENTED_EDGE('',*,*,#37077,.F.);
#51815=ORIENTED_EDGE('',*,*,#37078,.T.);
#51816=ORIENTED_EDGE('',*,*,#37077,.T.);
#51817=ORIENTED_EDGE('',*,*,#37079,.F.);
#51818=ORIENTED_EDGE('',*,*,#37080,.F.);
#51819=ORIENTED_EDGE('',*,*,#37081,.T.);
#51820=ORIENTED_EDGE('',*,*,#37080,.T.);
#51821=ORIENTED_EDGE('',*,*,#37082,.F.);
#51822=ORIENTED_EDGE('',*,*,#37083,.F.);
#51823=ORIENTED_EDGE('',*,*,#37084,.T.);
#51824=ORIENTED_EDGE('',*,*,#37083,.T.);
#51825=ORIENTED_EDGE('',*,*,#37085,.F.);
#51826=ORIENTED_EDGE('',*,*,#37086,.F.);
#51827=ORIENTED_EDGE('',*,*,#37087,.T.);
#51828=ORIENTED_EDGE('',*,*,#37086,.T.);
#51829=ORIENTED_EDGE('',*,*,#37088,.F.);
#51830=ORIENTED_EDGE('',*,*,#37089,.F.);
#51831=ORIENTED_EDGE('',*,*,#37090,.T.);
#51832=ORIENTED_EDGE('',*,*,#37089,.T.);
#51833=ORIENTED_EDGE('',*,*,#37091,.F.);
#51834=ORIENTED_EDGE('',*,*,#37092,.F.);
#51835=ORIENTED_EDGE('',*,*,#37093,.T.);
#51836=ORIENTED_EDGE('',*,*,#37092,.T.);
#51837=ORIENTED_EDGE('',*,*,#37094,.F.);
#51838=ORIENTED_EDGE('',*,*,#37095,.F.);
#51839=ORIENTED_EDGE('',*,*,#37096,.T.);
#51840=ORIENTED_EDGE('',*,*,#37095,.T.);
#51841=ORIENTED_EDGE('',*,*,#37097,.F.);
#51842=ORIENTED_EDGE('',*,*,#37098,.F.);
#51843=ORIENTED_EDGE('',*,*,#37099,.T.);
#51844=ORIENTED_EDGE('',*,*,#37098,.T.);
#51845=ORIENTED_EDGE('',*,*,#37100,.F.);
#51846=ORIENTED_EDGE('',*,*,#37101,.F.);
#51847=ORIENTED_EDGE('',*,*,#37102,.T.);
#51848=ORIENTED_EDGE('',*,*,#37101,.T.);
#51849=ORIENTED_EDGE('',*,*,#37103,.F.);
#51850=ORIENTED_EDGE('',*,*,#37104,.F.);
#51851=ORIENTED_EDGE('',*,*,#37105,.T.);
#51852=ORIENTED_EDGE('',*,*,#37104,.T.);
#51853=ORIENTED_EDGE('',*,*,#37106,.F.);
#51854=ORIENTED_EDGE('',*,*,#37107,.F.);
#51855=ORIENTED_EDGE('',*,*,#37108,.T.);
#51856=ORIENTED_EDGE('',*,*,#37107,.T.);
#51857=ORIENTED_EDGE('',*,*,#37109,.F.);
#51858=ORIENTED_EDGE('',*,*,#37110,.F.);
#51859=ORIENTED_EDGE('',*,*,#37111,.T.);
#51860=ORIENTED_EDGE('',*,*,#37110,.T.);
#51861=ORIENTED_EDGE('',*,*,#37112,.F.);
#51862=ORIENTED_EDGE('',*,*,#37113,.F.);
#51863=ORIENTED_EDGE('',*,*,#37114,.T.);
#51864=ORIENTED_EDGE('',*,*,#37113,.T.);
#51865=ORIENTED_EDGE('',*,*,#37115,.F.);
#51866=ORIENTED_EDGE('',*,*,#37116,.F.);
#51867=ORIENTED_EDGE('',*,*,#37117,.T.);
#51868=ORIENTED_EDGE('',*,*,#37116,.T.);
#51869=ORIENTED_EDGE('',*,*,#37118,.F.);
#51870=ORIENTED_EDGE('',*,*,#37119,.F.);
#51871=ORIENTED_EDGE('',*,*,#37120,.T.);
#51872=ORIENTED_EDGE('',*,*,#37119,.T.);
#51873=ORIENTED_EDGE('',*,*,#37121,.F.);
#51874=ORIENTED_EDGE('',*,*,#37122,.F.);
#51875=ORIENTED_EDGE('',*,*,#37123,.T.);
#51876=ORIENTED_EDGE('',*,*,#37122,.T.);
#51877=ORIENTED_EDGE('',*,*,#37124,.F.);
#51878=ORIENTED_EDGE('',*,*,#37125,.F.);
#51879=ORIENTED_EDGE('',*,*,#37126,.T.);
#51880=ORIENTED_EDGE('',*,*,#37125,.T.);
#51881=ORIENTED_EDGE('',*,*,#37127,.F.);
#51882=ORIENTED_EDGE('',*,*,#37128,.F.);
#51883=ORIENTED_EDGE('',*,*,#37129,.T.);
#51884=ORIENTED_EDGE('',*,*,#37128,.T.);
#51885=ORIENTED_EDGE('',*,*,#37130,.F.);
#51886=ORIENTED_EDGE('',*,*,#37131,.F.);
#51887=ORIENTED_EDGE('',*,*,#37132,.T.);
#51888=ORIENTED_EDGE('',*,*,#37131,.T.);
#51889=ORIENTED_EDGE('',*,*,#37133,.F.);
#51890=ORIENTED_EDGE('',*,*,#37134,.F.);
#51891=ORIENTED_EDGE('',*,*,#37135,.T.);
#51892=ORIENTED_EDGE('',*,*,#37134,.T.);
#51893=ORIENTED_EDGE('',*,*,#37136,.F.);
#51894=ORIENTED_EDGE('',*,*,#37137,.F.);
#51895=ORIENTED_EDGE('',*,*,#37138,.T.);
#51896=ORIENTED_EDGE('',*,*,#37137,.T.);
#51897=ORIENTED_EDGE('',*,*,#37139,.F.);
#51898=ORIENTED_EDGE('',*,*,#37140,.F.);
#51899=ORIENTED_EDGE('',*,*,#37141,.T.);
#51900=ORIENTED_EDGE('',*,*,#37140,.T.);
#51901=ORIENTED_EDGE('',*,*,#37142,.F.);
#51902=ORIENTED_EDGE('',*,*,#37143,.F.);
#51903=ORIENTED_EDGE('',*,*,#37144,.T.);
#51904=ORIENTED_EDGE('',*,*,#37143,.T.);
#51905=ORIENTED_EDGE('',*,*,#37145,.F.);
#51906=ORIENTED_EDGE('',*,*,#37146,.F.);
#51907=ORIENTED_EDGE('',*,*,#37147,.T.);
#51908=ORIENTED_EDGE('',*,*,#37146,.T.);
#51909=ORIENTED_EDGE('',*,*,#37148,.F.);
#51910=ORIENTED_EDGE('',*,*,#37149,.F.);
#51911=ORIENTED_EDGE('',*,*,#37150,.T.);
#51912=ORIENTED_EDGE('',*,*,#37149,.T.);
#51913=ORIENTED_EDGE('',*,*,#37151,.F.);
#51914=ORIENTED_EDGE('',*,*,#37152,.F.);
#51915=ORIENTED_EDGE('',*,*,#37153,.T.);
#51916=ORIENTED_EDGE('',*,*,#37152,.T.);
#51917=ORIENTED_EDGE('',*,*,#37154,.F.);
#51918=ORIENTED_EDGE('',*,*,#37155,.F.);
#51919=ORIENTED_EDGE('',*,*,#37156,.T.);
#51920=ORIENTED_EDGE('',*,*,#37155,.T.);
#51921=ORIENTED_EDGE('',*,*,#37157,.F.);
#51922=ORIENTED_EDGE('',*,*,#37158,.F.);
#51923=ORIENTED_EDGE('',*,*,#37159,.T.);
#51924=ORIENTED_EDGE('',*,*,#37158,.T.);
#51925=ORIENTED_EDGE('',*,*,#37160,.F.);
#51926=ORIENTED_EDGE('',*,*,#37161,.F.);
#51927=ORIENTED_EDGE('',*,*,#37162,.T.);
#51928=ORIENTED_EDGE('',*,*,#37161,.T.);
#51929=ORIENTED_EDGE('',*,*,#37163,.F.);
#51930=ORIENTED_EDGE('',*,*,#37164,.F.);
#51931=ORIENTED_EDGE('',*,*,#37165,.T.);
#51932=ORIENTED_EDGE('',*,*,#37164,.T.);
#51933=ORIENTED_EDGE('',*,*,#37166,.F.);
#51934=ORIENTED_EDGE('',*,*,#37167,.F.);
#51935=ORIENTED_EDGE('',*,*,#37168,.T.);
#51936=ORIENTED_EDGE('',*,*,#37167,.T.);
#51937=ORIENTED_EDGE('',*,*,#37169,.F.);
#51938=ORIENTED_EDGE('',*,*,#37170,.F.);
#51939=ORIENTED_EDGE('',*,*,#37171,.T.);
#51940=ORIENTED_EDGE('',*,*,#37170,.T.);
#51941=ORIENTED_EDGE('',*,*,#37172,.F.);
#51942=ORIENTED_EDGE('',*,*,#37173,.F.);
#51943=ORIENTED_EDGE('',*,*,#37174,.T.);
#51944=ORIENTED_EDGE('',*,*,#37173,.T.);
#51945=ORIENTED_EDGE('',*,*,#37175,.F.);
#51946=ORIENTED_EDGE('',*,*,#37176,.F.);
#51947=ORIENTED_EDGE('',*,*,#37177,.T.);
#51948=ORIENTED_EDGE('',*,*,#37176,.T.);
#51949=ORIENTED_EDGE('',*,*,#37178,.F.);
#51950=ORIENTED_EDGE('',*,*,#37179,.F.);
#51951=ORIENTED_EDGE('',*,*,#37180,.T.);
#51952=ORIENTED_EDGE('',*,*,#37179,.T.);
#51953=ORIENTED_EDGE('',*,*,#37181,.F.);
#51954=ORIENTED_EDGE('',*,*,#37182,.F.);
#51955=ORIENTED_EDGE('',*,*,#37183,.T.);
#51956=ORIENTED_EDGE('',*,*,#37182,.T.);
#51957=ORIENTED_EDGE('',*,*,#37184,.F.);
#51958=ORIENTED_EDGE('',*,*,#37185,.F.);
#51959=ORIENTED_EDGE('',*,*,#37186,.T.);
#51960=ORIENTED_EDGE('',*,*,#37185,.T.);
#51961=ORIENTED_EDGE('',*,*,#37187,.F.);
#51962=ORIENTED_EDGE('',*,*,#37188,.F.);
#51963=ORIENTED_EDGE('',*,*,#37189,.T.);
#51964=ORIENTED_EDGE('',*,*,#37188,.T.);
#51965=ORIENTED_EDGE('',*,*,#37190,.F.);
#51966=ORIENTED_EDGE('',*,*,#37191,.F.);
#51967=ORIENTED_EDGE('',*,*,#37192,.T.);
#51968=ORIENTED_EDGE('',*,*,#37191,.T.);
#51969=ORIENTED_EDGE('',*,*,#37193,.F.);
#51970=ORIENTED_EDGE('',*,*,#37194,.F.);
#51971=ORIENTED_EDGE('',*,*,#37195,.T.);
#51972=ORIENTED_EDGE('',*,*,#37194,.T.);
#51973=ORIENTED_EDGE('',*,*,#37196,.F.);
#51974=ORIENTED_EDGE('',*,*,#37197,.F.);
#51975=ORIENTED_EDGE('',*,*,#37198,.T.);
#51976=ORIENTED_EDGE('',*,*,#37197,.T.);
#51977=ORIENTED_EDGE('',*,*,#37199,.F.);
#51978=ORIENTED_EDGE('',*,*,#37200,.F.);
#51979=ORIENTED_EDGE('',*,*,#37201,.T.);
#51980=ORIENTED_EDGE('',*,*,#37200,.T.);
#51981=ORIENTED_EDGE('',*,*,#37202,.F.);
#51982=ORIENTED_EDGE('',*,*,#37203,.F.);
#51983=ORIENTED_EDGE('',*,*,#37204,.T.);
#51984=ORIENTED_EDGE('',*,*,#37203,.T.);
#51985=ORIENTED_EDGE('',*,*,#37205,.F.);
#51986=ORIENTED_EDGE('',*,*,#37206,.F.);
#51987=ORIENTED_EDGE('',*,*,#37207,.T.);
#51988=ORIENTED_EDGE('',*,*,#37206,.T.);
#51989=ORIENTED_EDGE('',*,*,#37208,.F.);
#51990=ORIENTED_EDGE('',*,*,#37209,.F.);
#51991=ORIENTED_EDGE('',*,*,#37210,.T.);
#51992=ORIENTED_EDGE('',*,*,#37209,.T.);
#51993=ORIENTED_EDGE('',*,*,#37211,.F.);
#51994=ORIENTED_EDGE('',*,*,#37212,.F.);
#51995=ORIENTED_EDGE('',*,*,#37213,.T.);
#51996=ORIENTED_EDGE('',*,*,#37212,.T.);
#51997=ORIENTED_EDGE('',*,*,#37214,.F.);
#51998=ORIENTED_EDGE('',*,*,#37215,.F.);
#51999=ORIENTED_EDGE('',*,*,#37216,.T.);
#52000=ORIENTED_EDGE('',*,*,#37215,.T.);
#52001=ORIENTED_EDGE('',*,*,#37217,.F.);
#52002=ORIENTED_EDGE('',*,*,#37218,.F.);
#52003=ORIENTED_EDGE('',*,*,#37219,.T.);
#52004=ORIENTED_EDGE('',*,*,#37218,.T.);
#52005=ORIENTED_EDGE('',*,*,#37220,.F.);
#52006=ORIENTED_EDGE('',*,*,#37221,.F.);
#52007=ORIENTED_EDGE('',*,*,#37222,.T.);
#52008=ORIENTED_EDGE('',*,*,#37221,.T.);
#52009=ORIENTED_EDGE('',*,*,#37223,.F.);
#52010=ORIENTED_EDGE('',*,*,#37224,.F.);
#52011=ORIENTED_EDGE('',*,*,#37225,.T.);
#52012=ORIENTED_EDGE('',*,*,#37224,.T.);
#52013=ORIENTED_EDGE('',*,*,#37226,.F.);
#52014=ORIENTED_EDGE('',*,*,#37227,.F.);
#52015=ORIENTED_EDGE('',*,*,#37228,.T.);
#52016=ORIENTED_EDGE('',*,*,#37227,.T.);
#52017=ORIENTED_EDGE('',*,*,#37229,.F.);
#52018=ORIENTED_EDGE('',*,*,#37230,.F.);
#52019=ORIENTED_EDGE('',*,*,#37231,.T.);
#52020=ORIENTED_EDGE('',*,*,#37230,.T.);
#52021=ORIENTED_EDGE('',*,*,#37232,.F.);
#52022=ORIENTED_EDGE('',*,*,#37233,.F.);
#52023=ORIENTED_EDGE('',*,*,#37234,.T.);
#52024=ORIENTED_EDGE('',*,*,#37233,.T.);
#52025=ORIENTED_EDGE('',*,*,#37235,.F.);
#52026=ORIENTED_EDGE('',*,*,#37236,.F.);
#52027=ORIENTED_EDGE('',*,*,#37237,.T.);
#52028=ORIENTED_EDGE('',*,*,#37236,.T.);
#52029=ORIENTED_EDGE('',*,*,#37238,.F.);
#52030=ORIENTED_EDGE('',*,*,#37239,.F.);
#52031=ORIENTED_EDGE('',*,*,#37240,.T.);
#52032=ORIENTED_EDGE('',*,*,#37239,.T.);
#52033=ORIENTED_EDGE('',*,*,#37241,.F.);
#52034=ORIENTED_EDGE('',*,*,#37242,.F.);
#52035=ORIENTED_EDGE('',*,*,#37243,.T.);
#52036=ORIENTED_EDGE('',*,*,#37242,.T.);
#52037=ORIENTED_EDGE('',*,*,#37244,.F.);
#52038=ORIENTED_EDGE('',*,*,#37245,.F.);
#52039=ORIENTED_EDGE('',*,*,#37246,.T.);
#52040=ORIENTED_EDGE('',*,*,#37245,.T.);
#52041=ORIENTED_EDGE('',*,*,#37247,.F.);
#52042=ORIENTED_EDGE('',*,*,#37248,.F.);
#52043=ORIENTED_EDGE('',*,*,#37249,.T.);
#52044=ORIENTED_EDGE('',*,*,#37248,.T.);
#52045=ORIENTED_EDGE('',*,*,#37250,.F.);
#52046=ORIENTED_EDGE('',*,*,#37251,.F.);
#52047=ORIENTED_EDGE('',*,*,#37252,.T.);
#52048=ORIENTED_EDGE('',*,*,#37251,.T.);
#52049=ORIENTED_EDGE('',*,*,#37253,.F.);
#52050=ORIENTED_EDGE('',*,*,#37254,.F.);
#52051=ORIENTED_EDGE('',*,*,#37255,.T.);
#52052=ORIENTED_EDGE('',*,*,#37254,.T.);
#52053=ORIENTED_EDGE('',*,*,#37256,.F.);
#52054=ORIENTED_EDGE('',*,*,#37257,.F.);
#52055=ORIENTED_EDGE('',*,*,#37258,.T.);
#52056=ORIENTED_EDGE('',*,*,#37257,.T.);
#52057=ORIENTED_EDGE('',*,*,#37259,.F.);
#52058=ORIENTED_EDGE('',*,*,#37260,.F.);
#52059=ORIENTED_EDGE('',*,*,#37261,.T.);
#52060=ORIENTED_EDGE('',*,*,#37260,.T.);
#52061=ORIENTED_EDGE('',*,*,#37262,.F.);
#52062=ORIENTED_EDGE('',*,*,#37263,.F.);
#52063=ORIENTED_EDGE('',*,*,#37264,.T.);
#52064=ORIENTED_EDGE('',*,*,#37263,.T.);
#52065=ORIENTED_EDGE('',*,*,#37265,.F.);
#52066=ORIENTED_EDGE('',*,*,#37266,.F.);
#52067=ORIENTED_EDGE('',*,*,#37267,.T.);
#52068=ORIENTED_EDGE('',*,*,#37266,.T.);
#52069=ORIENTED_EDGE('',*,*,#37268,.F.);
#52070=ORIENTED_EDGE('',*,*,#37269,.F.);
#52071=ORIENTED_EDGE('',*,*,#37270,.T.);
#52072=ORIENTED_EDGE('',*,*,#37269,.T.);
#52073=ORIENTED_EDGE('',*,*,#37271,.F.);
#52074=ORIENTED_EDGE('',*,*,#37272,.F.);
#52075=ORIENTED_EDGE('',*,*,#37273,.T.);
#52076=ORIENTED_EDGE('',*,*,#37272,.T.);
#52077=ORIENTED_EDGE('',*,*,#37274,.F.);
#52078=ORIENTED_EDGE('',*,*,#37275,.F.);
#52079=ORIENTED_EDGE('',*,*,#37276,.T.);
#52080=ORIENTED_EDGE('',*,*,#37275,.T.);
#52081=ORIENTED_EDGE('',*,*,#37277,.F.);
#52082=ORIENTED_EDGE('',*,*,#37278,.F.);
#52083=ORIENTED_EDGE('',*,*,#37279,.T.);
#52084=ORIENTED_EDGE('',*,*,#37278,.T.);
#52085=ORIENTED_EDGE('',*,*,#37280,.F.);
#52086=ORIENTED_EDGE('',*,*,#37281,.F.);
#52087=ORIENTED_EDGE('',*,*,#37282,.T.);
#52088=ORIENTED_EDGE('',*,*,#37281,.T.);
#52089=ORIENTED_EDGE('',*,*,#37283,.F.);
#52090=ORIENTED_EDGE('',*,*,#37284,.F.);
#52091=ORIENTED_EDGE('',*,*,#37285,.T.);
#52092=ORIENTED_EDGE('',*,*,#37284,.T.);
#52093=ORIENTED_EDGE('',*,*,#37286,.F.);
#52094=ORIENTED_EDGE('',*,*,#37287,.F.);
#52095=ORIENTED_EDGE('',*,*,#37288,.T.);
#52096=ORIENTED_EDGE('',*,*,#37287,.T.);
#52097=ORIENTED_EDGE('',*,*,#37289,.F.);
#52098=ORIENTED_EDGE('',*,*,#37290,.F.);
#52099=ORIENTED_EDGE('',*,*,#37291,.T.);
#52100=ORIENTED_EDGE('',*,*,#37290,.T.);
#52101=ORIENTED_EDGE('',*,*,#37292,.F.);
#52102=ORIENTED_EDGE('',*,*,#37293,.F.);
#52103=ORIENTED_EDGE('',*,*,#37294,.T.);
#52104=ORIENTED_EDGE('',*,*,#37293,.T.);
#52105=ORIENTED_EDGE('',*,*,#37295,.F.);
#52106=ORIENTED_EDGE('',*,*,#37296,.F.);
#52107=ORIENTED_EDGE('',*,*,#37297,.T.);
#52108=ORIENTED_EDGE('',*,*,#37296,.T.);
#52109=ORIENTED_EDGE('',*,*,#37298,.F.);
#52110=ORIENTED_EDGE('',*,*,#37299,.F.);
#52111=ORIENTED_EDGE('',*,*,#37300,.T.);
#52112=ORIENTED_EDGE('',*,*,#37299,.T.);
#52113=ORIENTED_EDGE('',*,*,#37301,.F.);
#52114=ORIENTED_EDGE('',*,*,#37302,.F.);
#52115=ORIENTED_EDGE('',*,*,#37303,.T.);
#52116=ORIENTED_EDGE('',*,*,#37302,.T.);
#52117=ORIENTED_EDGE('',*,*,#37304,.F.);
#52118=ORIENTED_EDGE('',*,*,#37305,.F.);
#52119=ORIENTED_EDGE('',*,*,#37306,.T.);
#52120=ORIENTED_EDGE('',*,*,#37305,.T.);
#52121=ORIENTED_EDGE('',*,*,#37307,.F.);
#52122=ORIENTED_EDGE('',*,*,#37308,.F.);
#52123=ORIENTED_EDGE('',*,*,#37309,.T.);
#52124=ORIENTED_EDGE('',*,*,#37308,.T.);
#52125=ORIENTED_EDGE('',*,*,#37310,.F.);
#52126=ORIENTED_EDGE('',*,*,#37311,.F.);
#52127=ORIENTED_EDGE('',*,*,#37312,.T.);
#52128=ORIENTED_EDGE('',*,*,#37311,.T.);
#52129=ORIENTED_EDGE('',*,*,#37313,.F.);
#52130=ORIENTED_EDGE('',*,*,#37314,.F.);
#52131=ORIENTED_EDGE('',*,*,#37315,.T.);
#52132=ORIENTED_EDGE('',*,*,#37314,.T.);
#52133=ORIENTED_EDGE('',*,*,#37316,.F.);
#52134=ORIENTED_EDGE('',*,*,#37317,.F.);
#52135=ORIENTED_EDGE('',*,*,#37318,.T.);
#52136=ORIENTED_EDGE('',*,*,#37317,.T.);
#52137=ORIENTED_EDGE('',*,*,#37319,.F.);
#52138=ORIENTED_EDGE('',*,*,#37320,.F.);
#52139=ORIENTED_EDGE('',*,*,#37321,.T.);
#52140=ORIENTED_EDGE('',*,*,#37320,.T.);
#52141=ORIENTED_EDGE('',*,*,#37322,.F.);
#52142=ORIENTED_EDGE('',*,*,#37323,.F.);
#52143=ORIENTED_EDGE('',*,*,#37324,.T.);
#52144=ORIENTED_EDGE('',*,*,#37323,.T.);
#52145=ORIENTED_EDGE('',*,*,#37325,.F.);
#52146=ORIENTED_EDGE('',*,*,#37326,.F.);
#52147=ORIENTED_EDGE('',*,*,#37327,.T.);
#52148=ORIENTED_EDGE('',*,*,#37326,.T.);
#52149=ORIENTED_EDGE('',*,*,#37328,.F.);
#52150=ORIENTED_EDGE('',*,*,#37329,.F.);
#52151=ORIENTED_EDGE('',*,*,#37330,.T.);
#52152=ORIENTED_EDGE('',*,*,#37329,.T.);
#52153=ORIENTED_EDGE('',*,*,#37331,.F.);
#52154=ORIENTED_EDGE('',*,*,#37332,.F.);
#52155=ORIENTED_EDGE('',*,*,#37333,.T.);
#52156=ORIENTED_EDGE('',*,*,#37332,.T.);
#52157=ORIENTED_EDGE('',*,*,#37334,.F.);
#52158=ORIENTED_EDGE('',*,*,#37335,.F.);
#52159=ORIENTED_EDGE('',*,*,#37336,.T.);
#52160=ORIENTED_EDGE('',*,*,#37335,.T.);
#52161=ORIENTED_EDGE('',*,*,#37337,.F.);
#52162=ORIENTED_EDGE('',*,*,#37338,.F.);
#52163=ORIENTED_EDGE('',*,*,#37339,.T.);
#52164=ORIENTED_EDGE('',*,*,#37338,.T.);
#52165=ORIENTED_EDGE('',*,*,#37340,.F.);
#52166=ORIENTED_EDGE('',*,*,#37341,.F.);
#52167=ORIENTED_EDGE('',*,*,#37342,.T.);
#52168=ORIENTED_EDGE('',*,*,#37341,.T.);
#52169=ORIENTED_EDGE('',*,*,#37343,.F.);
#52170=ORIENTED_EDGE('',*,*,#37344,.F.);
#52171=ORIENTED_EDGE('',*,*,#37345,.T.);
#52172=ORIENTED_EDGE('',*,*,#37344,.T.);
#52173=ORIENTED_EDGE('',*,*,#37346,.F.);
#52174=ORIENTED_EDGE('',*,*,#37347,.F.);
#52175=ORIENTED_EDGE('',*,*,#37348,.T.);
#52176=ORIENTED_EDGE('',*,*,#37347,.T.);
#52177=ORIENTED_EDGE('',*,*,#37349,.F.);
#52178=ORIENTED_EDGE('',*,*,#37350,.F.);
#52179=ORIENTED_EDGE('',*,*,#37351,.T.);
#52180=ORIENTED_EDGE('',*,*,#37350,.T.);
#52181=ORIENTED_EDGE('',*,*,#37352,.F.);
#52182=ORIENTED_EDGE('',*,*,#37353,.F.);
#52183=ORIENTED_EDGE('',*,*,#37354,.T.);
#52184=ORIENTED_EDGE('',*,*,#37353,.T.);
#52185=ORIENTED_EDGE('',*,*,#37355,.F.);
#52186=ORIENTED_EDGE('',*,*,#37356,.F.);
#52187=ORIENTED_EDGE('',*,*,#37357,.T.);
#52188=ORIENTED_EDGE('',*,*,#37356,.T.);
#52189=ORIENTED_EDGE('',*,*,#37358,.F.);
#52190=ORIENTED_EDGE('',*,*,#37359,.F.);
#52191=ORIENTED_EDGE('',*,*,#37360,.T.);
#52192=ORIENTED_EDGE('',*,*,#37359,.T.);
#52193=ORIENTED_EDGE('',*,*,#37361,.F.);
#52194=ORIENTED_EDGE('',*,*,#37362,.F.);
#52195=ORIENTED_EDGE('',*,*,#37363,.T.);
#52196=ORIENTED_EDGE('',*,*,#37362,.T.);
#52197=ORIENTED_EDGE('',*,*,#37364,.F.);
#52198=ORIENTED_EDGE('',*,*,#37365,.F.);
#52199=ORIENTED_EDGE('',*,*,#37366,.T.);
#52200=ORIENTED_EDGE('',*,*,#37365,.T.);
#52201=ORIENTED_EDGE('',*,*,#37367,.F.);
#52202=ORIENTED_EDGE('',*,*,#37368,.F.);
#52203=ORIENTED_EDGE('',*,*,#37369,.T.);
#52204=ORIENTED_EDGE('',*,*,#37368,.T.);
#52205=ORIENTED_EDGE('',*,*,#37370,.F.);
#52206=ORIENTED_EDGE('',*,*,#37371,.F.);
#52207=ORIENTED_EDGE('',*,*,#37372,.T.);
#52208=ORIENTED_EDGE('',*,*,#37371,.T.);
#52209=ORIENTED_EDGE('',*,*,#37373,.F.);
#52210=ORIENTED_EDGE('',*,*,#37374,.F.);
#52211=ORIENTED_EDGE('',*,*,#37375,.T.);
#52212=ORIENTED_EDGE('',*,*,#37374,.T.);
#52213=ORIENTED_EDGE('',*,*,#37376,.F.);
#52214=ORIENTED_EDGE('',*,*,#37377,.F.);
#52215=ORIENTED_EDGE('',*,*,#37378,.T.);
#52216=ORIENTED_EDGE('',*,*,#37377,.T.);
#52217=ORIENTED_EDGE('',*,*,#37379,.F.);
#52218=ORIENTED_EDGE('',*,*,#37380,.F.);
#52219=ORIENTED_EDGE('',*,*,#37381,.T.);
#52220=ORIENTED_EDGE('',*,*,#37380,.T.);
#52221=ORIENTED_EDGE('',*,*,#37382,.F.);
#52222=ORIENTED_EDGE('',*,*,#37383,.F.);
#52223=ORIENTED_EDGE('',*,*,#37384,.T.);
#52224=ORIENTED_EDGE('',*,*,#37383,.T.);
#52225=ORIENTED_EDGE('',*,*,#37385,.F.);
#52226=ORIENTED_EDGE('',*,*,#37386,.F.);
#52227=ORIENTED_EDGE('',*,*,#37387,.T.);
#52228=ORIENTED_EDGE('',*,*,#37386,.T.);
#52229=ORIENTED_EDGE('',*,*,#37388,.F.);
#52230=ORIENTED_EDGE('',*,*,#37389,.F.);
#52231=ORIENTED_EDGE('',*,*,#37390,.T.);
#52232=ORIENTED_EDGE('',*,*,#37389,.T.);
#52233=ORIENTED_EDGE('',*,*,#37391,.F.);
#52234=ORIENTED_EDGE('',*,*,#37392,.F.);
#52235=ORIENTED_EDGE('',*,*,#37393,.T.);
#52236=ORIENTED_EDGE('',*,*,#37392,.T.);
#52237=ORIENTED_EDGE('',*,*,#37394,.F.);
#52238=ORIENTED_EDGE('',*,*,#37395,.F.);
#52239=ORIENTED_EDGE('',*,*,#37396,.T.);
#52240=ORIENTED_EDGE('',*,*,#37395,.T.);
#52241=ORIENTED_EDGE('',*,*,#37397,.F.);
#52242=ORIENTED_EDGE('',*,*,#37398,.F.);
#52243=ORIENTED_EDGE('',*,*,#37399,.T.);
#52244=ORIENTED_EDGE('',*,*,#37398,.T.);
#52245=ORIENTED_EDGE('',*,*,#37400,.F.);
#52246=ORIENTED_EDGE('',*,*,#37401,.F.);
#52247=ORIENTED_EDGE('',*,*,#37402,.T.);
#52248=ORIENTED_EDGE('',*,*,#37401,.T.);
#52249=ORIENTED_EDGE('',*,*,#37403,.F.);
#52250=ORIENTED_EDGE('',*,*,#37404,.F.);
#52251=ORIENTED_EDGE('',*,*,#37405,.T.);
#52252=ORIENTED_EDGE('',*,*,#37404,.T.);
#52253=ORIENTED_EDGE('',*,*,#37406,.F.);
#52254=ORIENTED_EDGE('',*,*,#37407,.F.);
#52255=ORIENTED_EDGE('',*,*,#37408,.T.);
#52256=ORIENTED_EDGE('',*,*,#37407,.T.);
#52257=ORIENTED_EDGE('',*,*,#37409,.F.);
#52258=ORIENTED_EDGE('',*,*,#37410,.F.);
#52259=ORIENTED_EDGE('',*,*,#37411,.T.);
#52260=ORIENTED_EDGE('',*,*,#37410,.T.);
#52261=ORIENTED_EDGE('',*,*,#37412,.F.);
#52262=ORIENTED_EDGE('',*,*,#37413,.F.);
#52263=ORIENTED_EDGE('',*,*,#37414,.T.);
#52264=ORIENTED_EDGE('',*,*,#37413,.T.);
#52265=ORIENTED_EDGE('',*,*,#37415,.F.);
#52266=ORIENTED_EDGE('',*,*,#37416,.F.);
#52267=ORIENTED_EDGE('',*,*,#37417,.T.);
#52268=ORIENTED_EDGE('',*,*,#37416,.T.);
#52269=ORIENTED_EDGE('',*,*,#37418,.F.);
#52270=ORIENTED_EDGE('',*,*,#37419,.F.);
#52271=ORIENTED_EDGE('',*,*,#37420,.T.);
#52272=ORIENTED_EDGE('',*,*,#37419,.T.);
#52273=ORIENTED_EDGE('',*,*,#37421,.F.);
#52274=ORIENTED_EDGE('',*,*,#37422,.F.);
#52275=ORIENTED_EDGE('',*,*,#37423,.T.);
#52276=ORIENTED_EDGE('',*,*,#37422,.T.);
#52277=ORIENTED_EDGE('',*,*,#37424,.F.);
#52278=ORIENTED_EDGE('',*,*,#37425,.F.);
#52279=ORIENTED_EDGE('',*,*,#37426,.T.);
#52280=ORIENTED_EDGE('',*,*,#37425,.T.);
#52281=ORIENTED_EDGE('',*,*,#37427,.F.);
#52282=ORIENTED_EDGE('',*,*,#37428,.F.);
#52283=ORIENTED_EDGE('',*,*,#37429,.T.);
#52284=ORIENTED_EDGE('',*,*,#37428,.T.);
#52285=ORIENTED_EDGE('',*,*,#37430,.F.);
#52286=ORIENTED_EDGE('',*,*,#37431,.F.);
#52287=ORIENTED_EDGE('',*,*,#37432,.T.);
#52288=ORIENTED_EDGE('',*,*,#37431,.T.);
#52289=ORIENTED_EDGE('',*,*,#37433,.F.);
#52290=ORIENTED_EDGE('',*,*,#37434,.F.);
#52291=ORIENTED_EDGE('',*,*,#37435,.T.);
#52292=ORIENTED_EDGE('',*,*,#37434,.T.);
#52293=ORIENTED_EDGE('',*,*,#37436,.F.);
#52294=ORIENTED_EDGE('',*,*,#37437,.F.);
#52295=ORIENTED_EDGE('',*,*,#37438,.T.);
#52296=ORIENTED_EDGE('',*,*,#37437,.T.);
#52297=ORIENTED_EDGE('',*,*,#37439,.F.);
#52298=ORIENTED_EDGE('',*,*,#37440,.F.);
#52299=ORIENTED_EDGE('',*,*,#37441,.T.);
#52300=ORIENTED_EDGE('',*,*,#37440,.T.);
#52301=ORIENTED_EDGE('',*,*,#37442,.F.);
#52302=ORIENTED_EDGE('',*,*,#37443,.F.);
#52303=ORIENTED_EDGE('',*,*,#37444,.T.);
#52304=ORIENTED_EDGE('',*,*,#37443,.T.);
#52305=ORIENTED_EDGE('',*,*,#37445,.F.);
#52306=ORIENTED_EDGE('',*,*,#37446,.F.);
#52307=ORIENTED_EDGE('',*,*,#37447,.T.);
#52308=ORIENTED_EDGE('',*,*,#37446,.T.);
#52309=ORIENTED_EDGE('',*,*,#37448,.F.);
#52310=ORIENTED_EDGE('',*,*,#37449,.F.);
#52311=ORIENTED_EDGE('',*,*,#37450,.T.);
#52312=ORIENTED_EDGE('',*,*,#37449,.T.);
#52313=ORIENTED_EDGE('',*,*,#37451,.F.);
#52314=ORIENTED_EDGE('',*,*,#37452,.F.);
#52315=ORIENTED_EDGE('',*,*,#37453,.T.);
#52316=ORIENTED_EDGE('',*,*,#37452,.T.);
#52317=ORIENTED_EDGE('',*,*,#37454,.F.);
#52318=ORIENTED_EDGE('',*,*,#37455,.F.);
#52319=ORIENTED_EDGE('',*,*,#37456,.T.);
#52320=ORIENTED_EDGE('',*,*,#37455,.T.);
#52321=ORIENTED_EDGE('',*,*,#37457,.F.);
#52322=ORIENTED_EDGE('',*,*,#37458,.F.);
#52323=ORIENTED_EDGE('',*,*,#37459,.T.);
#52324=ORIENTED_EDGE('',*,*,#37458,.T.);
#52325=ORIENTED_EDGE('',*,*,#37460,.F.);
#52326=ORIENTED_EDGE('',*,*,#37461,.F.);
#52327=ORIENTED_EDGE('',*,*,#37462,.T.);
#52328=ORIENTED_EDGE('',*,*,#37461,.T.);
#52329=ORIENTED_EDGE('',*,*,#37463,.F.);
#52330=ORIENTED_EDGE('',*,*,#37464,.F.);
#52331=ORIENTED_EDGE('',*,*,#37465,.T.);
#52332=ORIENTED_EDGE('',*,*,#37464,.T.);
#52333=ORIENTED_EDGE('',*,*,#37466,.F.);
#52334=ORIENTED_EDGE('',*,*,#37467,.F.);
#52335=ORIENTED_EDGE('',*,*,#37468,.T.);
#52336=ORIENTED_EDGE('',*,*,#37467,.T.);
#52337=ORIENTED_EDGE('',*,*,#37469,.F.);
#52338=ORIENTED_EDGE('',*,*,#37470,.F.);
#52339=ORIENTED_EDGE('',*,*,#37471,.T.);
#52340=ORIENTED_EDGE('',*,*,#37470,.T.);
#52341=ORIENTED_EDGE('',*,*,#37472,.F.);
#52342=ORIENTED_EDGE('',*,*,#37473,.F.);
#52343=ORIENTED_EDGE('',*,*,#37474,.T.);
#52344=ORIENTED_EDGE('',*,*,#37473,.T.);
#52345=ORIENTED_EDGE('',*,*,#37475,.F.);
#52346=ORIENTED_EDGE('',*,*,#37476,.F.);
#52347=ORIENTED_EDGE('',*,*,#37477,.T.);
#52348=ORIENTED_EDGE('',*,*,#37476,.T.);
#52349=ORIENTED_EDGE('',*,*,#37478,.F.);
#52350=ORIENTED_EDGE('',*,*,#37479,.F.);
#52351=ORIENTED_EDGE('',*,*,#37480,.T.);
#52352=ORIENTED_EDGE('',*,*,#37479,.T.);
#52353=ORIENTED_EDGE('',*,*,#37481,.F.);
#52354=ORIENTED_EDGE('',*,*,#37482,.F.);
#52355=ORIENTED_EDGE('',*,*,#37483,.T.);
#52356=ORIENTED_EDGE('',*,*,#37482,.T.);
#52357=ORIENTED_EDGE('',*,*,#37484,.F.);
#52358=ORIENTED_EDGE('',*,*,#37485,.F.);
#52359=ORIENTED_EDGE('',*,*,#37486,.T.);
#52360=ORIENTED_EDGE('',*,*,#37485,.T.);
#52361=ORIENTED_EDGE('',*,*,#37487,.F.);
#52362=ORIENTED_EDGE('',*,*,#37488,.F.);
#52363=ORIENTED_EDGE('',*,*,#37489,.T.);
#52364=ORIENTED_EDGE('',*,*,#37488,.T.);
#52365=ORIENTED_EDGE('',*,*,#37490,.F.);
#52366=ORIENTED_EDGE('',*,*,#37491,.F.);
#52367=ORIENTED_EDGE('',*,*,#37492,.T.);
#52368=ORIENTED_EDGE('',*,*,#37491,.T.);
#52369=ORIENTED_EDGE('',*,*,#37493,.F.);
#52370=ORIENTED_EDGE('',*,*,#37494,.F.);
#52371=ORIENTED_EDGE('',*,*,#37495,.T.);
#52372=ORIENTED_EDGE('',*,*,#37494,.T.);
#52373=ORIENTED_EDGE('',*,*,#37496,.F.);
#52374=ORIENTED_EDGE('',*,*,#37497,.F.);
#52375=ORIENTED_EDGE('',*,*,#37498,.T.);
#52376=ORIENTED_EDGE('',*,*,#37497,.T.);
#52377=ORIENTED_EDGE('',*,*,#37499,.F.);
#52378=ORIENTED_EDGE('',*,*,#37500,.F.);
#52379=ORIENTED_EDGE('',*,*,#37501,.T.);
#52380=ORIENTED_EDGE('',*,*,#37500,.T.);
#52381=ORIENTED_EDGE('',*,*,#37502,.F.);
#52382=ORIENTED_EDGE('',*,*,#37503,.F.);
#52383=ORIENTED_EDGE('',*,*,#37504,.T.);
#52384=ORIENTED_EDGE('',*,*,#37503,.T.);
#52385=ORIENTED_EDGE('',*,*,#37505,.F.);
#52386=ORIENTED_EDGE('',*,*,#37506,.F.);
#52387=ORIENTED_EDGE('',*,*,#37507,.T.);
#52388=ORIENTED_EDGE('',*,*,#37506,.T.);
#52389=ORIENTED_EDGE('',*,*,#37508,.F.);
#52390=ORIENTED_EDGE('',*,*,#37509,.F.);
#52391=ORIENTED_EDGE('',*,*,#37510,.T.);
#52392=ORIENTED_EDGE('',*,*,#37509,.T.);
#52393=ORIENTED_EDGE('',*,*,#37511,.F.);
#52394=ORIENTED_EDGE('',*,*,#37512,.F.);
#52395=ORIENTED_EDGE('',*,*,#37513,.T.);
#52396=ORIENTED_EDGE('',*,*,#37512,.T.);
#52397=ORIENTED_EDGE('',*,*,#37514,.F.);
#52398=ORIENTED_EDGE('',*,*,#37515,.F.);
#52399=ORIENTED_EDGE('',*,*,#37516,.T.);
#52400=ORIENTED_EDGE('',*,*,#37515,.T.);
#52401=ORIENTED_EDGE('',*,*,#37517,.F.);
#52402=ORIENTED_EDGE('',*,*,#37518,.F.);
#52403=ORIENTED_EDGE('',*,*,#37519,.T.);
#52404=ORIENTED_EDGE('',*,*,#37518,.T.);
#52405=ORIENTED_EDGE('',*,*,#37520,.F.);
#52406=ORIENTED_EDGE('',*,*,#37521,.F.);
#52407=ORIENTED_EDGE('',*,*,#37522,.T.);
#52408=ORIENTED_EDGE('',*,*,#37521,.T.);
#52409=ORIENTED_EDGE('',*,*,#37523,.F.);
#52410=ORIENTED_EDGE('',*,*,#37524,.F.);
#52411=ORIENTED_EDGE('',*,*,#37525,.T.);
#52412=ORIENTED_EDGE('',*,*,#37524,.T.);
#52413=ORIENTED_EDGE('',*,*,#37526,.F.);
#52414=ORIENTED_EDGE('',*,*,#37527,.F.);
#52415=ORIENTED_EDGE('',*,*,#37528,.T.);
#52416=ORIENTED_EDGE('',*,*,#37527,.T.);
#52417=ORIENTED_EDGE('',*,*,#37529,.F.);
#52418=ORIENTED_EDGE('',*,*,#37530,.F.);
#52419=ORIENTED_EDGE('',*,*,#37531,.T.);
#52420=ORIENTED_EDGE('',*,*,#37530,.T.);
#52421=ORIENTED_EDGE('',*,*,#37532,.F.);
#52422=ORIENTED_EDGE('',*,*,#37533,.F.);
#52423=ORIENTED_EDGE('',*,*,#37534,.T.);
#52424=ORIENTED_EDGE('',*,*,#37533,.T.);
#52425=ORIENTED_EDGE('',*,*,#37535,.F.);
#52426=ORIENTED_EDGE('',*,*,#37536,.F.);
#52427=ORIENTED_EDGE('',*,*,#37537,.T.);
#52428=ORIENTED_EDGE('',*,*,#37536,.T.);
#52429=ORIENTED_EDGE('',*,*,#37538,.F.);
#52430=ORIENTED_EDGE('',*,*,#37539,.F.);
#52431=ORIENTED_EDGE('',*,*,#37540,.T.);
#52432=ORIENTED_EDGE('',*,*,#37539,.T.);
#52433=ORIENTED_EDGE('',*,*,#37541,.F.);
#52434=ORIENTED_EDGE('',*,*,#37542,.F.);
#52435=ORIENTED_EDGE('',*,*,#37543,.T.);
#52436=ORIENTED_EDGE('',*,*,#37542,.T.);
#52437=ORIENTED_EDGE('',*,*,#37544,.F.);
#52438=ORIENTED_EDGE('',*,*,#37545,.F.);
#52439=ORIENTED_EDGE('',*,*,#37546,.T.);
#52440=ORIENTED_EDGE('',*,*,#37545,.T.);
#52441=ORIENTED_EDGE('',*,*,#37547,.F.);
#52442=ORIENTED_EDGE('',*,*,#37548,.F.);
#52443=ORIENTED_EDGE('',*,*,#37549,.T.);
#52444=ORIENTED_EDGE('',*,*,#37548,.T.);
#52445=ORIENTED_EDGE('',*,*,#37550,.F.);
#52446=ORIENTED_EDGE('',*,*,#37551,.F.);
#52447=ORIENTED_EDGE('',*,*,#37552,.T.);
#52448=ORIENTED_EDGE('',*,*,#37551,.T.);
#52449=ORIENTED_EDGE('',*,*,#37553,.F.);
#52450=ORIENTED_EDGE('',*,*,#37554,.F.);
#52451=ORIENTED_EDGE('',*,*,#37555,.T.);
#52452=ORIENTED_EDGE('',*,*,#37554,.T.);
#52453=ORIENTED_EDGE('',*,*,#37556,.F.);
#52454=ORIENTED_EDGE('',*,*,#37557,.F.);
#52455=ORIENTED_EDGE('',*,*,#37558,.T.);
#52456=ORIENTED_EDGE('',*,*,#37557,.T.);
#52457=ORIENTED_EDGE('',*,*,#37559,.F.);
#52458=ORIENTED_EDGE('',*,*,#37560,.F.);
#52459=ORIENTED_EDGE('',*,*,#37561,.T.);
#52460=ORIENTED_EDGE('',*,*,#37560,.T.);
#52461=ORIENTED_EDGE('',*,*,#37562,.F.);
#52462=ORIENTED_EDGE('',*,*,#37563,.F.);
#52463=ORIENTED_EDGE('',*,*,#37564,.T.);
#52464=ORIENTED_EDGE('',*,*,#37563,.T.);
#52465=ORIENTED_EDGE('',*,*,#37565,.F.);
#52466=ORIENTED_EDGE('',*,*,#37566,.F.);
#52467=ORIENTED_EDGE('',*,*,#37567,.T.);
#52468=ORIENTED_EDGE('',*,*,#37566,.T.);
#52469=ORIENTED_EDGE('',*,*,#37568,.F.);
#52470=ORIENTED_EDGE('',*,*,#37569,.F.);
#52471=ORIENTED_EDGE('',*,*,#37570,.T.);
#52472=ORIENTED_EDGE('',*,*,#37569,.T.);
#52473=ORIENTED_EDGE('',*,*,#37571,.F.);
#52474=ORIENTED_EDGE('',*,*,#37572,.F.);
#52475=ORIENTED_EDGE('',*,*,#37573,.T.);
#52476=ORIENTED_EDGE('',*,*,#37572,.T.);
#52477=ORIENTED_EDGE('',*,*,#37574,.F.);
#52478=ORIENTED_EDGE('',*,*,#37575,.F.);
#52479=ORIENTED_EDGE('',*,*,#37576,.T.);
#52480=ORIENTED_EDGE('',*,*,#37575,.T.);
#52481=ORIENTED_EDGE('',*,*,#37577,.F.);
#52482=ORIENTED_EDGE('',*,*,#37578,.F.);
#52483=ORIENTED_EDGE('',*,*,#37579,.T.);
#52484=ORIENTED_EDGE('',*,*,#37578,.T.);
#52485=ORIENTED_EDGE('',*,*,#37580,.F.);
#52486=ORIENTED_EDGE('',*,*,#36055,.F.);
#52487=ORIENTED_EDGE('',*,*,#36075,.F.);
#52488=ORIENTED_EDGE('',*,*,#37581,.F.);
#52489=ORIENTED_EDGE('',*,*,#36064,.F.);
#52490=ORIENTED_EDGE('',*,*,#37582,.T.);
#52491=ORIENTED_EDGE('',*,*,#36083,.F.);
#52492=ORIENTED_EDGE('',*,*,#36081,.T.);
#52493=ORIENTED_EDGE('',*,*,#36074,.F.);
#52494=ORIENTED_EDGE('',*,*,#36080,.T.);
#52495=ORIENTED_EDGE('',*,*,#36056,.T.);
#52496=ORIENTED_EDGE('',*,*,#37580,.T.);
#52497=ORIENTED_EDGE('',*,*,#37577,.T.);
#52498=ORIENTED_EDGE('',*,*,#37574,.T.);
#52499=ORIENTED_EDGE('',*,*,#37571,.T.);
#52500=ORIENTED_EDGE('',*,*,#37568,.T.);
#52501=ORIENTED_EDGE('',*,*,#37565,.T.);
#52502=ORIENTED_EDGE('',*,*,#37562,.T.);
#52503=ORIENTED_EDGE('',*,*,#37559,.T.);
#52504=ORIENTED_EDGE('',*,*,#37556,.T.);
#52505=ORIENTED_EDGE('',*,*,#37553,.T.);
#52506=ORIENTED_EDGE('',*,*,#37550,.T.);
#52507=ORIENTED_EDGE('',*,*,#37547,.T.);
#52508=ORIENTED_EDGE('',*,*,#37544,.T.);
#52509=ORIENTED_EDGE('',*,*,#37541,.T.);
#52510=ORIENTED_EDGE('',*,*,#37538,.T.);
#52511=ORIENTED_EDGE('',*,*,#37535,.T.);
#52512=ORIENTED_EDGE('',*,*,#37532,.T.);
#52513=ORIENTED_EDGE('',*,*,#37529,.T.);
#52514=ORIENTED_EDGE('',*,*,#37526,.T.);
#52515=ORIENTED_EDGE('',*,*,#37523,.T.);
#52516=ORIENTED_EDGE('',*,*,#37520,.T.);
#52517=ORIENTED_EDGE('',*,*,#37517,.T.);
#52518=ORIENTED_EDGE('',*,*,#37514,.T.);
#52519=ORIENTED_EDGE('',*,*,#37511,.T.);
#52520=ORIENTED_EDGE('',*,*,#37508,.T.);
#52521=ORIENTED_EDGE('',*,*,#37505,.T.);
#52522=ORIENTED_EDGE('',*,*,#37502,.T.);
#52523=ORIENTED_EDGE('',*,*,#37499,.T.);
#52524=ORIENTED_EDGE('',*,*,#37496,.T.);
#52525=ORIENTED_EDGE('',*,*,#37493,.T.);
#52526=ORIENTED_EDGE('',*,*,#37490,.T.);
#52527=ORIENTED_EDGE('',*,*,#37487,.T.);
#52528=ORIENTED_EDGE('',*,*,#37484,.T.);
#52529=ORIENTED_EDGE('',*,*,#37481,.T.);
#52530=ORIENTED_EDGE('',*,*,#37478,.T.);
#52531=ORIENTED_EDGE('',*,*,#37475,.T.);
#52532=ORIENTED_EDGE('',*,*,#37472,.T.);
#52533=ORIENTED_EDGE('',*,*,#37469,.T.);
#52534=ORIENTED_EDGE('',*,*,#37466,.T.);
#52535=ORIENTED_EDGE('',*,*,#37463,.T.);
#52536=ORIENTED_EDGE('',*,*,#37460,.T.);
#52537=ORIENTED_EDGE('',*,*,#37457,.T.);
#52538=ORIENTED_EDGE('',*,*,#37454,.T.);
#52539=ORIENTED_EDGE('',*,*,#37451,.T.);
#52540=ORIENTED_EDGE('',*,*,#37448,.T.);
#52541=ORIENTED_EDGE('',*,*,#37445,.T.);
#52542=ORIENTED_EDGE('',*,*,#37442,.T.);
#52543=ORIENTED_EDGE('',*,*,#37439,.T.);
#52544=ORIENTED_EDGE('',*,*,#37436,.T.);
#52545=ORIENTED_EDGE('',*,*,#37433,.T.);
#52546=ORIENTED_EDGE('',*,*,#37430,.T.);
#52547=ORIENTED_EDGE('',*,*,#37427,.T.);
#52548=ORIENTED_EDGE('',*,*,#37424,.T.);
#52549=ORIENTED_EDGE('',*,*,#37421,.T.);
#52550=ORIENTED_EDGE('',*,*,#37418,.T.);
#52551=ORIENTED_EDGE('',*,*,#37415,.T.);
#52552=ORIENTED_EDGE('',*,*,#37412,.T.);
#52553=ORIENTED_EDGE('',*,*,#37409,.T.);
#52554=ORIENTED_EDGE('',*,*,#37406,.T.);
#52555=ORIENTED_EDGE('',*,*,#37403,.T.);
#52556=ORIENTED_EDGE('',*,*,#37400,.T.);
#52557=ORIENTED_EDGE('',*,*,#37397,.T.);
#52558=ORIENTED_EDGE('',*,*,#37394,.T.);
#52559=ORIENTED_EDGE('',*,*,#37391,.T.);
#52560=ORIENTED_EDGE('',*,*,#37388,.T.);
#52561=ORIENTED_EDGE('',*,*,#37385,.T.);
#52562=ORIENTED_EDGE('',*,*,#37382,.T.);
#52563=ORIENTED_EDGE('',*,*,#37379,.T.);
#52564=ORIENTED_EDGE('',*,*,#37376,.T.);
#52565=ORIENTED_EDGE('',*,*,#37373,.T.);
#52566=ORIENTED_EDGE('',*,*,#37370,.T.);
#52567=ORIENTED_EDGE('',*,*,#37367,.T.);
#52568=ORIENTED_EDGE('',*,*,#37364,.T.);
#52569=ORIENTED_EDGE('',*,*,#37361,.T.);
#52570=ORIENTED_EDGE('',*,*,#37358,.T.);
#52571=ORIENTED_EDGE('',*,*,#37355,.T.);
#52572=ORIENTED_EDGE('',*,*,#37352,.T.);
#52573=ORIENTED_EDGE('',*,*,#37349,.T.);
#52574=ORIENTED_EDGE('',*,*,#37346,.T.);
#52575=ORIENTED_EDGE('',*,*,#37343,.T.);
#52576=ORIENTED_EDGE('',*,*,#37340,.T.);
#52577=ORIENTED_EDGE('',*,*,#37337,.T.);
#52578=ORIENTED_EDGE('',*,*,#37334,.T.);
#52579=ORIENTED_EDGE('',*,*,#37331,.T.);
#52580=ORIENTED_EDGE('',*,*,#37328,.T.);
#52581=ORIENTED_EDGE('',*,*,#37325,.T.);
#52582=ORIENTED_EDGE('',*,*,#37322,.T.);
#52583=ORIENTED_EDGE('',*,*,#37319,.T.);
#52584=ORIENTED_EDGE('',*,*,#37316,.T.);
#52585=ORIENTED_EDGE('',*,*,#37313,.T.);
#52586=ORIENTED_EDGE('',*,*,#37310,.T.);
#52587=ORIENTED_EDGE('',*,*,#37307,.T.);
#52588=ORIENTED_EDGE('',*,*,#37304,.T.);
#52589=ORIENTED_EDGE('',*,*,#37301,.T.);
#52590=ORIENTED_EDGE('',*,*,#37298,.T.);
#52591=ORIENTED_EDGE('',*,*,#37295,.T.);
#52592=ORIENTED_EDGE('',*,*,#37292,.T.);
#52593=ORIENTED_EDGE('',*,*,#37289,.T.);
#52594=ORIENTED_EDGE('',*,*,#37286,.T.);
#52595=ORIENTED_EDGE('',*,*,#37283,.T.);
#52596=ORIENTED_EDGE('',*,*,#37280,.T.);
#52597=ORIENTED_EDGE('',*,*,#37277,.T.);
#52598=ORIENTED_EDGE('',*,*,#37274,.T.);
#52599=ORIENTED_EDGE('',*,*,#37271,.T.);
#52600=ORIENTED_EDGE('',*,*,#37268,.T.);
#52601=ORIENTED_EDGE('',*,*,#37265,.T.);
#52602=ORIENTED_EDGE('',*,*,#37262,.T.);
#52603=ORIENTED_EDGE('',*,*,#37259,.T.);
#52604=ORIENTED_EDGE('',*,*,#37256,.T.);
#52605=ORIENTED_EDGE('',*,*,#37253,.T.);
#52606=ORIENTED_EDGE('',*,*,#37250,.T.);
#52607=ORIENTED_EDGE('',*,*,#37247,.T.);
#52608=ORIENTED_EDGE('',*,*,#37244,.T.);
#52609=ORIENTED_EDGE('',*,*,#37241,.T.);
#52610=ORIENTED_EDGE('',*,*,#37238,.T.);
#52611=ORIENTED_EDGE('',*,*,#37235,.T.);
#52612=ORIENTED_EDGE('',*,*,#37232,.T.);
#52613=ORIENTED_EDGE('',*,*,#37229,.T.);
#52614=ORIENTED_EDGE('',*,*,#37226,.T.);
#52615=ORIENTED_EDGE('',*,*,#37223,.T.);
#52616=ORIENTED_EDGE('',*,*,#37220,.T.);
#52617=ORIENTED_EDGE('',*,*,#37217,.T.);
#52618=ORIENTED_EDGE('',*,*,#37214,.T.);
#52619=ORIENTED_EDGE('',*,*,#37211,.T.);
#52620=ORIENTED_EDGE('',*,*,#37208,.T.);
#52621=ORIENTED_EDGE('',*,*,#37205,.T.);
#52622=ORIENTED_EDGE('',*,*,#37202,.T.);
#52623=ORIENTED_EDGE('',*,*,#37199,.T.);
#52624=ORIENTED_EDGE('',*,*,#37196,.T.);
#52625=ORIENTED_EDGE('',*,*,#37193,.T.);
#52626=ORIENTED_EDGE('',*,*,#37190,.T.);
#52627=ORIENTED_EDGE('',*,*,#37187,.T.);
#52628=ORIENTED_EDGE('',*,*,#37184,.T.);
#52629=ORIENTED_EDGE('',*,*,#37181,.T.);
#52630=ORIENTED_EDGE('',*,*,#37178,.T.);
#52631=ORIENTED_EDGE('',*,*,#37175,.T.);
#52632=ORIENTED_EDGE('',*,*,#37172,.T.);
#52633=ORIENTED_EDGE('',*,*,#37169,.T.);
#52634=ORIENTED_EDGE('',*,*,#37166,.T.);
#52635=ORIENTED_EDGE('',*,*,#37163,.T.);
#52636=ORIENTED_EDGE('',*,*,#37160,.T.);
#52637=ORIENTED_EDGE('',*,*,#37157,.T.);
#52638=ORIENTED_EDGE('',*,*,#37154,.T.);
#52639=ORIENTED_EDGE('',*,*,#37151,.T.);
#52640=ORIENTED_EDGE('',*,*,#37148,.T.);
#52641=ORIENTED_EDGE('',*,*,#37145,.T.);
#52642=ORIENTED_EDGE('',*,*,#37142,.T.);
#52643=ORIENTED_EDGE('',*,*,#37139,.T.);
#52644=ORIENTED_EDGE('',*,*,#37136,.T.);
#52645=ORIENTED_EDGE('',*,*,#37133,.T.);
#52646=ORIENTED_EDGE('',*,*,#37130,.T.);
#52647=ORIENTED_EDGE('',*,*,#37127,.T.);
#52648=ORIENTED_EDGE('',*,*,#37124,.T.);
#52649=ORIENTED_EDGE('',*,*,#37121,.T.);
#52650=ORIENTED_EDGE('',*,*,#37118,.T.);
#52651=ORIENTED_EDGE('',*,*,#37115,.T.);
#52652=ORIENTED_EDGE('',*,*,#37112,.T.);
#52653=ORIENTED_EDGE('',*,*,#37109,.T.);
#52654=ORIENTED_EDGE('',*,*,#37106,.T.);
#52655=ORIENTED_EDGE('',*,*,#37103,.T.);
#52656=ORIENTED_EDGE('',*,*,#37100,.T.);
#52657=ORIENTED_EDGE('',*,*,#37097,.T.);
#52658=ORIENTED_EDGE('',*,*,#37094,.T.);
#52659=ORIENTED_EDGE('',*,*,#37091,.T.);
#52660=ORIENTED_EDGE('',*,*,#37088,.T.);
#52661=ORIENTED_EDGE('',*,*,#37085,.T.);
#52662=ORIENTED_EDGE('',*,*,#37082,.T.);
#52663=ORIENTED_EDGE('',*,*,#37079,.T.);
#52664=ORIENTED_EDGE('',*,*,#37076,.T.);
#52665=ORIENTED_EDGE('',*,*,#37073,.T.);
#52666=ORIENTED_EDGE('',*,*,#37070,.T.);
#52667=ORIENTED_EDGE('',*,*,#37067,.T.);
#52668=ORIENTED_EDGE('',*,*,#37064,.T.);
#52669=ORIENTED_EDGE('',*,*,#37061,.T.);
#52670=ORIENTED_EDGE('',*,*,#37058,.T.);
#52671=ORIENTED_EDGE('',*,*,#37055,.T.);
#52672=ORIENTED_EDGE('',*,*,#37052,.T.);
#52673=ORIENTED_EDGE('',*,*,#37049,.T.);
#52674=ORIENTED_EDGE('',*,*,#37046,.T.);
#52675=ORIENTED_EDGE('',*,*,#37043,.T.);
#52676=ORIENTED_EDGE('',*,*,#37040,.T.);
#52677=ORIENTED_EDGE('',*,*,#37037,.T.);
#52678=ORIENTED_EDGE('',*,*,#37034,.T.);
#52679=ORIENTED_EDGE('',*,*,#37031,.T.);
#52680=ORIENTED_EDGE('',*,*,#37028,.T.);
#52681=ORIENTED_EDGE('',*,*,#37025,.T.);
#52682=ORIENTED_EDGE('',*,*,#37022,.T.);
#52683=ORIENTED_EDGE('',*,*,#37019,.T.);
#52684=ORIENTED_EDGE('',*,*,#37016,.T.);
#52685=ORIENTED_EDGE('',*,*,#37013,.T.);
#52686=ORIENTED_EDGE('',*,*,#37010,.T.);
#52687=ORIENTED_EDGE('',*,*,#37007,.T.);
#52688=ORIENTED_EDGE('',*,*,#37004,.T.);
#52689=ORIENTED_EDGE('',*,*,#37001,.T.);
#52690=ORIENTED_EDGE('',*,*,#36998,.T.);
#52691=ORIENTED_EDGE('',*,*,#36995,.T.);
#52692=ORIENTED_EDGE('',*,*,#36992,.T.);
#52693=ORIENTED_EDGE('',*,*,#36989,.T.);
#52694=ORIENTED_EDGE('',*,*,#36986,.T.);
#52695=ORIENTED_EDGE('',*,*,#36983,.T.);
#52696=ORIENTED_EDGE('',*,*,#36980,.T.);
#52697=ORIENTED_EDGE('',*,*,#36977,.T.);
#52698=ORIENTED_EDGE('',*,*,#36974,.T.);
#52699=ORIENTED_EDGE('',*,*,#36971,.T.);
#52700=ORIENTED_EDGE('',*,*,#36968,.T.);
#52701=ORIENTED_EDGE('',*,*,#36965,.T.);
#52702=ORIENTED_EDGE('',*,*,#36962,.T.);
#52703=ORIENTED_EDGE('',*,*,#36959,.T.);
#52704=ORIENTED_EDGE('',*,*,#36956,.T.);
#52705=ORIENTED_EDGE('',*,*,#36953,.T.);
#52706=ORIENTED_EDGE('',*,*,#36950,.T.);
#52707=ORIENTED_EDGE('',*,*,#36947,.T.);
#52708=ORIENTED_EDGE('',*,*,#36944,.T.);
#52709=ORIENTED_EDGE('',*,*,#36941,.T.);
#52710=ORIENTED_EDGE('',*,*,#36938,.T.);
#52711=ORIENTED_EDGE('',*,*,#36935,.T.);
#52712=ORIENTED_EDGE('',*,*,#36932,.T.);
#52713=ORIENTED_EDGE('',*,*,#36929,.T.);
#52714=ORIENTED_EDGE('',*,*,#36926,.T.);
#52715=ORIENTED_EDGE('',*,*,#36923,.T.);
#52716=ORIENTED_EDGE('',*,*,#36920,.T.);
#52717=ORIENTED_EDGE('',*,*,#36917,.T.);
#52718=ORIENTED_EDGE('',*,*,#36914,.T.);
#52719=ORIENTED_EDGE('',*,*,#36911,.T.);
#52720=ORIENTED_EDGE('',*,*,#36908,.T.);
#52721=ORIENTED_EDGE('',*,*,#36905,.T.);
#52722=ORIENTED_EDGE('',*,*,#36902,.T.);
#52723=ORIENTED_EDGE('',*,*,#36899,.T.);
#52724=ORIENTED_EDGE('',*,*,#36896,.T.);
#52725=ORIENTED_EDGE('',*,*,#36893,.T.);
#52726=ORIENTED_EDGE('',*,*,#36890,.T.);
#52727=ORIENTED_EDGE('',*,*,#36887,.T.);
#52728=ORIENTED_EDGE('',*,*,#36884,.T.);
#52729=ORIENTED_EDGE('',*,*,#36881,.T.);
#52730=ORIENTED_EDGE('',*,*,#36878,.T.);
#52731=ORIENTED_EDGE('',*,*,#36875,.T.);
#52732=ORIENTED_EDGE('',*,*,#36872,.T.);
#52733=ORIENTED_EDGE('',*,*,#36869,.T.);
#52734=ORIENTED_EDGE('',*,*,#36866,.T.);
#52735=ORIENTED_EDGE('',*,*,#36863,.T.);
#52736=ORIENTED_EDGE('',*,*,#36860,.T.);
#52737=ORIENTED_EDGE('',*,*,#36857,.T.);
#52738=ORIENTED_EDGE('',*,*,#36854,.T.);
#52739=ORIENTED_EDGE('',*,*,#36851,.T.);
#52740=ORIENTED_EDGE('',*,*,#36848,.T.);
#52741=ORIENTED_EDGE('',*,*,#36845,.T.);
#52742=ORIENTED_EDGE('',*,*,#36842,.T.);
#52743=ORIENTED_EDGE('',*,*,#36839,.T.);
#52744=ORIENTED_EDGE('',*,*,#36836,.T.);
#52745=ORIENTED_EDGE('',*,*,#36833,.T.);
#52746=ORIENTED_EDGE('',*,*,#36830,.T.);
#52747=ORIENTED_EDGE('',*,*,#36827,.T.);
#52748=ORIENTED_EDGE('',*,*,#36824,.T.);
#52749=ORIENTED_EDGE('',*,*,#36821,.T.);
#52750=ORIENTED_EDGE('',*,*,#36818,.T.);
#52751=ORIENTED_EDGE('',*,*,#36815,.T.);
#52752=ORIENTED_EDGE('',*,*,#36812,.T.);
#52753=ORIENTED_EDGE('',*,*,#36809,.T.);
#52754=ORIENTED_EDGE('',*,*,#36806,.T.);
#52755=ORIENTED_EDGE('',*,*,#36803,.T.);
#52756=ORIENTED_EDGE('',*,*,#36800,.T.);
#52757=ORIENTED_EDGE('',*,*,#36797,.T.);
#52758=ORIENTED_EDGE('',*,*,#36794,.T.);
#52759=ORIENTED_EDGE('',*,*,#36791,.T.);
#52760=ORIENTED_EDGE('',*,*,#36788,.T.);
#52761=ORIENTED_EDGE('',*,*,#36785,.T.);
#52762=ORIENTED_EDGE('',*,*,#36782,.T.);
#52763=ORIENTED_EDGE('',*,*,#36779,.T.);
#52764=ORIENTED_EDGE('',*,*,#36776,.T.);
#52765=ORIENTED_EDGE('',*,*,#36773,.T.);
#52766=ORIENTED_EDGE('',*,*,#36770,.T.);
#52767=ORIENTED_EDGE('',*,*,#36767,.T.);
#52768=ORIENTED_EDGE('',*,*,#36764,.T.);
#52769=ORIENTED_EDGE('',*,*,#36761,.T.);
#52770=ORIENTED_EDGE('',*,*,#36758,.T.);
#52771=ORIENTED_EDGE('',*,*,#36755,.T.);
#52772=ORIENTED_EDGE('',*,*,#36752,.T.);
#52773=ORIENTED_EDGE('',*,*,#36749,.T.);
#52774=ORIENTED_EDGE('',*,*,#36746,.T.);
#52775=ORIENTED_EDGE('',*,*,#36743,.T.);
#52776=ORIENTED_EDGE('',*,*,#36740,.T.);
#52777=ORIENTED_EDGE('',*,*,#36737,.T.);
#52778=ORIENTED_EDGE('',*,*,#36734,.T.);
#52779=ORIENTED_EDGE('',*,*,#36731,.T.);
#52780=ORIENTED_EDGE('',*,*,#36728,.T.);
#52781=ORIENTED_EDGE('',*,*,#36725,.T.);
#52782=ORIENTED_EDGE('',*,*,#36722,.T.);
#52783=ORIENTED_EDGE('',*,*,#36719,.T.);
#52784=ORIENTED_EDGE('',*,*,#36716,.T.);
#52785=ORIENTED_EDGE('',*,*,#36713,.T.);
#52786=ORIENTED_EDGE('',*,*,#36710,.T.);
#52787=ORIENTED_EDGE('',*,*,#36707,.T.);
#52788=ORIENTED_EDGE('',*,*,#36704,.T.);
#52789=ORIENTED_EDGE('',*,*,#36701,.T.);
#52790=ORIENTED_EDGE('',*,*,#36698,.T.);
#52791=ORIENTED_EDGE('',*,*,#36695,.T.);
#52792=ORIENTED_EDGE('',*,*,#36692,.T.);
#52793=ORIENTED_EDGE('',*,*,#36689,.T.);
#52794=ORIENTED_EDGE('',*,*,#36686,.T.);
#52795=ORIENTED_EDGE('',*,*,#36683,.T.);
#52796=ORIENTED_EDGE('',*,*,#36680,.T.);
#52797=ORIENTED_EDGE('',*,*,#36677,.T.);
#52798=ORIENTED_EDGE('',*,*,#36674,.T.);
#52799=ORIENTED_EDGE('',*,*,#36671,.T.);
#52800=ORIENTED_EDGE('',*,*,#36668,.T.);
#52801=ORIENTED_EDGE('',*,*,#36665,.T.);
#52802=ORIENTED_EDGE('',*,*,#36662,.T.);
#52803=ORIENTED_EDGE('',*,*,#36659,.T.);
#52804=ORIENTED_EDGE('',*,*,#36656,.T.);
#52805=ORIENTED_EDGE('',*,*,#36653,.T.);
#52806=ORIENTED_EDGE('',*,*,#36650,.T.);
#52807=ORIENTED_EDGE('',*,*,#36647,.T.);
#52808=ORIENTED_EDGE('',*,*,#36644,.T.);
#52809=ORIENTED_EDGE('',*,*,#36641,.T.);
#52810=ORIENTED_EDGE('',*,*,#36638,.T.);
#52811=ORIENTED_EDGE('',*,*,#36635,.T.);
#52812=ORIENTED_EDGE('',*,*,#36632,.T.);
#52813=ORIENTED_EDGE('',*,*,#36629,.T.);
#52814=ORIENTED_EDGE('',*,*,#36626,.T.);
#52815=ORIENTED_EDGE('',*,*,#36623,.T.);
#52816=ORIENTED_EDGE('',*,*,#36620,.T.);
#52817=ORIENTED_EDGE('',*,*,#36617,.T.);
#52818=ORIENTED_EDGE('',*,*,#36614,.T.);
#52819=ORIENTED_EDGE('',*,*,#36611,.T.);
#52820=ORIENTED_EDGE('',*,*,#36608,.T.);
#52821=ORIENTED_EDGE('',*,*,#36605,.T.);
#52822=ORIENTED_EDGE('',*,*,#36602,.T.);
#52823=ORIENTED_EDGE('',*,*,#36599,.T.);
#52824=ORIENTED_EDGE('',*,*,#36596,.T.);
#52825=ORIENTED_EDGE('',*,*,#36593,.T.);
#52826=ORIENTED_EDGE('',*,*,#36590,.T.);
#52827=ORIENTED_EDGE('',*,*,#36587,.T.);
#52828=ORIENTED_EDGE('',*,*,#36584,.T.);
#52829=ORIENTED_EDGE('',*,*,#36581,.T.);
#52830=ORIENTED_EDGE('',*,*,#36578,.T.);
#52831=ORIENTED_EDGE('',*,*,#36575,.T.);
#52832=ORIENTED_EDGE('',*,*,#36572,.T.);
#52833=ORIENTED_EDGE('',*,*,#36569,.T.);
#52834=ORIENTED_EDGE('',*,*,#36566,.T.);
#52835=ORIENTED_EDGE('',*,*,#36563,.T.);
#52836=ORIENTED_EDGE('',*,*,#36560,.T.);
#52837=ORIENTED_EDGE('',*,*,#36557,.T.);
#52838=ORIENTED_EDGE('',*,*,#36554,.T.);
#52839=ORIENTED_EDGE('',*,*,#36551,.T.);
#52840=ORIENTED_EDGE('',*,*,#36548,.T.);
#52841=ORIENTED_EDGE('',*,*,#36545,.T.);
#52842=ORIENTED_EDGE('',*,*,#36542,.T.);
#52843=ORIENTED_EDGE('',*,*,#36539,.T.);
#52844=ORIENTED_EDGE('',*,*,#36536,.T.);
#52845=ORIENTED_EDGE('',*,*,#36533,.T.);
#52846=ORIENTED_EDGE('',*,*,#36530,.T.);
#52847=ORIENTED_EDGE('',*,*,#36527,.T.);
#52848=ORIENTED_EDGE('',*,*,#36524,.T.);
#52849=ORIENTED_EDGE('',*,*,#36521,.T.);
#52850=ORIENTED_EDGE('',*,*,#36518,.T.);
#52851=ORIENTED_EDGE('',*,*,#36515,.T.);
#52852=ORIENTED_EDGE('',*,*,#36512,.T.);
#52853=ORIENTED_EDGE('',*,*,#36509,.T.);
#52854=ORIENTED_EDGE('',*,*,#36506,.T.);
#52855=ORIENTED_EDGE('',*,*,#36503,.T.);
#52856=ORIENTED_EDGE('',*,*,#36500,.T.);
#52857=ORIENTED_EDGE('',*,*,#36497,.T.);
#52858=ORIENTED_EDGE('',*,*,#36494,.T.);
#52859=ORIENTED_EDGE('',*,*,#36491,.T.);
#52860=ORIENTED_EDGE('',*,*,#36488,.T.);
#52861=ORIENTED_EDGE('',*,*,#36485,.T.);
#52862=ORIENTED_EDGE('',*,*,#36482,.T.);
#52863=ORIENTED_EDGE('',*,*,#36479,.T.);
#52864=ORIENTED_EDGE('',*,*,#36476,.T.);
#52865=ORIENTED_EDGE('',*,*,#36473,.T.);
#52866=ORIENTED_EDGE('',*,*,#36470,.T.);
#52867=ORIENTED_EDGE('',*,*,#36467,.T.);
#52868=ORIENTED_EDGE('',*,*,#36464,.T.);
#52869=ORIENTED_EDGE('',*,*,#36461,.T.);
#52870=ORIENTED_EDGE('',*,*,#36458,.T.);
#52871=ORIENTED_EDGE('',*,*,#36455,.T.);
#52872=ORIENTED_EDGE('',*,*,#36452,.T.);
#52873=ORIENTED_EDGE('',*,*,#36449,.T.);
#52874=ORIENTED_EDGE('',*,*,#36446,.T.);
#52875=ORIENTED_EDGE('',*,*,#36443,.T.);
#52876=ORIENTED_EDGE('',*,*,#36440,.T.);
#52877=ORIENTED_EDGE('',*,*,#36437,.T.);
#52878=ORIENTED_EDGE('',*,*,#36434,.T.);
#52879=ORIENTED_EDGE('',*,*,#36431,.T.);
#52880=ORIENTED_EDGE('',*,*,#36428,.T.);
#52881=ORIENTED_EDGE('',*,*,#36425,.T.);
#52882=ORIENTED_EDGE('',*,*,#36422,.T.);
#52883=ORIENTED_EDGE('',*,*,#36419,.T.);
#52884=ORIENTED_EDGE('',*,*,#36416,.T.);
#52885=ORIENTED_EDGE('',*,*,#36413,.T.);
#52886=ORIENTED_EDGE('',*,*,#36410,.T.);
#52887=ORIENTED_EDGE('',*,*,#36407,.T.);
#52888=ORIENTED_EDGE('',*,*,#36404,.T.);
#52889=ORIENTED_EDGE('',*,*,#36401,.T.);
#52890=ORIENTED_EDGE('',*,*,#36398,.T.);
#52891=ORIENTED_EDGE('',*,*,#36395,.T.);
#52892=ORIENTED_EDGE('',*,*,#36392,.T.);
#52893=ORIENTED_EDGE('',*,*,#36389,.T.);
#52894=ORIENTED_EDGE('',*,*,#36386,.T.);
#52895=ORIENTED_EDGE('',*,*,#36383,.T.);
#52896=ORIENTED_EDGE('',*,*,#36380,.T.);
#52897=ORIENTED_EDGE('',*,*,#36377,.T.);
#52898=ORIENTED_EDGE('',*,*,#36374,.T.);
#52899=ORIENTED_EDGE('',*,*,#36371,.T.);
#52900=ORIENTED_EDGE('',*,*,#36368,.T.);
#52901=ORIENTED_EDGE('',*,*,#36365,.T.);
#52902=ORIENTED_EDGE('',*,*,#36362,.T.);
#52903=ORIENTED_EDGE('',*,*,#36359,.T.);
#52904=ORIENTED_EDGE('',*,*,#36356,.T.);
#52905=ORIENTED_EDGE('',*,*,#36353,.T.);
#52906=ORIENTED_EDGE('',*,*,#36350,.T.);
#52907=ORIENTED_EDGE('',*,*,#36347,.T.);
#52908=ORIENTED_EDGE('',*,*,#36344,.T.);
#52909=ORIENTED_EDGE('',*,*,#36341,.T.);
#52910=ORIENTED_EDGE('',*,*,#36338,.T.);
#52911=ORIENTED_EDGE('',*,*,#36335,.T.);
#52912=ORIENTED_EDGE('',*,*,#36332,.T.);
#52913=ORIENTED_EDGE('',*,*,#36329,.T.);
#52914=ORIENTED_EDGE('',*,*,#36326,.T.);
#52915=ORIENTED_EDGE('',*,*,#36323,.T.);
#52916=ORIENTED_EDGE('',*,*,#36320,.T.);
#52917=ORIENTED_EDGE('',*,*,#36317,.T.);
#52918=ORIENTED_EDGE('',*,*,#36314,.T.);
#52919=ORIENTED_EDGE('',*,*,#36311,.T.);
#52920=ORIENTED_EDGE('',*,*,#36308,.T.);
#52921=ORIENTED_EDGE('',*,*,#36305,.T.);
#52922=ORIENTED_EDGE('',*,*,#36302,.T.);
#52923=ORIENTED_EDGE('',*,*,#36299,.T.);
#52924=ORIENTED_EDGE('',*,*,#36296,.T.);
#52925=ORIENTED_EDGE('',*,*,#36293,.T.);
#52926=ORIENTED_EDGE('',*,*,#36290,.T.);
#52927=ORIENTED_EDGE('',*,*,#36287,.T.);
#52928=ORIENTED_EDGE('',*,*,#36284,.T.);
#52929=ORIENTED_EDGE('',*,*,#36281,.T.);
#52930=ORIENTED_EDGE('',*,*,#36278,.T.);
#52931=ORIENTED_EDGE('',*,*,#36275,.T.);
#52932=ORIENTED_EDGE('',*,*,#36272,.T.);
#52933=ORIENTED_EDGE('',*,*,#36269,.T.);
#52934=ORIENTED_EDGE('',*,*,#36266,.T.);
#52935=ORIENTED_EDGE('',*,*,#36263,.T.);
#52936=ORIENTED_EDGE('',*,*,#36260,.T.);
#52937=ORIENTED_EDGE('',*,*,#36257,.T.);
#52938=ORIENTED_EDGE('',*,*,#36254,.T.);
#52939=ORIENTED_EDGE('',*,*,#36251,.T.);
#52940=ORIENTED_EDGE('',*,*,#36248,.T.);
#52941=ORIENTED_EDGE('',*,*,#36245,.T.);
#52942=ORIENTED_EDGE('',*,*,#36242,.T.);
#52943=ORIENTED_EDGE('',*,*,#36239,.T.);
#52944=ORIENTED_EDGE('',*,*,#36236,.T.);
#52945=ORIENTED_EDGE('',*,*,#36233,.T.);
#52946=ORIENTED_EDGE('',*,*,#36230,.T.);
#52947=ORIENTED_EDGE('',*,*,#36227,.T.);
#52948=ORIENTED_EDGE('',*,*,#36224,.T.);
#52949=ORIENTED_EDGE('',*,*,#36221,.T.);
#52950=ORIENTED_EDGE('',*,*,#36218,.T.);
#52951=ORIENTED_EDGE('',*,*,#36215,.T.);
#52952=ORIENTED_EDGE('',*,*,#36212,.T.);
#52953=ORIENTED_EDGE('',*,*,#36209,.T.);
#52954=ORIENTED_EDGE('',*,*,#36206,.T.);
#52955=ORIENTED_EDGE('',*,*,#36203,.T.);
#52956=ORIENTED_EDGE('',*,*,#36200,.T.);
#52957=ORIENTED_EDGE('',*,*,#36197,.T.);
#52958=ORIENTED_EDGE('',*,*,#36194,.T.);
#52959=ORIENTED_EDGE('',*,*,#36191,.T.);
#52960=ORIENTED_EDGE('',*,*,#36188,.T.);
#52961=ORIENTED_EDGE('',*,*,#36185,.T.);
#52962=ORIENTED_EDGE('',*,*,#36182,.T.);
#52963=ORIENTED_EDGE('',*,*,#36179,.T.);
#52964=ORIENTED_EDGE('',*,*,#36176,.T.);
#52965=ORIENTED_EDGE('',*,*,#36173,.T.);
#52966=ORIENTED_EDGE('',*,*,#36170,.T.);
#52967=ORIENTED_EDGE('',*,*,#36167,.T.);
#52968=ORIENTED_EDGE('',*,*,#36164,.T.);
#52969=ORIENTED_EDGE('',*,*,#36161,.T.);
#52970=ORIENTED_EDGE('',*,*,#36158,.T.);
#52971=ORIENTED_EDGE('',*,*,#36155,.T.);
#52972=ORIENTED_EDGE('',*,*,#36152,.T.);
#52973=ORIENTED_EDGE('',*,*,#36149,.T.);
#52974=ORIENTED_EDGE('',*,*,#36146,.T.);
#52975=ORIENTED_EDGE('',*,*,#36143,.T.);
#52976=ORIENTED_EDGE('',*,*,#36140,.T.);
#52977=ORIENTED_EDGE('',*,*,#36137,.T.);
#52978=ORIENTED_EDGE('',*,*,#36134,.T.);
#52979=ORIENTED_EDGE('',*,*,#36131,.T.);
#52980=ORIENTED_EDGE('',*,*,#36128,.T.);
#52981=ORIENTED_EDGE('',*,*,#36125,.T.);
#52982=ORIENTED_EDGE('',*,*,#36122,.T.);
#52983=ORIENTED_EDGE('',*,*,#36119,.T.);
#52984=ORIENTED_EDGE('',*,*,#36116,.T.);
#52985=ORIENTED_EDGE('',*,*,#36113,.T.);
#52986=ORIENTED_EDGE('',*,*,#36110,.T.);
#52987=ORIENTED_EDGE('',*,*,#36107,.T.);
#52988=ORIENTED_EDGE('',*,*,#36104,.T.);
#52989=ORIENTED_EDGE('',*,*,#36101,.T.);
#52990=ORIENTED_EDGE('',*,*,#36098,.T.);
#52991=ORIENTED_EDGE('',*,*,#36095,.T.);
#52992=ORIENTED_EDGE('',*,*,#36092,.T.);
#52993=ORIENTED_EDGE('',*,*,#36089,.T.);
#52994=ORIENTED_EDGE('',*,*,#36086,.T.);
#52995=ORIENTED_EDGE('',*,*,#36065,.T.);
#52996=ORIENTED_EDGE('',*,*,#37581,.T.);
#52997=ORIENTED_EDGE('',*,*,#36084,.F.);
#52998=ORIENTED_EDGE('',*,*,#37582,.F.);
#52999=ORIENTED_EDGE('',*,*,#36063,.F.);
#53000=ORIENTED_EDGE('',*,*,#36085,.F.);
#53001=ORIENTED_EDGE('',*,*,#36088,.F.);
#53002=ORIENTED_EDGE('',*,*,#36091,.F.);
#53003=ORIENTED_EDGE('',*,*,#36094,.F.);
#53004=ORIENTED_EDGE('',*,*,#36097,.F.);
#53005=ORIENTED_EDGE('',*,*,#36100,.F.);
#53006=ORIENTED_EDGE('',*,*,#36103,.F.);
#53007=ORIENTED_EDGE('',*,*,#36106,.F.);
#53008=ORIENTED_EDGE('',*,*,#36109,.F.);
#53009=ORIENTED_EDGE('',*,*,#36112,.F.);
#53010=ORIENTED_EDGE('',*,*,#36115,.F.);
#53011=ORIENTED_EDGE('',*,*,#36118,.F.);
#53012=ORIENTED_EDGE('',*,*,#36121,.F.);
#53013=ORIENTED_EDGE('',*,*,#36124,.F.);
#53014=ORIENTED_EDGE('',*,*,#36127,.F.);
#53015=ORIENTED_EDGE('',*,*,#36130,.F.);
#53016=ORIENTED_EDGE('',*,*,#36133,.F.);
#53017=ORIENTED_EDGE('',*,*,#36136,.F.);
#53018=ORIENTED_EDGE('',*,*,#36139,.F.);
#53019=ORIENTED_EDGE('',*,*,#36142,.F.);
#53020=ORIENTED_EDGE('',*,*,#36145,.F.);
#53021=ORIENTED_EDGE('',*,*,#36148,.F.);
#53022=ORIENTED_EDGE('',*,*,#36151,.F.);
#53023=ORIENTED_EDGE('',*,*,#36154,.F.);
#53024=ORIENTED_EDGE('',*,*,#36157,.F.);
#53025=ORIENTED_EDGE('',*,*,#36160,.F.);
#53026=ORIENTED_EDGE('',*,*,#36163,.F.);
#53027=ORIENTED_EDGE('',*,*,#36166,.F.);
#53028=ORIENTED_EDGE('',*,*,#36169,.F.);
#53029=ORIENTED_EDGE('',*,*,#36172,.F.);
#53030=ORIENTED_EDGE('',*,*,#36175,.F.);
#53031=ORIENTED_EDGE('',*,*,#36178,.F.);
#53032=ORIENTED_EDGE('',*,*,#36181,.F.);
#53033=ORIENTED_EDGE('',*,*,#36184,.F.);
#53034=ORIENTED_EDGE('',*,*,#36187,.F.);
#53035=ORIENTED_EDGE('',*,*,#36190,.F.);
#53036=ORIENTED_EDGE('',*,*,#36193,.F.);
#53037=ORIENTED_EDGE('',*,*,#36196,.F.);
#53038=ORIENTED_EDGE('',*,*,#36199,.F.);
#53039=ORIENTED_EDGE('',*,*,#36202,.F.);
#53040=ORIENTED_EDGE('',*,*,#36205,.F.);
#53041=ORIENTED_EDGE('',*,*,#36208,.F.);
#53042=ORIENTED_EDGE('',*,*,#36211,.F.);
#53043=ORIENTED_EDGE('',*,*,#36214,.F.);
#53044=ORIENTED_EDGE('',*,*,#36217,.F.);
#53045=ORIENTED_EDGE('',*,*,#36220,.F.);
#53046=ORIENTED_EDGE('',*,*,#36223,.F.);
#53047=ORIENTED_EDGE('',*,*,#36226,.F.);
#53048=ORIENTED_EDGE('',*,*,#36229,.F.);
#53049=ORIENTED_EDGE('',*,*,#36232,.F.);
#53050=ORIENTED_EDGE('',*,*,#36235,.F.);
#53051=ORIENTED_EDGE('',*,*,#36238,.F.);
#53052=ORIENTED_EDGE('',*,*,#36241,.F.);
#53053=ORIENTED_EDGE('',*,*,#36244,.F.);
#53054=ORIENTED_EDGE('',*,*,#36247,.F.);
#53055=ORIENTED_EDGE('',*,*,#36250,.F.);
#53056=ORIENTED_EDGE('',*,*,#36253,.F.);
#53057=ORIENTED_EDGE('',*,*,#36256,.F.);
#53058=ORIENTED_EDGE('',*,*,#36259,.F.);
#53059=ORIENTED_EDGE('',*,*,#36262,.F.);
#53060=ORIENTED_EDGE('',*,*,#36265,.F.);
#53061=ORIENTED_EDGE('',*,*,#36268,.F.);
#53062=ORIENTED_EDGE('',*,*,#36271,.F.);
#53063=ORIENTED_EDGE('',*,*,#36274,.F.);
#53064=ORIENTED_EDGE('',*,*,#36277,.F.);
#53065=ORIENTED_EDGE('',*,*,#36280,.F.);
#53066=ORIENTED_EDGE('',*,*,#36283,.F.);
#53067=ORIENTED_EDGE('',*,*,#36286,.F.);
#53068=ORIENTED_EDGE('',*,*,#36289,.F.);
#53069=ORIENTED_EDGE('',*,*,#36292,.F.);
#53070=ORIENTED_EDGE('',*,*,#36295,.F.);
#53071=ORIENTED_EDGE('',*,*,#36298,.F.);
#53072=ORIENTED_EDGE('',*,*,#36301,.F.);
#53073=ORIENTED_EDGE('',*,*,#36304,.F.);
#53074=ORIENTED_EDGE('',*,*,#36307,.F.);
#53075=ORIENTED_EDGE('',*,*,#36310,.F.);
#53076=ORIENTED_EDGE('',*,*,#36313,.F.);
#53077=ORIENTED_EDGE('',*,*,#36316,.F.);
#53078=ORIENTED_EDGE('',*,*,#36319,.F.);
#53079=ORIENTED_EDGE('',*,*,#36322,.F.);
#53080=ORIENTED_EDGE('',*,*,#36325,.F.);
#53081=ORIENTED_EDGE('',*,*,#36328,.F.);
#53082=ORIENTED_EDGE('',*,*,#36331,.F.);
#53083=ORIENTED_EDGE('',*,*,#36334,.F.);
#53084=ORIENTED_EDGE('',*,*,#36337,.F.);
#53085=ORIENTED_EDGE('',*,*,#36340,.F.);
#53086=ORIENTED_EDGE('',*,*,#36343,.F.);
#53087=ORIENTED_EDGE('',*,*,#36346,.F.);
#53088=ORIENTED_EDGE('',*,*,#36349,.F.);
#53089=ORIENTED_EDGE('',*,*,#36352,.F.);
#53090=ORIENTED_EDGE('',*,*,#36355,.F.);
#53091=ORIENTED_EDGE('',*,*,#36358,.F.);
#53092=ORIENTED_EDGE('',*,*,#36361,.F.);
#53093=ORIENTED_EDGE('',*,*,#36364,.F.);
#53094=ORIENTED_EDGE('',*,*,#36367,.F.);
#53095=ORIENTED_EDGE('',*,*,#36370,.F.);
#53096=ORIENTED_EDGE('',*,*,#36373,.F.);
#53097=ORIENTED_EDGE('',*,*,#36376,.F.);
#53098=ORIENTED_EDGE('',*,*,#36379,.F.);
#53099=ORIENTED_EDGE('',*,*,#36382,.F.);
#53100=ORIENTED_EDGE('',*,*,#36385,.F.);
#53101=ORIENTED_EDGE('',*,*,#36388,.F.);
#53102=ORIENTED_EDGE('',*,*,#36391,.F.);
#53103=ORIENTED_EDGE('',*,*,#36394,.F.);
#53104=ORIENTED_EDGE('',*,*,#36397,.F.);
#53105=ORIENTED_EDGE('',*,*,#36400,.F.);
#53106=ORIENTED_EDGE('',*,*,#36403,.F.);
#53107=ORIENTED_EDGE('',*,*,#36406,.F.);
#53108=ORIENTED_EDGE('',*,*,#36409,.F.);
#53109=ORIENTED_EDGE('',*,*,#36412,.F.);
#53110=ORIENTED_EDGE('',*,*,#36415,.F.);
#53111=ORIENTED_EDGE('',*,*,#36418,.F.);
#53112=ORIENTED_EDGE('',*,*,#36421,.F.);
#53113=ORIENTED_EDGE('',*,*,#36424,.F.);
#53114=ORIENTED_EDGE('',*,*,#36427,.F.);
#53115=ORIENTED_EDGE('',*,*,#36430,.F.);
#53116=ORIENTED_EDGE('',*,*,#36433,.F.);
#53117=ORIENTED_EDGE('',*,*,#36436,.F.);
#53118=ORIENTED_EDGE('',*,*,#36439,.F.);
#53119=ORIENTED_EDGE('',*,*,#36442,.F.);
#53120=ORIENTED_EDGE('',*,*,#36445,.F.);
#53121=ORIENTED_EDGE('',*,*,#36448,.F.);
#53122=ORIENTED_EDGE('',*,*,#36451,.F.);
#53123=ORIENTED_EDGE('',*,*,#36454,.F.);
#53124=ORIENTED_EDGE('',*,*,#36457,.F.);
#53125=ORIENTED_EDGE('',*,*,#36460,.F.);
#53126=ORIENTED_EDGE('',*,*,#36463,.F.);
#53127=ORIENTED_EDGE('',*,*,#36466,.F.);
#53128=ORIENTED_EDGE('',*,*,#36469,.F.);
#53129=ORIENTED_EDGE('',*,*,#36472,.F.);
#53130=ORIENTED_EDGE('',*,*,#36475,.F.);
#53131=ORIENTED_EDGE('',*,*,#36478,.F.);
#53132=ORIENTED_EDGE('',*,*,#36481,.F.);
#53133=ORIENTED_EDGE('',*,*,#36484,.F.);
#53134=ORIENTED_EDGE('',*,*,#36487,.F.);
#53135=ORIENTED_EDGE('',*,*,#36490,.F.);
#53136=ORIENTED_EDGE('',*,*,#36493,.F.);
#53137=ORIENTED_EDGE('',*,*,#36496,.F.);
#53138=ORIENTED_EDGE('',*,*,#36499,.F.);
#53139=ORIENTED_EDGE('',*,*,#36502,.F.);
#53140=ORIENTED_EDGE('',*,*,#36505,.F.);
#53141=ORIENTED_EDGE('',*,*,#36508,.F.);
#53142=ORIENTED_EDGE('',*,*,#36511,.F.);
#53143=ORIENTED_EDGE('',*,*,#36514,.F.);
#53144=ORIENTED_EDGE('',*,*,#36517,.F.);
#53145=ORIENTED_EDGE('',*,*,#36520,.F.);
#53146=ORIENTED_EDGE('',*,*,#36523,.F.);
#53147=ORIENTED_EDGE('',*,*,#36526,.F.);
#53148=ORIENTED_EDGE('',*,*,#36529,.F.);
#53149=ORIENTED_EDGE('',*,*,#36532,.F.);
#53150=ORIENTED_EDGE('',*,*,#36535,.F.);
#53151=ORIENTED_EDGE('',*,*,#36538,.F.);
#53152=ORIENTED_EDGE('',*,*,#36541,.F.);
#53153=ORIENTED_EDGE('',*,*,#36544,.F.);
#53154=ORIENTED_EDGE('',*,*,#36547,.F.);
#53155=ORIENTED_EDGE('',*,*,#36550,.F.);
#53156=ORIENTED_EDGE('',*,*,#36553,.F.);
#53157=ORIENTED_EDGE('',*,*,#36556,.F.);
#53158=ORIENTED_EDGE('',*,*,#36559,.F.);
#53159=ORIENTED_EDGE('',*,*,#36562,.F.);
#53160=ORIENTED_EDGE('',*,*,#36565,.F.);
#53161=ORIENTED_EDGE('',*,*,#36568,.F.);
#53162=ORIENTED_EDGE('',*,*,#36571,.F.);
#53163=ORIENTED_EDGE('',*,*,#36574,.F.);
#53164=ORIENTED_EDGE('',*,*,#36577,.F.);
#53165=ORIENTED_EDGE('',*,*,#36580,.F.);
#53166=ORIENTED_EDGE('',*,*,#36583,.F.);
#53167=ORIENTED_EDGE('',*,*,#36586,.F.);
#53168=ORIENTED_EDGE('',*,*,#36589,.F.);
#53169=ORIENTED_EDGE('',*,*,#36592,.F.);
#53170=ORIENTED_EDGE('',*,*,#36595,.F.);
#53171=ORIENTED_EDGE('',*,*,#36598,.F.);
#53172=ORIENTED_EDGE('',*,*,#36601,.F.);
#53173=ORIENTED_EDGE('',*,*,#36604,.F.);
#53174=ORIENTED_EDGE('',*,*,#36607,.F.);
#53175=ORIENTED_EDGE('',*,*,#36610,.F.);
#53176=ORIENTED_EDGE('',*,*,#36613,.F.);
#53177=ORIENTED_EDGE('',*,*,#36616,.F.);
#53178=ORIENTED_EDGE('',*,*,#36619,.F.);
#53179=ORIENTED_EDGE('',*,*,#36622,.F.);
#53180=ORIENTED_EDGE('',*,*,#36625,.F.);
#53181=ORIENTED_EDGE('',*,*,#36628,.F.);
#53182=ORIENTED_EDGE('',*,*,#36631,.F.);
#53183=ORIENTED_EDGE('',*,*,#36634,.F.);
#53184=ORIENTED_EDGE('',*,*,#36637,.F.);
#53185=ORIENTED_EDGE('',*,*,#36640,.F.);
#53186=ORIENTED_EDGE('',*,*,#36643,.F.);
#53187=ORIENTED_EDGE('',*,*,#36646,.F.);
#53188=ORIENTED_EDGE('',*,*,#36649,.F.);
#53189=ORIENTED_EDGE('',*,*,#36652,.F.);
#53190=ORIENTED_EDGE('',*,*,#36655,.F.);
#53191=ORIENTED_EDGE('',*,*,#36658,.F.);
#53192=ORIENTED_EDGE('',*,*,#36661,.F.);
#53193=ORIENTED_EDGE('',*,*,#36664,.F.);
#53194=ORIENTED_EDGE('',*,*,#36667,.F.);
#53195=ORIENTED_EDGE('',*,*,#36670,.F.);
#53196=ORIENTED_EDGE('',*,*,#36673,.F.);
#53197=ORIENTED_EDGE('',*,*,#36676,.F.);
#53198=ORIENTED_EDGE('',*,*,#36679,.F.);
#53199=ORIENTED_EDGE('',*,*,#36682,.F.);
#53200=ORIENTED_EDGE('',*,*,#36685,.F.);
#53201=ORIENTED_EDGE('',*,*,#36688,.F.);
#53202=ORIENTED_EDGE('',*,*,#36691,.F.);
#53203=ORIENTED_EDGE('',*,*,#36694,.F.);
#53204=ORIENTED_EDGE('',*,*,#36697,.F.);
#53205=ORIENTED_EDGE('',*,*,#36700,.F.);
#53206=ORIENTED_EDGE('',*,*,#36703,.F.);
#53207=ORIENTED_EDGE('',*,*,#36706,.F.);
#53208=ORIENTED_EDGE('',*,*,#36709,.F.);
#53209=ORIENTED_EDGE('',*,*,#36712,.F.);
#53210=ORIENTED_EDGE('',*,*,#36715,.F.);
#53211=ORIENTED_EDGE('',*,*,#36718,.F.);
#53212=ORIENTED_EDGE('',*,*,#36721,.F.);
#53213=ORIENTED_EDGE('',*,*,#36724,.F.);
#53214=ORIENTED_EDGE('',*,*,#36727,.F.);
#53215=ORIENTED_EDGE('',*,*,#36730,.F.);
#53216=ORIENTED_EDGE('',*,*,#36733,.F.);
#53217=ORIENTED_EDGE('',*,*,#36736,.F.);
#53218=ORIENTED_EDGE('',*,*,#36739,.F.);
#53219=ORIENTED_EDGE('',*,*,#36742,.F.);
#53220=ORIENTED_EDGE('',*,*,#36745,.F.);
#53221=ORIENTED_EDGE('',*,*,#36748,.F.);
#53222=ORIENTED_EDGE('',*,*,#36751,.F.);
#53223=ORIENTED_EDGE('',*,*,#36754,.F.);
#53224=ORIENTED_EDGE('',*,*,#36757,.F.);
#53225=ORIENTED_EDGE('',*,*,#36760,.F.);
#53226=ORIENTED_EDGE('',*,*,#36763,.F.);
#53227=ORIENTED_EDGE('',*,*,#36766,.F.);
#53228=ORIENTED_EDGE('',*,*,#36769,.F.);
#53229=ORIENTED_EDGE('',*,*,#36772,.F.);
#53230=ORIENTED_EDGE('',*,*,#36775,.F.);
#53231=ORIENTED_EDGE('',*,*,#36778,.F.);
#53232=ORIENTED_EDGE('',*,*,#36781,.F.);
#53233=ORIENTED_EDGE('',*,*,#36784,.F.);
#53234=ORIENTED_EDGE('',*,*,#36787,.F.);
#53235=ORIENTED_EDGE('',*,*,#36790,.F.);
#53236=ORIENTED_EDGE('',*,*,#36793,.F.);
#53237=ORIENTED_EDGE('',*,*,#36796,.F.);
#53238=ORIENTED_EDGE('',*,*,#36799,.F.);
#53239=ORIENTED_EDGE('',*,*,#36802,.F.);
#53240=ORIENTED_EDGE('',*,*,#36805,.F.);
#53241=ORIENTED_EDGE('',*,*,#36808,.F.);
#53242=ORIENTED_EDGE('',*,*,#36811,.F.);
#53243=ORIENTED_EDGE('',*,*,#36814,.F.);
#53244=ORIENTED_EDGE('',*,*,#36817,.F.);
#53245=ORIENTED_EDGE('',*,*,#36820,.F.);
#53246=ORIENTED_EDGE('',*,*,#36823,.F.);
#53247=ORIENTED_EDGE('',*,*,#36826,.F.);
#53248=ORIENTED_EDGE('',*,*,#36829,.F.);
#53249=ORIENTED_EDGE('',*,*,#36832,.F.);
#53250=ORIENTED_EDGE('',*,*,#36835,.F.);
#53251=ORIENTED_EDGE('',*,*,#36838,.F.);
#53252=ORIENTED_EDGE('',*,*,#36841,.F.);
#53253=ORIENTED_EDGE('',*,*,#36844,.F.);
#53254=ORIENTED_EDGE('',*,*,#36847,.F.);
#53255=ORIENTED_EDGE('',*,*,#36850,.F.);
#53256=ORIENTED_EDGE('',*,*,#36853,.F.);
#53257=ORIENTED_EDGE('',*,*,#36856,.F.);
#53258=ORIENTED_EDGE('',*,*,#36859,.F.);
#53259=ORIENTED_EDGE('',*,*,#36862,.F.);
#53260=ORIENTED_EDGE('',*,*,#36865,.F.);
#53261=ORIENTED_EDGE('',*,*,#36868,.F.);
#53262=ORIENTED_EDGE('',*,*,#36871,.F.);
#53263=ORIENTED_EDGE('',*,*,#36874,.F.);
#53264=ORIENTED_EDGE('',*,*,#36877,.F.);
#53265=ORIENTED_EDGE('',*,*,#36880,.F.);
#53266=ORIENTED_EDGE('',*,*,#36883,.F.);
#53267=ORIENTED_EDGE('',*,*,#36886,.F.);
#53268=ORIENTED_EDGE('',*,*,#36889,.F.);
#53269=ORIENTED_EDGE('',*,*,#36892,.F.);
#53270=ORIENTED_EDGE('',*,*,#36895,.F.);
#53271=ORIENTED_EDGE('',*,*,#36898,.F.);
#53272=ORIENTED_EDGE('',*,*,#36901,.F.);
#53273=ORIENTED_EDGE('',*,*,#36904,.F.);
#53274=ORIENTED_EDGE('',*,*,#36907,.F.);
#53275=ORIENTED_EDGE('',*,*,#36910,.F.);
#53276=ORIENTED_EDGE('',*,*,#36913,.F.);
#53277=ORIENTED_EDGE('',*,*,#36916,.F.);
#53278=ORIENTED_EDGE('',*,*,#36919,.F.);
#53279=ORIENTED_EDGE('',*,*,#36922,.F.);
#53280=ORIENTED_EDGE('',*,*,#36925,.F.);
#53281=ORIENTED_EDGE('',*,*,#36928,.F.);
#53282=ORIENTED_EDGE('',*,*,#36931,.F.);
#53283=ORIENTED_EDGE('',*,*,#36934,.F.);
#53284=ORIENTED_EDGE('',*,*,#36937,.F.);
#53285=ORIENTED_EDGE('',*,*,#36940,.F.);
#53286=ORIENTED_EDGE('',*,*,#36943,.F.);
#53287=ORIENTED_EDGE('',*,*,#36946,.F.);
#53288=ORIENTED_EDGE('',*,*,#36949,.F.);
#53289=ORIENTED_EDGE('',*,*,#36952,.F.);
#53290=ORIENTED_EDGE('',*,*,#36955,.F.);
#53291=ORIENTED_EDGE('',*,*,#36958,.F.);
#53292=ORIENTED_EDGE('',*,*,#36961,.F.);
#53293=ORIENTED_EDGE('',*,*,#36964,.F.);
#53294=ORIENTED_EDGE('',*,*,#36967,.F.);
#53295=ORIENTED_EDGE('',*,*,#36970,.F.);
#53296=ORIENTED_EDGE('',*,*,#36973,.F.);
#53297=ORIENTED_EDGE('',*,*,#36976,.F.);
#53298=ORIENTED_EDGE('',*,*,#36979,.F.);
#53299=ORIENTED_EDGE('',*,*,#36982,.F.);
#53300=ORIENTED_EDGE('',*,*,#36985,.F.);
#53301=ORIENTED_EDGE('',*,*,#36988,.F.);
#53302=ORIENTED_EDGE('',*,*,#36991,.F.);
#53303=ORIENTED_EDGE('',*,*,#36994,.F.);
#53304=ORIENTED_EDGE('',*,*,#36997,.F.);
#53305=ORIENTED_EDGE('',*,*,#37000,.F.);
#53306=ORIENTED_EDGE('',*,*,#37003,.F.);
#53307=ORIENTED_EDGE('',*,*,#37006,.F.);
#53308=ORIENTED_EDGE('',*,*,#37009,.F.);
#53309=ORIENTED_EDGE('',*,*,#37012,.F.);
#53310=ORIENTED_EDGE('',*,*,#37015,.F.);
#53311=ORIENTED_EDGE('',*,*,#37018,.F.);
#53312=ORIENTED_EDGE('',*,*,#37021,.F.);
#53313=ORIENTED_EDGE('',*,*,#37024,.F.);
#53314=ORIENTED_EDGE('',*,*,#37027,.F.);
#53315=ORIENTED_EDGE('',*,*,#37030,.F.);
#53316=ORIENTED_EDGE('',*,*,#37033,.F.);
#53317=ORIENTED_EDGE('',*,*,#37036,.F.);
#53318=ORIENTED_EDGE('',*,*,#37039,.F.);
#53319=ORIENTED_EDGE('',*,*,#37042,.F.);
#53320=ORIENTED_EDGE('',*,*,#37045,.F.);
#53321=ORIENTED_EDGE('',*,*,#37048,.F.);
#53322=ORIENTED_EDGE('',*,*,#37051,.F.);
#53323=ORIENTED_EDGE('',*,*,#37054,.F.);
#53324=ORIENTED_EDGE('',*,*,#37057,.F.);
#53325=ORIENTED_EDGE('',*,*,#37060,.F.);
#53326=ORIENTED_EDGE('',*,*,#37063,.F.);
#53327=ORIENTED_EDGE('',*,*,#37066,.F.);
#53328=ORIENTED_EDGE('',*,*,#37069,.F.);
#53329=ORIENTED_EDGE('',*,*,#37072,.F.);
#53330=ORIENTED_EDGE('',*,*,#37075,.F.);
#53331=ORIENTED_EDGE('',*,*,#37078,.F.);
#53332=ORIENTED_EDGE('',*,*,#37081,.F.);
#53333=ORIENTED_EDGE('',*,*,#37084,.F.);
#53334=ORIENTED_EDGE('',*,*,#37087,.F.);
#53335=ORIENTED_EDGE('',*,*,#37090,.F.);
#53336=ORIENTED_EDGE('',*,*,#37093,.F.);
#53337=ORIENTED_EDGE('',*,*,#37096,.F.);
#53338=ORIENTED_EDGE('',*,*,#37099,.F.);
#53339=ORIENTED_EDGE('',*,*,#37102,.F.);
#53340=ORIENTED_EDGE('',*,*,#37105,.F.);
#53341=ORIENTED_EDGE('',*,*,#37108,.F.);
#53342=ORIENTED_EDGE('',*,*,#37111,.F.);
#53343=ORIENTED_EDGE('',*,*,#37114,.F.);
#53344=ORIENTED_EDGE('',*,*,#37117,.F.);
#53345=ORIENTED_EDGE('',*,*,#37120,.F.);
#53346=ORIENTED_EDGE('',*,*,#37123,.F.);
#53347=ORIENTED_EDGE('',*,*,#37126,.F.);
#53348=ORIENTED_EDGE('',*,*,#37129,.F.);
#53349=ORIENTED_EDGE('',*,*,#37132,.F.);
#53350=ORIENTED_EDGE('',*,*,#37135,.F.);
#53351=ORIENTED_EDGE('',*,*,#37138,.F.);
#53352=ORIENTED_EDGE('',*,*,#37141,.F.);
#53353=ORIENTED_EDGE('',*,*,#37144,.F.);
#53354=ORIENTED_EDGE('',*,*,#37147,.F.);
#53355=ORIENTED_EDGE('',*,*,#37150,.F.);
#53356=ORIENTED_EDGE('',*,*,#37153,.F.);
#53357=ORIENTED_EDGE('',*,*,#37156,.F.);
#53358=ORIENTED_EDGE('',*,*,#37159,.F.);
#53359=ORIENTED_EDGE('',*,*,#37162,.F.);
#53360=ORIENTED_EDGE('',*,*,#37165,.F.);
#53361=ORIENTED_EDGE('',*,*,#37168,.F.);
#53362=ORIENTED_EDGE('',*,*,#37171,.F.);
#53363=ORIENTED_EDGE('',*,*,#37174,.F.);
#53364=ORIENTED_EDGE('',*,*,#37177,.F.);
#53365=ORIENTED_EDGE('',*,*,#37180,.F.);
#53366=ORIENTED_EDGE('',*,*,#37183,.F.);
#53367=ORIENTED_EDGE('',*,*,#37186,.F.);
#53368=ORIENTED_EDGE('',*,*,#37189,.F.);
#53369=ORIENTED_EDGE('',*,*,#37192,.F.);
#53370=ORIENTED_EDGE('',*,*,#37195,.F.);
#53371=ORIENTED_EDGE('',*,*,#37198,.F.);
#53372=ORIENTED_EDGE('',*,*,#37201,.F.);
#53373=ORIENTED_EDGE('',*,*,#37204,.F.);
#53374=ORIENTED_EDGE('',*,*,#37207,.F.);
#53375=ORIENTED_EDGE('',*,*,#37210,.F.);
#53376=ORIENTED_EDGE('',*,*,#37213,.F.);
#53377=ORIENTED_EDGE('',*,*,#37216,.F.);
#53378=ORIENTED_EDGE('',*,*,#37219,.F.);
#53379=ORIENTED_EDGE('',*,*,#37222,.F.);
#53380=ORIENTED_EDGE('',*,*,#37225,.F.);
#53381=ORIENTED_EDGE('',*,*,#37228,.F.);
#53382=ORIENTED_EDGE('',*,*,#37231,.F.);
#53383=ORIENTED_EDGE('',*,*,#37234,.F.);
#53384=ORIENTED_EDGE('',*,*,#37237,.F.);
#53385=ORIENTED_EDGE('',*,*,#37240,.F.);
#53386=ORIENTED_EDGE('',*,*,#37243,.F.);
#53387=ORIENTED_EDGE('',*,*,#37246,.F.);
#53388=ORIENTED_EDGE('',*,*,#37249,.F.);
#53389=ORIENTED_EDGE('',*,*,#37252,.F.);
#53390=ORIENTED_EDGE('',*,*,#37255,.F.);
#53391=ORIENTED_EDGE('',*,*,#37258,.F.);
#53392=ORIENTED_EDGE('',*,*,#37261,.F.);
#53393=ORIENTED_EDGE('',*,*,#37264,.F.);
#53394=ORIENTED_EDGE('',*,*,#37267,.F.);
#53395=ORIENTED_EDGE('',*,*,#37270,.F.);
#53396=ORIENTED_EDGE('',*,*,#37273,.F.);
#53397=ORIENTED_EDGE('',*,*,#37276,.F.);
#53398=ORIENTED_EDGE('',*,*,#37279,.F.);
#53399=ORIENTED_EDGE('',*,*,#37282,.F.);
#53400=ORIENTED_EDGE('',*,*,#37285,.F.);
#53401=ORIENTED_EDGE('',*,*,#37288,.F.);
#53402=ORIENTED_EDGE('',*,*,#37291,.F.);
#53403=ORIENTED_EDGE('',*,*,#37294,.F.);
#53404=ORIENTED_EDGE('',*,*,#37297,.F.);
#53405=ORIENTED_EDGE('',*,*,#37300,.F.);
#53406=ORIENTED_EDGE('',*,*,#37303,.F.);
#53407=ORIENTED_EDGE('',*,*,#37306,.F.);
#53408=ORIENTED_EDGE('',*,*,#37309,.F.);
#53409=ORIENTED_EDGE('',*,*,#37312,.F.);
#53410=ORIENTED_EDGE('',*,*,#37315,.F.);
#53411=ORIENTED_EDGE('',*,*,#37318,.F.);
#53412=ORIENTED_EDGE('',*,*,#37321,.F.);
#53413=ORIENTED_EDGE('',*,*,#37324,.F.);
#53414=ORIENTED_EDGE('',*,*,#37327,.F.);
#53415=ORIENTED_EDGE('',*,*,#37330,.F.);
#53416=ORIENTED_EDGE('',*,*,#37333,.F.);
#53417=ORIENTED_EDGE('',*,*,#37336,.F.);
#53418=ORIENTED_EDGE('',*,*,#37339,.F.);
#53419=ORIENTED_EDGE('',*,*,#37342,.F.);
#53420=ORIENTED_EDGE('',*,*,#37345,.F.);
#53421=ORIENTED_EDGE('',*,*,#37348,.F.);
#53422=ORIENTED_EDGE('',*,*,#37351,.F.);
#53423=ORIENTED_EDGE('',*,*,#37354,.F.);
#53424=ORIENTED_EDGE('',*,*,#37357,.F.);
#53425=ORIENTED_EDGE('',*,*,#37360,.F.);
#53426=ORIENTED_EDGE('',*,*,#37363,.F.);
#53427=ORIENTED_EDGE('',*,*,#37366,.F.);
#53428=ORIENTED_EDGE('',*,*,#37369,.F.);
#53429=ORIENTED_EDGE('',*,*,#37372,.F.);
#53430=ORIENTED_EDGE('',*,*,#37375,.F.);
#53431=ORIENTED_EDGE('',*,*,#37378,.F.);
#53432=ORIENTED_EDGE('',*,*,#37381,.F.);
#53433=ORIENTED_EDGE('',*,*,#37384,.F.);
#53434=ORIENTED_EDGE('',*,*,#37387,.F.);
#53435=ORIENTED_EDGE('',*,*,#37390,.F.);
#53436=ORIENTED_EDGE('',*,*,#37393,.F.);
#53437=ORIENTED_EDGE('',*,*,#37396,.F.);
#53438=ORIENTED_EDGE('',*,*,#37399,.F.);
#53439=ORIENTED_EDGE('',*,*,#37402,.F.);
#53440=ORIENTED_EDGE('',*,*,#37405,.F.);
#53441=ORIENTED_EDGE('',*,*,#37408,.F.);
#53442=ORIENTED_EDGE('',*,*,#37411,.F.);
#53443=ORIENTED_EDGE('',*,*,#37414,.F.);
#53444=ORIENTED_EDGE('',*,*,#37417,.F.);
#53445=ORIENTED_EDGE('',*,*,#37420,.F.);
#53446=ORIENTED_EDGE('',*,*,#37423,.F.);
#53447=ORIENTED_EDGE('',*,*,#37426,.F.);
#53448=ORIENTED_EDGE('',*,*,#37429,.F.);
#53449=ORIENTED_EDGE('',*,*,#37432,.F.);
#53450=ORIENTED_EDGE('',*,*,#37435,.F.);
#53451=ORIENTED_EDGE('',*,*,#37438,.F.);
#53452=ORIENTED_EDGE('',*,*,#37441,.F.);
#53453=ORIENTED_EDGE('',*,*,#37444,.F.);
#53454=ORIENTED_EDGE('',*,*,#37447,.F.);
#53455=ORIENTED_EDGE('',*,*,#37450,.F.);
#53456=ORIENTED_EDGE('',*,*,#37453,.F.);
#53457=ORIENTED_EDGE('',*,*,#37456,.F.);
#53458=ORIENTED_EDGE('',*,*,#37459,.F.);
#53459=ORIENTED_EDGE('',*,*,#37462,.F.);
#53460=ORIENTED_EDGE('',*,*,#37465,.F.);
#53461=ORIENTED_EDGE('',*,*,#37468,.F.);
#53462=ORIENTED_EDGE('',*,*,#37471,.F.);
#53463=ORIENTED_EDGE('',*,*,#37474,.F.);
#53464=ORIENTED_EDGE('',*,*,#37477,.F.);
#53465=ORIENTED_EDGE('',*,*,#37480,.F.);
#53466=ORIENTED_EDGE('',*,*,#37483,.F.);
#53467=ORIENTED_EDGE('',*,*,#37486,.F.);
#53468=ORIENTED_EDGE('',*,*,#37489,.F.);
#53469=ORIENTED_EDGE('',*,*,#37492,.F.);
#53470=ORIENTED_EDGE('',*,*,#37495,.F.);
#53471=ORIENTED_EDGE('',*,*,#37498,.F.);
#53472=ORIENTED_EDGE('',*,*,#37501,.F.);
#53473=ORIENTED_EDGE('',*,*,#37504,.F.);
#53474=ORIENTED_EDGE('',*,*,#37507,.F.);
#53475=ORIENTED_EDGE('',*,*,#37510,.F.);
#53476=ORIENTED_EDGE('',*,*,#37513,.F.);
#53477=ORIENTED_EDGE('',*,*,#37516,.F.);
#53478=ORIENTED_EDGE('',*,*,#37519,.F.);
#53479=ORIENTED_EDGE('',*,*,#37522,.F.);
#53480=ORIENTED_EDGE('',*,*,#37525,.F.);
#53481=ORIENTED_EDGE('',*,*,#37528,.F.);
#53482=ORIENTED_EDGE('',*,*,#37531,.F.);
#53483=ORIENTED_EDGE('',*,*,#37534,.F.);
#53484=ORIENTED_EDGE('',*,*,#37537,.F.);
#53485=ORIENTED_EDGE('',*,*,#37540,.F.);
#53486=ORIENTED_EDGE('',*,*,#37543,.F.);
#53487=ORIENTED_EDGE('',*,*,#37546,.F.);
#53488=ORIENTED_EDGE('',*,*,#37549,.F.);
#53489=ORIENTED_EDGE('',*,*,#37552,.F.);
#53490=ORIENTED_EDGE('',*,*,#37555,.F.);
#53491=ORIENTED_EDGE('',*,*,#37558,.F.);
#53492=ORIENTED_EDGE('',*,*,#37561,.F.);
#53493=ORIENTED_EDGE('',*,*,#37564,.F.);
#53494=ORIENTED_EDGE('',*,*,#37567,.F.);
#53495=ORIENTED_EDGE('',*,*,#37570,.F.);
#53496=ORIENTED_EDGE('',*,*,#37573,.F.);
#53497=ORIENTED_EDGE('',*,*,#37576,.F.);
#53498=ORIENTED_EDGE('',*,*,#37579,.F.);
#53499=ORIENTED_EDGE('',*,*,#36054,.F.);
#53500=ORIENTED_EDGE('',*,*,#36079,.F.);
#59333=ADVANCED_FACE('',(#6233),#926,.F.);
#59334=ADVANCED_FACE('',(#6234),#703,.F.);
#59335=ADVANCED_FACE('',(#6235,#1841),#3186,.T.);
#59336=ADVANCED_FACE('',(#6236),#927,.F.);
#59337=ADVANCED_FACE('',(#6237),#704,.F.);
#59338=ADVANCED_FACE('',(#6238,#1842),#3187,.T.);
#59339=ADVANCED_FACE('',(#6239,#1843),#3188,.T.);
#59340=ADVANCED_FACE('',(#6240,#1844),#3189,.T.);
#59341=ADVANCED_FACE('',(#6241),#705,.F.);
#59342=ADVANCED_FACE('',(#6242),#706,.F.);
#59343=ADVANCED_FACE('',(#6243),#3190,.T.);
#59344=ADVANCED_FACE('',(#6244),#3191,.T.);
#59345=ADVANCED_FACE('',(#6245,#1845,#1846),#3192,.T.);
#59346=ADVANCED_FACE('',(#6246),#3193,.T.);
#59347=ADVANCED_FACE('',(#6247),#3194,.T.);
#59348=ADVANCED_FACE('',(#6248),#3195,.T.);
#59349=ADVANCED_FACE('',(#6249),#3196,.T.);
#59350=ADVANCED_FACE('',(#6250),#3197,.T.);
#59351=ADVANCED_FACE('',(#6251),#3198,.T.);
#59352=ADVANCED_FACE('',(#6252),#3199,.T.);
#59353=ADVANCED_FACE('',(#6253),#3200,.T.);
#59354=ADVANCED_FACE('',(#6254),#3201,.T.);
#59355=ADVANCED_FACE('',(#6255),#3202,.T.);
#59356=ADVANCED_FACE('',(#6256),#3203,.T.);
#59357=ADVANCED_FACE('',(#6257),#3204,.T.);
#59358=ADVANCED_FACE('',(#6258),#3205,.T.);
#59359=ADVANCED_FACE('',(#6259),#3206,.T.);
#59360=ADVANCED_FACE('',(#6260),#3207,.T.);
#59361=ADVANCED_FACE('',(#6261),#3208,.T.);
#59362=ADVANCED_FACE('',(#6262),#3209,.T.);
#59363=ADVANCED_FACE('',(#6263),#3210,.T.);
#59364=ADVANCED_FACE('',(#6264),#3211,.T.);
#59365=ADVANCED_FACE('',(#6265),#3212,.T.);
#59366=ADVANCED_FACE('',(#6266),#3213,.T.);
#59367=ADVANCED_FACE('',(#6267),#3214,.T.);
#59368=ADVANCED_FACE('',(#6268),#3215,.T.);
#59369=ADVANCED_FACE('',(#6269),#3216,.T.);
#59370=ADVANCED_FACE('',(#6270),#3217,.T.);
#59371=ADVANCED_FACE('',(#6271),#3218,.T.);
#59372=ADVANCED_FACE('',(#6272),#3219,.T.);
#59373=ADVANCED_FACE('',(#6273),#3220,.T.);
#59374=ADVANCED_FACE('',(#6274),#3221,.T.);
#59375=ADVANCED_FACE('',(#6275),#3222,.T.);
#59376=ADVANCED_FACE('',(#6276),#3223,.T.);
#59377=ADVANCED_FACE('',(#6277),#3224,.T.);
#59378=ADVANCED_FACE('',(#6278),#3225,.T.);
#59379=ADVANCED_FACE('',(#6279),#3226,.T.);
#59380=ADVANCED_FACE('',(#6280),#3227,.T.);
#59381=ADVANCED_FACE('',(#6281),#3228,.T.);
#59382=ADVANCED_FACE('',(#6282),#3229,.T.);
#59383=ADVANCED_FACE('',(#6283),#3230,.T.);
#59384=ADVANCED_FACE('',(#6284),#3231,.T.);
#59385=ADVANCED_FACE('',(#6285),#3232,.T.);
#59386=ADVANCED_FACE('',(#6286),#3233,.T.);
#59387=ADVANCED_FACE('',(#6287),#3234,.T.);
#59388=ADVANCED_FACE('',(#6288),#3235,.T.);
#59389=ADVANCED_FACE('',(#6289),#3236,.T.);
#59390=ADVANCED_FACE('',(#6290),#3237,.T.);
#59391=ADVANCED_FACE('',(#6291),#3238,.T.);
#59392=ADVANCED_FACE('',(#6292),#3239,.T.);
#59393=ADVANCED_FACE('',(#6293),#3240,.T.);
#59394=ADVANCED_FACE('',(#6294),#3241,.T.);
#59395=ADVANCED_FACE('',(#6295),#3242,.T.);
#59396=ADVANCED_FACE('',(#6296),#3243,.T.);
#59397=ADVANCED_FACE('',(#6297),#3244,.T.);
#59398=ADVANCED_FACE('',(#6298),#3245,.T.);
#59399=ADVANCED_FACE('',(#6299),#3246,.T.);
#59400=ADVANCED_FACE('',(#6300),#3247,.T.);
#59401=ADVANCED_FACE('',(#6301),#3248,.T.);
#59402=ADVANCED_FACE('',(#6302),#3249,.T.);
#59403=ADVANCED_FACE('',(#6303),#3250,.T.);
#59404=ADVANCED_FACE('',(#6304),#3251,.T.);
#59405=ADVANCED_FACE('',(#6305),#3252,.T.);
#59406=ADVANCED_FACE('',(#6306),#3253,.T.);
#59407=ADVANCED_FACE('',(#6307),#3254,.T.);
#59408=ADVANCED_FACE('',(#6308),#3255,.T.);
#59409=ADVANCED_FACE('',(#6309),#3256,.T.);
#59410=ADVANCED_FACE('',(#6310),#3257,.T.);
#59411=ADVANCED_FACE('',(#6311),#3258,.T.);
#59412=ADVANCED_FACE('',(#6312),#3259,.T.);
#59413=ADVANCED_FACE('',(#6313),#3260,.T.);
#59414=ADVANCED_FACE('',(#6314),#3261,.T.);
#59415=ADVANCED_FACE('',(#6315),#3262,.T.);
#59416=ADVANCED_FACE('',(#6316),#3263,.T.);
#59417=ADVANCED_FACE('',(#6317),#3264,.T.);
#59418=ADVANCED_FACE('',(#6318),#3265,.T.);
#59419=ADVANCED_FACE('',(#6319),#3266,.T.);
#59420=ADVANCED_FACE('',(#6320),#3267,.T.);
#59421=ADVANCED_FACE('',(#6321),#3268,.T.);
#59422=ADVANCED_FACE('',(#6322),#3269,.T.);
#59423=ADVANCED_FACE('',(#6323),#3270,.T.);
#59424=ADVANCED_FACE('',(#6324),#3271,.T.);
#59425=ADVANCED_FACE('',(#6325),#3272,.T.);
#59426=ADVANCED_FACE('',(#6326),#3273,.T.);
#59427=ADVANCED_FACE('',(#6327),#3274,.T.);
#59428=ADVANCED_FACE('',(#6328),#3275,.T.);
#59429=ADVANCED_FACE('',(#6329),#3276,.T.);
#59430=ADVANCED_FACE('',(#6330),#3277,.T.);
#59431=ADVANCED_FACE('',(#6331),#3278,.T.);
#59432=ADVANCED_FACE('',(#6332),#3279,.T.);
#59433=ADVANCED_FACE('',(#6333),#3280,.T.);
#59434=ADVANCED_FACE('',(#6334),#3281,.T.);
#59435=ADVANCED_FACE('',(#6335),#3282,.T.);
#59436=ADVANCED_FACE('',(#6336),#3283,.T.);
#59437=ADVANCED_FACE('',(#6337),#3284,.T.);
#59438=ADVANCED_FACE('',(#6338),#3285,.T.);
#59439=ADVANCED_FACE('',(#6339),#3286,.T.);
#59440=ADVANCED_FACE('',(#6340),#3287,.T.);
#59441=ADVANCED_FACE('',(#6341),#3288,.T.);
#59442=ADVANCED_FACE('',(#6342),#3289,.T.);
#59443=ADVANCED_FACE('',(#6343),#3290,.T.);
#59444=ADVANCED_FACE('',(#6344),#3291,.T.);
#59445=ADVANCED_FACE('',(#6345),#3292,.T.);
#59446=ADVANCED_FACE('',(#6346),#3293,.T.);
#59447=ADVANCED_FACE('',(#6347),#3294,.T.);
#59448=ADVANCED_FACE('',(#6348),#3295,.T.);
#59449=ADVANCED_FACE('',(#6349),#3296,.T.);
#59450=ADVANCED_FACE('',(#6350),#3297,.T.);
#59451=ADVANCED_FACE('',(#6351),#3298,.T.);
#59452=ADVANCED_FACE('',(#6352),#3299,.T.);
#59453=ADVANCED_FACE('',(#6353),#3300,.T.);
#59454=ADVANCED_FACE('',(#6354),#3301,.T.);
#59455=ADVANCED_FACE('',(#6355),#3302,.T.);
#59456=ADVANCED_FACE('',(#6356),#3303,.T.);
#59457=ADVANCED_FACE('',(#6357),#3304,.T.);
#59458=ADVANCED_FACE('',(#6358),#3305,.T.);
#59459=ADVANCED_FACE('',(#6359),#3306,.T.);
#59460=ADVANCED_FACE('',(#6360),#3307,.T.);
#59461=ADVANCED_FACE('',(#6361),#3308,.T.);
#59462=ADVANCED_FACE('',(#6362),#3309,.T.);
#59463=ADVANCED_FACE('',(#6363),#3310,.T.);
#59464=ADVANCED_FACE('',(#6364),#3311,.T.);
#59465=ADVANCED_FACE('',(#6365),#3312,.T.);
#59466=ADVANCED_FACE('',(#6366),#3313,.T.);
#59467=ADVANCED_FACE('',(#6367),#3314,.T.);
#59468=ADVANCED_FACE('',(#6368),#3315,.T.);
#59469=ADVANCED_FACE('',(#6369),#3316,.T.);
#59470=ADVANCED_FACE('',(#6370),#3317,.T.);
#59471=ADVANCED_FACE('',(#6371),#3318,.T.);
#59472=ADVANCED_FACE('',(#6372),#3319,.T.);
#59473=ADVANCED_FACE('',(#6373),#3320,.T.);
#59474=ADVANCED_FACE('',(#6374),#3321,.T.);
#59475=ADVANCED_FACE('',(#6375),#3322,.T.);
#59476=ADVANCED_FACE('',(#6376),#3323,.T.);
#59477=ADVANCED_FACE('',(#6377),#3324,.T.);
#59478=ADVANCED_FACE('',(#6378),#3325,.T.);
#59479=ADVANCED_FACE('',(#6379),#3326,.T.);
#59480=ADVANCED_FACE('',(#6380),#3327,.T.);
#59481=ADVANCED_FACE('',(#6381),#3328,.T.);
#59482=ADVANCED_FACE('',(#6382),#3329,.T.);
#59483=ADVANCED_FACE('',(#6383),#3330,.T.);
#59484=ADVANCED_FACE('',(#6384),#3331,.T.);
#59485=ADVANCED_FACE('',(#6385),#3332,.T.);
#59486=ADVANCED_FACE('',(#6386),#3333,.T.);
#59487=ADVANCED_FACE('',(#6387),#3334,.T.);
#59488=ADVANCED_FACE('',(#6388),#3335,.T.);
#59489=ADVANCED_FACE('',(#6389),#3336,.T.);
#59490=ADVANCED_FACE('',(#6390),#3337,.T.);
#59491=ADVANCED_FACE('',(#6391),#3338,.T.);
#59492=ADVANCED_FACE('',(#6392),#3339,.T.);
#59493=ADVANCED_FACE('',(#6393),#3340,.T.);
#59494=ADVANCED_FACE('',(#6394),#3341,.T.);
#59495=ADVANCED_FACE('',(#6395),#3342,.T.);
#59496=ADVANCED_FACE('',(#6396),#3343,.T.);
#59497=ADVANCED_FACE('',(#6397),#3344,.T.);
#59498=ADVANCED_FACE('',(#6398),#3345,.T.);
#59499=ADVANCED_FACE('',(#6399),#3346,.T.);
#59500=ADVANCED_FACE('',(#6400),#3347,.T.);
#59501=ADVANCED_FACE('',(#6401),#3348,.T.);
#59502=ADVANCED_FACE('',(#6402),#3349,.T.);
#59503=ADVANCED_FACE('',(#6403),#3350,.T.);
#59504=ADVANCED_FACE('',(#6404),#3351,.T.);
#59505=ADVANCED_FACE('',(#6405),#3352,.T.);
#59506=ADVANCED_FACE('',(#6406),#3353,.T.);
#59507=ADVANCED_FACE('',(#6407),#3354,.T.);
#59508=ADVANCED_FACE('',(#6408),#3355,.T.);
#59509=ADVANCED_FACE('',(#6409),#3356,.T.);
#59510=ADVANCED_FACE('',(#6410),#3357,.T.);
#59511=ADVANCED_FACE('',(#6411),#3358,.T.);
#59512=ADVANCED_FACE('',(#6412),#3359,.T.);
#59513=ADVANCED_FACE('',(#6413),#3360,.T.);
#59514=ADVANCED_FACE('',(#6414),#3361,.T.);
#59515=ADVANCED_FACE('',(#6415),#3362,.T.);
#59516=ADVANCED_FACE('',(#6416),#3363,.T.);
#59517=ADVANCED_FACE('',(#6417),#3364,.T.);
#59518=ADVANCED_FACE('',(#6418),#3365,.T.);
#59519=ADVANCED_FACE('',(#6419),#3366,.T.);
#59520=ADVANCED_FACE('',(#6420),#3367,.T.);
#59521=ADVANCED_FACE('',(#6421),#3368,.T.);
#59522=ADVANCED_FACE('',(#6422),#3369,.T.);
#59523=ADVANCED_FACE('',(#6423),#3370,.T.);
#59524=ADVANCED_FACE('',(#6424),#3371,.T.);
#59525=ADVANCED_FACE('',(#6425),#3372,.T.);
#59526=ADVANCED_FACE('',(#6426),#3373,.T.);
#59527=ADVANCED_FACE('',(#6427),#3374,.T.);
#59528=ADVANCED_FACE('',(#6428),#3375,.T.);
#59529=ADVANCED_FACE('',(#6429),#3376,.T.);
#59530=ADVANCED_FACE('',(#6430),#3377,.T.);
#59531=ADVANCED_FACE('',(#6431),#3378,.T.);
#59532=ADVANCED_FACE('',(#6432),#3379,.T.);
#59533=ADVANCED_FACE('',(#6433),#3380,.T.);
#59534=ADVANCED_FACE('',(#6434),#3381,.T.);
#59535=ADVANCED_FACE('',(#6435),#3382,.T.);
#59536=ADVANCED_FACE('',(#6436),#3383,.T.);
#59537=ADVANCED_FACE('',(#6437),#3384,.T.);
#59538=ADVANCED_FACE('',(#6438),#3385,.T.);
#59539=ADVANCED_FACE('',(#6439),#3386,.T.);
#59540=ADVANCED_FACE('',(#6440),#3387,.T.);
#59541=ADVANCED_FACE('',(#6441),#3388,.T.);
#59542=ADVANCED_FACE('',(#6442),#3389,.T.);
#59543=ADVANCED_FACE('',(#6443),#3390,.T.);
#59544=ADVANCED_FACE('',(#6444),#3391,.T.);
#59545=ADVANCED_FACE('',(#6445),#3392,.T.);
#59546=ADVANCED_FACE('',(#6446),#3393,.T.);
#59547=ADVANCED_FACE('',(#6447),#3394,.T.);
#59548=ADVANCED_FACE('',(#6448),#3395,.T.);
#59549=ADVANCED_FACE('',(#6449),#3396,.T.);
#59550=ADVANCED_FACE('',(#6450),#3397,.T.);
#59551=ADVANCED_FACE('',(#6451),#3398,.T.);
#59552=ADVANCED_FACE('',(#6452),#3399,.T.);
#59553=ADVANCED_FACE('',(#6453),#3400,.T.);
#59554=ADVANCED_FACE('',(#6454),#3401,.T.);
#59555=ADVANCED_FACE('',(#6455),#3402,.T.);
#59556=ADVANCED_FACE('',(#6456),#3403,.T.);
#59557=ADVANCED_FACE('',(#6457),#3404,.T.);
#59558=ADVANCED_FACE('',(#6458),#3405,.T.);
#59559=ADVANCED_FACE('',(#6459),#3406,.T.);
#59560=ADVANCED_FACE('',(#6460),#3407,.T.);
#59561=ADVANCED_FACE('',(#6461),#3408,.T.);
#59562=ADVANCED_FACE('',(#6462),#3409,.T.);
#59563=ADVANCED_FACE('',(#6463),#3410,.T.);
#59564=ADVANCED_FACE('',(#6464),#3411,.T.);
#59565=ADVANCED_FACE('',(#6465),#3412,.T.);
#59566=ADVANCED_FACE('',(#6466),#3413,.T.);
#59567=ADVANCED_FACE('',(#6467),#3414,.T.);
#59568=ADVANCED_FACE('',(#6468),#3415,.T.);
#59569=ADVANCED_FACE('',(#6469),#3416,.T.);
#59570=ADVANCED_FACE('',(#6470),#3417,.T.);
#59571=ADVANCED_FACE('',(#6471),#3418,.T.);
#59572=ADVANCED_FACE('',(#6472),#3419,.T.);
#59573=ADVANCED_FACE('',(#6473),#3420,.T.);
#59574=ADVANCED_FACE('',(#6474),#3421,.T.);
#59575=ADVANCED_FACE('',(#6475),#3422,.T.);
#59576=ADVANCED_FACE('',(#6476),#3423,.T.);
#59577=ADVANCED_FACE('',(#6477),#3424,.T.);
#59578=ADVANCED_FACE('',(#6478),#3425,.T.);
#59579=ADVANCED_FACE('',(#6479),#3426,.T.);
#59580=ADVANCED_FACE('',(#6480),#3427,.T.);
#59581=ADVANCED_FACE('',(#6481),#3428,.T.);
#59582=ADVANCED_FACE('',(#6482),#3429,.T.);
#59583=ADVANCED_FACE('',(#6483),#3430,.T.);
#59584=ADVANCED_FACE('',(#6484),#3431,.T.);
#59585=ADVANCED_FACE('',(#6485),#3432,.T.);
#59586=ADVANCED_FACE('',(#6486),#3433,.T.);
#59587=ADVANCED_FACE('',(#6487),#3434,.T.);
#59588=ADVANCED_FACE('',(#6488),#3435,.T.);
#59589=ADVANCED_FACE('',(#6489),#3436,.T.);
#59590=ADVANCED_FACE('',(#6490),#3437,.T.);
#59591=ADVANCED_FACE('',(#6491),#3438,.T.);
#59592=ADVANCED_FACE('',(#6492),#3439,.T.);
#59593=ADVANCED_FACE('',(#6493),#3440,.T.);
#59594=ADVANCED_FACE('',(#6494),#3441,.T.);
#59595=ADVANCED_FACE('',(#6495),#3442,.T.);
#59596=ADVANCED_FACE('',(#6496),#3443,.T.);
#59597=ADVANCED_FACE('',(#6497),#3444,.T.);
#59598=ADVANCED_FACE('',(#6498),#3445,.T.);
#59599=ADVANCED_FACE('',(#6499),#3446,.T.);
#59600=ADVANCED_FACE('',(#6500),#3447,.T.);
#59601=ADVANCED_FACE('',(#6501),#3448,.T.);
#59602=ADVANCED_FACE('',(#6502),#3449,.T.);
#59603=ADVANCED_FACE('',(#6503),#3450,.T.);
#59604=ADVANCED_FACE('',(#6504),#3451,.T.);
#59605=ADVANCED_FACE('',(#6505),#3452,.T.);
#59606=ADVANCED_FACE('',(#6506),#3453,.T.);
#59607=ADVANCED_FACE('',(#6507),#3454,.T.);
#59608=ADVANCED_FACE('',(#6508),#3455,.T.);
#59609=ADVANCED_FACE('',(#6509),#3456,.T.);
#59610=ADVANCED_FACE('',(#6510),#3457,.T.);
#59611=ADVANCED_FACE('',(#6511),#3458,.T.);
#59612=ADVANCED_FACE('',(#6512),#3459,.T.);
#59613=ADVANCED_FACE('',(#6513),#3460,.T.);
#59614=ADVANCED_FACE('',(#6514),#3461,.T.);
#59615=ADVANCED_FACE('',(#6515),#3462,.T.);
#59616=ADVANCED_FACE('',(#6516),#3463,.T.);
#59617=ADVANCED_FACE('',(#6517),#3464,.T.);
#59618=ADVANCED_FACE('',(#6518),#3465,.T.);
#59619=ADVANCED_FACE('',(#6519),#3466,.T.);
#59620=ADVANCED_FACE('',(#6520),#3467,.T.);
#59621=ADVANCED_FACE('',(#6521),#3468,.T.);
#59622=ADVANCED_FACE('',(#6522),#3469,.T.);
#59623=ADVANCED_FACE('',(#6523),#3470,.T.);
#59624=ADVANCED_FACE('',(#6524),#3471,.T.);
#59625=ADVANCED_FACE('',(#6525),#3472,.T.);
#59626=ADVANCED_FACE('',(#6526),#3473,.T.);
#59627=ADVANCED_FACE('',(#6527),#3474,.T.);
#59628=ADVANCED_FACE('',(#6528),#3475,.T.);
#59629=ADVANCED_FACE('',(#6529),#3476,.T.);
#59630=ADVANCED_FACE('',(#6530),#3477,.T.);
#59631=ADVANCED_FACE('',(#6531),#3478,.T.);
#59632=ADVANCED_FACE('',(#6532),#3479,.T.);
#59633=ADVANCED_FACE('',(#6533),#3480,.T.);
#59634=ADVANCED_FACE('',(#6534),#3481,.T.);
#59635=ADVANCED_FACE('',(#6535),#3482,.T.);
#59636=ADVANCED_FACE('',(#6536),#3483,.T.);
#59637=ADVANCED_FACE('',(#6537),#3484,.T.);
#59638=ADVANCED_FACE('',(#6538),#3485,.T.);
#59639=ADVANCED_FACE('',(#6539),#3486,.T.);
#59640=ADVANCED_FACE('',(#6540),#3487,.T.);
#59641=ADVANCED_FACE('',(#6541),#3488,.T.);
#59642=ADVANCED_FACE('',(#6542),#3489,.T.);
#59643=ADVANCED_FACE('',(#6543),#3490,.T.);
#59644=ADVANCED_FACE('',(#6544),#3491,.T.);
#59645=ADVANCED_FACE('',(#6545),#3492,.T.);
#59646=ADVANCED_FACE('',(#6546),#3493,.T.);
#59647=ADVANCED_FACE('',(#6547),#3494,.T.);
#59648=ADVANCED_FACE('',(#6548),#3495,.T.);
#59649=ADVANCED_FACE('',(#6549),#3496,.T.);
#59650=ADVANCED_FACE('',(#6550),#3497,.T.);
#59651=ADVANCED_FACE('',(#6551),#3498,.T.);
#59652=ADVANCED_FACE('',(#6552),#3499,.T.);
#59653=ADVANCED_FACE('',(#6553),#3500,.T.);
#59654=ADVANCED_FACE('',(#6554),#3501,.T.);
#59655=ADVANCED_FACE('',(#6555),#3502,.T.);
#59656=ADVANCED_FACE('',(#6556),#3503,.T.);
#59657=ADVANCED_FACE('',(#6557),#3504,.T.);
#59658=ADVANCED_FACE('',(#6558),#3505,.T.);
#59659=ADVANCED_FACE('',(#6559),#3506,.T.);
#59660=ADVANCED_FACE('',(#6560),#3507,.T.);
#59661=ADVANCED_FACE('',(#6561),#3508,.T.);
#59662=ADVANCED_FACE('',(#6562),#3509,.T.);
#59663=ADVANCED_FACE('',(#6563),#3510,.T.);
#59664=ADVANCED_FACE('',(#6564),#3511,.T.);
#59665=ADVANCED_FACE('',(#6565),#3512,.T.);
#59666=ADVANCED_FACE('',(#6566),#3513,.T.);
#59667=ADVANCED_FACE('',(#6567),#3514,.T.);
#59668=ADVANCED_FACE('',(#6568),#3515,.T.);
#59669=ADVANCED_FACE('',(#6569),#3516,.T.);
#59670=ADVANCED_FACE('',(#6570),#3517,.T.);
#59671=ADVANCED_FACE('',(#6571),#3518,.T.);
#59672=ADVANCED_FACE('',(#6572),#3519,.T.);
#59673=ADVANCED_FACE('',(#6573),#3520,.T.);
#59674=ADVANCED_FACE('',(#6574),#3521,.T.);
#59675=ADVANCED_FACE('',(#6575),#3522,.T.);
#59676=ADVANCED_FACE('',(#6576),#3523,.T.);
#59677=ADVANCED_FACE('',(#6577),#3524,.T.);
#59678=ADVANCED_FACE('',(#6578),#3525,.T.);
#59679=ADVANCED_FACE('',(#6579),#3526,.T.);
#59680=ADVANCED_FACE('',(#6580),#3527,.T.);
#59681=ADVANCED_FACE('',(#6581),#3528,.T.);
#59682=ADVANCED_FACE('',(#6582),#3529,.T.);
#59683=ADVANCED_FACE('',(#6583),#3530,.T.);
#59684=ADVANCED_FACE('',(#6584),#3531,.T.);
#59685=ADVANCED_FACE('',(#6585),#3532,.T.);
#59686=ADVANCED_FACE('',(#6586),#3533,.T.);
#59687=ADVANCED_FACE('',(#6587),#3534,.T.);
#59688=ADVANCED_FACE('',(#6588),#3535,.T.);
#59689=ADVANCED_FACE('',(#6589),#3536,.T.);
#59690=ADVANCED_FACE('',(#6590),#3537,.T.);
#59691=ADVANCED_FACE('',(#6591),#3538,.T.);
#59692=ADVANCED_FACE('',(#6592),#3539,.T.);
#59693=ADVANCED_FACE('',(#6593),#3540,.T.);
#59694=ADVANCED_FACE('',(#6594),#3541,.T.);
#59695=ADVANCED_FACE('',(#6595),#3542,.T.);
#59696=ADVANCED_FACE('',(#6596),#3543,.T.);
#59697=ADVANCED_FACE('',(#6597),#3544,.T.);
#59698=ADVANCED_FACE('',(#6598),#3545,.T.);
#59699=ADVANCED_FACE('',(#6599),#3546,.T.);
#59700=ADVANCED_FACE('',(#6600),#3547,.T.);
#59701=ADVANCED_FACE('',(#6601),#3548,.T.);
#59702=ADVANCED_FACE('',(#6602),#3549,.T.);
#59703=ADVANCED_FACE('',(#6603),#3550,.T.);
#59704=ADVANCED_FACE('',(#6604),#3551,.T.);
#59705=ADVANCED_FACE('',(#6605),#3552,.T.);
#59706=ADVANCED_FACE('',(#6606),#3553,.T.);
#59707=ADVANCED_FACE('',(#6607),#3554,.T.);
#59708=ADVANCED_FACE('',(#6608),#3555,.T.);
#59709=ADVANCED_FACE('',(#6609),#3556,.T.);
#59710=ADVANCED_FACE('',(#6610),#3557,.T.);
#59711=ADVANCED_FACE('',(#6611),#3558,.T.);
#59712=ADVANCED_FACE('',(#6612),#3559,.T.);
#59713=ADVANCED_FACE('',(#6613),#3560,.T.);
#59714=ADVANCED_FACE('',(#6614),#3561,.T.);
#59715=ADVANCED_FACE('',(#6615),#3562,.T.);
#59716=ADVANCED_FACE('',(#6616),#3563,.T.);
#59717=ADVANCED_FACE('',(#6617),#3564,.T.);
#59718=ADVANCED_FACE('',(#6618),#3565,.T.);
#59719=ADVANCED_FACE('',(#6619),#3566,.T.);
#59720=ADVANCED_FACE('',(#6620),#3567,.T.);
#59721=ADVANCED_FACE('',(#6621),#3568,.T.);
#59722=ADVANCED_FACE('',(#6622),#3569,.T.);
#59723=ADVANCED_FACE('',(#6623),#3570,.T.);
#59724=ADVANCED_FACE('',(#6624),#3571,.T.);
#59725=ADVANCED_FACE('',(#6625),#3572,.T.);
#59726=ADVANCED_FACE('',(#6626),#3573,.T.);
#59727=ADVANCED_FACE('',(#6627),#3574,.T.);
#59728=ADVANCED_FACE('',(#6628),#3575,.T.);
#59729=ADVANCED_FACE('',(#6629),#3576,.T.);
#59730=ADVANCED_FACE('',(#6630),#3577,.T.);
#59731=ADVANCED_FACE('',(#6631),#3578,.T.);
#59732=ADVANCED_FACE('',(#6632),#3579,.T.);
#59733=ADVANCED_FACE('',(#6633),#3580,.T.);
#59734=ADVANCED_FACE('',(#6634),#3581,.T.);
#59735=ADVANCED_FACE('',(#6635),#3582,.T.);
#59736=ADVANCED_FACE('',(#6636),#3583,.T.);
#59737=ADVANCED_FACE('',(#6637),#3584,.T.);
#59738=ADVANCED_FACE('',(#6638),#3585,.T.);
#59739=ADVANCED_FACE('',(#6639),#3586,.T.);
#59740=ADVANCED_FACE('',(#6640),#3587,.T.);
#59741=ADVANCED_FACE('',(#6641),#3588,.T.);
#59742=ADVANCED_FACE('',(#6642),#3589,.T.);
#59743=ADVANCED_FACE('',(#6643),#3590,.T.);
#59744=ADVANCED_FACE('',(#6644),#3591,.T.);
#59745=ADVANCED_FACE('',(#6645),#3592,.T.);
#59746=ADVANCED_FACE('',(#6646),#3593,.T.);
#59747=ADVANCED_FACE('',(#6647),#3594,.T.);
#59748=ADVANCED_FACE('',(#6648),#3595,.T.);
#59749=ADVANCED_FACE('',(#6649),#3596,.T.);
#59750=ADVANCED_FACE('',(#6650),#3597,.T.);
#59751=ADVANCED_FACE('',(#6651),#3598,.T.);
#59752=ADVANCED_FACE('',(#6652),#3599,.T.);
#59753=ADVANCED_FACE('',(#6653),#3600,.T.);
#59754=ADVANCED_FACE('',(#6654),#3601,.T.);
#59755=ADVANCED_FACE('',(#6655),#3602,.T.);
#59756=ADVANCED_FACE('',(#6656),#3603,.T.);
#59757=ADVANCED_FACE('',(#6657),#3604,.T.);
#59758=ADVANCED_FACE('',(#6658),#3605,.T.);
#59759=ADVANCED_FACE('',(#6659),#3606,.T.);
#59760=ADVANCED_FACE('',(#6660),#3607,.T.);
#59761=ADVANCED_FACE('',(#6661),#3608,.T.);
#59762=ADVANCED_FACE('',(#6662),#3609,.T.);
#59763=ADVANCED_FACE('',(#6663),#3610,.T.);
#59764=ADVANCED_FACE('',(#6664),#3611,.T.);
#59765=ADVANCED_FACE('',(#6665),#3612,.T.);
#59766=ADVANCED_FACE('',(#6666),#3613,.T.);
#59767=ADVANCED_FACE('',(#6667),#3614,.T.);
#59768=ADVANCED_FACE('',(#6668),#3615,.T.);
#59769=ADVANCED_FACE('',(#6669),#3616,.T.);
#59770=ADVANCED_FACE('',(#6670),#3617,.T.);
#59771=ADVANCED_FACE('',(#6671),#3618,.T.);
#59772=ADVANCED_FACE('',(#6672),#3619,.T.);
#59773=ADVANCED_FACE('',(#6673),#3620,.T.);
#59774=ADVANCED_FACE('',(#6674),#3621,.T.);
#59775=ADVANCED_FACE('',(#6675),#3622,.T.);
#59776=ADVANCED_FACE('',(#6676),#3623,.T.);
#59777=ADVANCED_FACE('',(#6677),#3624,.T.);
#59778=ADVANCED_FACE('',(#6678),#3625,.T.);
#59779=ADVANCED_FACE('',(#6679),#3626,.T.);
#59780=ADVANCED_FACE('',(#6680),#3627,.T.);
#59781=ADVANCED_FACE('',(#6681),#3628,.T.);
#59782=ADVANCED_FACE('',(#6682),#3629,.T.);
#59783=ADVANCED_FACE('',(#6683),#3630,.T.);
#59784=ADVANCED_FACE('',(#6684),#3631,.T.);
#59785=ADVANCED_FACE('',(#6685),#3632,.T.);
#59786=ADVANCED_FACE('',(#6686),#3633,.T.);
#59787=ADVANCED_FACE('',(#6687),#3634,.T.);
#59788=ADVANCED_FACE('',(#6688),#3635,.T.);
#59789=ADVANCED_FACE('',(#6689),#3636,.T.);
#59790=ADVANCED_FACE('',(#6690),#3637,.T.);
#59791=ADVANCED_FACE('',(#6691),#3638,.T.);
#59792=ADVANCED_FACE('',(#6692),#3639,.T.);
#59793=ADVANCED_FACE('',(#6693),#3640,.T.);
#59794=ADVANCED_FACE('',(#6694),#3641,.T.);
#59795=ADVANCED_FACE('',(#6695),#3642,.T.);
#59796=ADVANCED_FACE('',(#6696),#3643,.T.);
#59797=ADVANCED_FACE('',(#6697),#3644,.T.);
#59798=ADVANCED_FACE('',(#6698),#3645,.T.);
#59799=ADVANCED_FACE('',(#6699),#3646,.T.);
#59800=ADVANCED_FACE('',(#6700),#3647,.T.);
#59801=ADVANCED_FACE('',(#6701),#3648,.T.);
#59802=ADVANCED_FACE('',(#6702),#3649,.T.);
#59803=ADVANCED_FACE('',(#6703),#3650,.T.);
#59804=ADVANCED_FACE('',(#6704),#3651,.T.);
#59805=ADVANCED_FACE('',(#6705),#3652,.T.);
#59806=ADVANCED_FACE('',(#6706),#3653,.T.);
#59807=ADVANCED_FACE('',(#6707),#3654,.T.);
#59808=ADVANCED_FACE('',(#6708),#3655,.T.);
#59809=ADVANCED_FACE('',(#6709),#3656,.T.);
#59810=ADVANCED_FACE('',(#6710),#3657,.T.);
#59811=ADVANCED_FACE('',(#6711),#3658,.T.);
#59812=ADVANCED_FACE('',(#6712),#3659,.T.);
#59813=ADVANCED_FACE('',(#6713),#3660,.T.);
#59814=ADVANCED_FACE('',(#6714),#3661,.T.);
#59815=ADVANCED_FACE('',(#6715),#3662,.T.);
#59816=ADVANCED_FACE('',(#6716),#3663,.T.);
#59817=ADVANCED_FACE('',(#6717),#3664,.T.);
#59818=ADVANCED_FACE('',(#6718),#3665,.T.);
#59819=ADVANCED_FACE('',(#6719),#3666,.T.);
#59820=ADVANCED_FACE('',(#6720),#3667,.T.);
#59821=ADVANCED_FACE('',(#6721),#3668,.T.);
#59822=ADVANCED_FACE('',(#6722),#3669,.T.);
#59823=ADVANCED_FACE('',(#6723),#3670,.T.);
#59824=ADVANCED_FACE('',(#6724),#3671,.T.);
#59825=ADVANCED_FACE('',(#6725),#3672,.T.);
#59826=ADVANCED_FACE('',(#6726),#3673,.T.);
#59827=ADVANCED_FACE('',(#6727),#3674,.T.);
#59828=ADVANCED_FACE('',(#6728),#3675,.T.);
#59829=ADVANCED_FACE('',(#6729),#3676,.T.);
#59830=ADVANCED_FACE('',(#6730),#3677,.T.);
#59831=ADVANCED_FACE('',(#6731),#3678,.T.);
#59832=ADVANCED_FACE('',(#6732),#3679,.T.);
#59833=ADVANCED_FACE('',(#6733),#3680,.T.);
#59834=ADVANCED_FACE('',(#6734),#3681,.T.);
#59835=ADVANCED_FACE('',(#6735),#3682,.T.);
#59836=ADVANCED_FACE('',(#6736),#3683,.T.);
#59837=ADVANCED_FACE('',(#6737),#3684,.T.);
#59838=ADVANCED_FACE('',(#6738),#3685,.T.);
#59839=ADVANCED_FACE('',(#6739),#3686,.T.);
#59840=ADVANCED_FACE('',(#6740),#3687,.T.);
#59841=ADVANCED_FACE('',(#6741),#3688,.T.);
#59842=ADVANCED_FACE('',(#6742),#3689,.T.);
#59843=ADVANCED_FACE('',(#6743),#3690,.T.);
#59844=ADVANCED_FACE('',(#6744),#3691,.T.);
#59845=ADVANCED_FACE('',(#6745),#3692,.T.);
#59846=ADVANCED_FACE('',(#6746),#3693,.T.);
#59847=ADVANCED_FACE('',(#6747),#3694,.T.);
#59848=ADVANCED_FACE('',(#6748),#3695,.F.);
#60399=CLOSED_SHELL('',(#59333,#59334,#59335,#59336,#59337,#59338,#59339,
#59340,#59341,#59342,#59343,#59344,#59345,#59346,#59347,#59348,#59349,#59350,
#59351,#59352,#59353,#59354,#59355,#59356,#59357,#59358,#59359,#59360,#59361,
#59362,#59363,#59364,#59365,#59366,#59367,#59368,#59369,#59370,#59371,#59372,
#59373,#59374,#59375,#59376,#59377,#59378,#59379,#59380,#59381,#59382,#59383,
#59384,#59385,#59386,#59387,#59388,#59389,#59390,#59391,#59392,#59393,#59394,
#59395,#59396,#59397,#59398,#59399,#59400,#59401,#59402,#59403,#59404,#59405,
#59406,#59407,#59408,#59409,#59410,#59411,#59412,#59413,#59414,#59415,#59416,
#59417,#59418,#59419,#59420,#59421,#59422,#59423,#59424,#59425,#59426,#59427,
#59428,#59429,#59430,#59431,#59432,#59433,#59434,#59435,#59436,#59437,#59438,
#59439,#59440,#59441,#59442,#59443,#59444,#59445,#59446,#59447,#59448,#59449,
#59450,#59451,#59452,#59453,#59454,#59455,#59456,#59457,#59458,#59459,#59460,
#59461,#59462,#59463,#59464,#59465,#59466,#59467,#59468,#59469,#59470,#59471,
#59472,#59473,#59474,#59475,#59476,#59477,#59478,#59479,#59480,#59481,#59482,
#59483,#59484,#59485,#59486,#59487,#59488,#59489,#59490,#59491,#59492,#59493,
#59494,#59495,#59496,#59497,#59498,#59499,#59500,#59501,#59502,#59503,#59504,
#59505,#59506,#59507,#59508,#59509,#59510,#59511,#59512,#59513,#59514,#59515,
#59516,#59517,#59518,#59519,#59520,#59521,#59522,#59523,#59524,#59525,#59526,
#59527,#59528,#59529,#59530,#59531,#59532,#59533,#59534,#59535,#59536,#59537,
#59538,#59539,#59540,#59541,#59542,#59543,#59544,#59545,#59546,#59547,#59548,
#59549,#59550,#59551,#59552,#59553,#59554,#59555,#59556,#59557,#59558,#59559,
#59560,#59561,#59562,#59563,#59564,#59565,#59566,#59567,#59568,#59569,#59570,
#59571,#59572,#59573,#59574,#59575,#59576,#59577,#59578,#59579,#59580,#59581,
#59582,#59583,#59584,#59585,#59586,#59587,#59588,#59589,#59590,#59591,#59592,
#59593,#59594,#59595,#59596,#59597,#59598,#59599,#59600,#59601,#59602,#59603,
#59604,#59605,#59606,#59607,#59608,#59609,#59610,#59611,#59612,#59613,#59614,
#59615,#59616,#59617,#59618,#59619,#59620,#59621,#59622,#59623,#59624,#59625,
#59626,#59627,#59628,#59629,#59630,#59631,#59632,#59633,#59634,#59635,#59636,
#59637,#59638,#59639,#59640,#59641,#59642,#59643,#59644,#59645,#59646,#59647,
#59648,#59649,#59650,#59651,#59652,#59653,#59654,#59655,#59656,#59657,#59658,
#59659,#59660,#59661,#59662,#59663,#59664,#59665,#59666,#59667,#59668,#59669,
#59670,#59671,#59672,#59673,#59674,#59675,#59676,#59677,#59678,#59679,#59680,
#59681,#59682,#59683,#59684,#59685,#59686,#59687,#59688,#59689,#59690,#59691,
#59692,#59693,#59694,#59695,#59696,#59697,#59698,#59699,#59700,#59701,#59702,
#59703,#59704,#59705,#59706,#59707,#59708,#59709,#59710,#59711,#59712,#59713,
#59714,#59715,#59716,#59717,#59718,#59719,#59720,#59721,#59722,#59723,#59724,
#59725,#59726,#59727,#59728,#59729,#59730,#59731,#59732,#59733,#59734,#59735,
#59736,#59737,#59738,#59739,#59740,#59741,#59742,#59743,#59744,#59745,#59746,
#59747,#59748,#59749,#59750,#59751,#59752,#59753,#59754,#59755,#59756,#59757,
#59758,#59759,#59760,#59761,#59762,#59763,#59764,#59765,#59766,#59767,#59768,
#59769,#59770,#59771,#59772,#59773,#59774,#59775,#59776,#59777,#59778,#59779,
#59780,#59781,#59782,#59783,#59784,#59785,#59786,#59787,#59788,#59789,#59790,
#59791,#59792,#59793,#59794,#59795,#59796,#59797,#59798,#59799,#59800,#59801,
#59802,#59803,#59804,#59805,#59806,#59807,#59808,#59809,#59810,#59811,#59812,
#59813,#59814,#59815,#59816,#59817,#59818,#59819,#59820,#59821,#59822,#59823,
#59824,#59825,#59826,#59827,#59828,#59829,#59830,#59831,#59832,#59833,#59834,
#59835,#59836,#59837,#59838,#59839,#59840,#59841,#59842,#59843,#59844,#59845,
#59846,#59847,#59848));
#62396=AXIS2_PLACEMENT_3D('',#98945,#71111,#71112);
#62397=AXIS2_PLACEMENT_3D('',#98946,#71113,#71114);
#62398=AXIS2_PLACEMENT_3D('',#98948,#71115,#71116);
#62399=AXIS2_PLACEMENT_3D('',#98951,#71118,#71119);
#62400=AXIS2_PLACEMENT_3D('',#98952,#71120,#71121);
#62401=AXIS2_PLACEMENT_3D('',#98955,#71123,#71124);
#62402=AXIS2_PLACEMENT_3D('',#98956,#71125,#71126);
#62403=AXIS2_PLACEMENT_3D('',#98965,#71131,#71132);
#62404=AXIS2_PLACEMENT_3D('',#98967,#71133,#71134);
#62405=AXIS2_PLACEMENT_3D('',#98970,#71136,#71137);
#62406=AXIS2_PLACEMENT_3D('',#98971,#71138,#71139);
#62407=AXIS2_PLACEMENT_3D('',#98974,#71141,#71142);
#62408=AXIS2_PLACEMENT_3D('',#98975,#71143,#71144);
#62409=AXIS2_PLACEMENT_3D('',#98984,#71149,#71150);
#62410=AXIS2_PLACEMENT_3D('',#98986,#71151,#71152);
#62411=AXIS2_PLACEMENT_3D('',#98987,#71153,#71154);
#62412=AXIS2_PLACEMENT_3D('',#98989,#71155,#71156);
#62413=AXIS2_PLACEMENT_3D('',#98990,#71157,#71158);
#62414=AXIS2_PLACEMENT_3D('',#98993,#71160,#71161);
#62415=AXIS2_PLACEMENT_3D('',#98994,#71162,#71163);
#62416=AXIS2_PLACEMENT_3D('',#98997,#71165,#71166);
#62417=AXIS2_PLACEMENT_3D('',#98998,#71167,#71168);
#62418=AXIS2_PLACEMENT_3D('',#99007,#71173,#71174);
#62419=AXIS2_PLACEMENT_3D('',#99014,#71179,#71180);
#62420=AXIS2_PLACEMENT_3D('',#99018,#71183,#71184);
#62421=AXIS2_PLACEMENT_3D('',#99022,#71187,#71188);
#62422=AXIS2_PLACEMENT_3D('',#99028,#71192,#71193);
#62423=AXIS2_PLACEMENT_3D('',#99034,#71197,#71198);
#62424=AXIS2_PLACEMENT_3D('',#99040,#71202,#71203);
#62425=AXIS2_PLACEMENT_3D('',#99046,#71207,#71208);
#62426=AXIS2_PLACEMENT_3D('',#99052,#71212,#71213);
#62427=AXIS2_PLACEMENT_3D('',#99058,#71217,#71218);
#62428=AXIS2_PLACEMENT_3D('',#99064,#71222,#71223);
#62429=AXIS2_PLACEMENT_3D('',#99070,#71227,#71228);
#62430=AXIS2_PLACEMENT_3D('',#99076,#71232,#71233);
#62431=AXIS2_PLACEMENT_3D('',#99082,#71237,#71238);
#62432=AXIS2_PLACEMENT_3D('',#99088,#71242,#71243);
#62433=AXIS2_PLACEMENT_3D('',#99094,#71247,#71248);
#62434=AXIS2_PLACEMENT_3D('',#99100,#71252,#71253);
#62435=AXIS2_PLACEMENT_3D('',#99106,#71257,#71258);
#62436=AXIS2_PLACEMENT_3D('',#99112,#71262,#71263);
#62437=AXIS2_PLACEMENT_3D('',#99118,#71267,#71268);
#62438=AXIS2_PLACEMENT_3D('',#99124,#71272,#71273);
#62439=AXIS2_PLACEMENT_3D('',#99130,#71277,#71278);
#62440=AXIS2_PLACEMENT_3D('',#99136,#71282,#71283);
#62441=AXIS2_PLACEMENT_3D('',#99142,#71287,#71288);
#62442=AXIS2_PLACEMENT_3D('',#99148,#71292,#71293);
#62443=AXIS2_PLACEMENT_3D('',#99154,#71297,#71298);
#62444=AXIS2_PLACEMENT_3D('',#99160,#71302,#71303);
#62445=AXIS2_PLACEMENT_3D('',#99166,#71307,#71308);
#62446=AXIS2_PLACEMENT_3D('',#99172,#71312,#71313);
#62447=AXIS2_PLACEMENT_3D('',#99178,#71317,#71318);
#62448=AXIS2_PLACEMENT_3D('',#99184,#71322,#71323);
#62449=AXIS2_PLACEMENT_3D('',#99190,#71327,#71328);
#62450=AXIS2_PLACEMENT_3D('',#99196,#71332,#71333);
#62451=AXIS2_PLACEMENT_3D('',#99202,#71337,#71338);
#62452=AXIS2_PLACEMENT_3D('',#99208,#71342,#71343);
#62453=AXIS2_PLACEMENT_3D('',#99214,#71347,#71348);
#62454=AXIS2_PLACEMENT_3D('',#99220,#71352,#71353);
#62455=AXIS2_PLACEMENT_3D('',#99226,#71357,#71358);
#62456=AXIS2_PLACEMENT_3D('',#99232,#71362,#71363);
#62457=AXIS2_PLACEMENT_3D('',#99238,#71367,#71368);
#62458=AXIS2_PLACEMENT_3D('',#99244,#71372,#71373);
#62459=AXIS2_PLACEMENT_3D('',#99250,#71377,#71378);
#62460=AXIS2_PLACEMENT_3D('',#99256,#71382,#71383);
#62461=AXIS2_PLACEMENT_3D('',#99262,#71387,#71388);
#62462=AXIS2_PLACEMENT_3D('',#99268,#71392,#71393);
#62463=AXIS2_PLACEMENT_3D('',#99274,#71397,#71398);
#62464=AXIS2_PLACEMENT_3D('',#99280,#71402,#71403);
#62465=AXIS2_PLACEMENT_3D('',#99286,#71407,#71408);
#62466=AXIS2_PLACEMENT_3D('',#99292,#71412,#71413);
#62467=AXIS2_PLACEMENT_3D('',#99298,#71417,#71418);
#62468=AXIS2_PLACEMENT_3D('',#99304,#71422,#71423);
#62469=AXIS2_PLACEMENT_3D('',#99310,#71427,#71428);
#62470=AXIS2_PLACEMENT_3D('',#99316,#71432,#71433);
#62471=AXIS2_PLACEMENT_3D('',#99322,#71437,#71438);
#62472=AXIS2_PLACEMENT_3D('',#99328,#71442,#71443);
#62473=AXIS2_PLACEMENT_3D('',#99334,#71447,#71448);
#62474=AXIS2_PLACEMENT_3D('',#99340,#71452,#71453);
#62475=AXIS2_PLACEMENT_3D('',#99346,#71457,#71458);
#62476=AXIS2_PLACEMENT_3D('',#99352,#71462,#71463);
#62477=AXIS2_PLACEMENT_3D('',#99358,#71467,#71468);
#62478=AXIS2_PLACEMENT_3D('',#99364,#71472,#71473);
#62479=AXIS2_PLACEMENT_3D('',#99370,#71477,#71478);
#62480=AXIS2_PLACEMENT_3D('',#99376,#71482,#71483);
#62481=AXIS2_PLACEMENT_3D('',#99382,#71487,#71488);
#62482=AXIS2_PLACEMENT_3D('',#99388,#71492,#71493);
#62483=AXIS2_PLACEMENT_3D('',#99394,#71497,#71498);
#62484=AXIS2_PLACEMENT_3D('',#99400,#71502,#71503);
#62485=AXIS2_PLACEMENT_3D('',#99406,#71507,#71508);
#62486=AXIS2_PLACEMENT_3D('',#99412,#71512,#71513);
#62487=AXIS2_PLACEMENT_3D('',#99418,#71517,#71518);
#62488=AXIS2_PLACEMENT_3D('',#99424,#71522,#71523);
#62489=AXIS2_PLACEMENT_3D('',#99430,#71527,#71528);
#62490=AXIS2_PLACEMENT_3D('',#99436,#71532,#71533);
#62491=AXIS2_PLACEMENT_3D('',#99442,#71537,#71538);
#62492=AXIS2_PLACEMENT_3D('',#99448,#71542,#71543);
#62493=AXIS2_PLACEMENT_3D('',#99454,#71547,#71548);
#62494=AXIS2_PLACEMENT_3D('',#99460,#71552,#71553);
#62495=AXIS2_PLACEMENT_3D('',#99466,#71557,#71558);
#62496=AXIS2_PLACEMENT_3D('',#99472,#71562,#71563);
#62497=AXIS2_PLACEMENT_3D('',#99478,#71567,#71568);
#62498=AXIS2_PLACEMENT_3D('',#99484,#71572,#71573);
#62499=AXIS2_PLACEMENT_3D('',#99490,#71577,#71578);
#62500=AXIS2_PLACEMENT_3D('',#99496,#71582,#71583);
#62501=AXIS2_PLACEMENT_3D('',#99502,#71587,#71588);
#62502=AXIS2_PLACEMENT_3D('',#99508,#71592,#71593);
#62503=AXIS2_PLACEMENT_3D('',#99514,#71597,#71598);
#62504=AXIS2_PLACEMENT_3D('',#99520,#71602,#71603);
#62505=AXIS2_PLACEMENT_3D('',#99526,#71607,#71608);
#62506=AXIS2_PLACEMENT_3D('',#99532,#71612,#71613);
#62507=AXIS2_PLACEMENT_3D('',#99538,#71617,#71618);
#62508=AXIS2_PLACEMENT_3D('',#99544,#71622,#71623);
#62509=AXIS2_PLACEMENT_3D('',#99550,#71627,#71628);
#62510=AXIS2_PLACEMENT_3D('',#99556,#71632,#71633);
#62511=AXIS2_PLACEMENT_3D('',#99562,#71637,#71638);
#62512=AXIS2_PLACEMENT_3D('',#99568,#71642,#71643);
#62513=AXIS2_PLACEMENT_3D('',#99574,#71647,#71648);
#62514=AXIS2_PLACEMENT_3D('',#99580,#71652,#71653);
#62515=AXIS2_PLACEMENT_3D('',#99586,#71657,#71658);
#62516=AXIS2_PLACEMENT_3D('',#99592,#71662,#71663);
#62517=AXIS2_PLACEMENT_3D('',#99598,#71667,#71668);
#62518=AXIS2_PLACEMENT_3D('',#99604,#71672,#71673);
#62519=AXIS2_PLACEMENT_3D('',#99610,#71677,#71678);
#62520=AXIS2_PLACEMENT_3D('',#99616,#71682,#71683);
#62521=AXIS2_PLACEMENT_3D('',#99622,#71687,#71688);
#62522=AXIS2_PLACEMENT_3D('',#99628,#71692,#71693);
#62523=AXIS2_PLACEMENT_3D('',#99634,#71697,#71698);
#62524=AXIS2_PLACEMENT_3D('',#99640,#71702,#71703);
#62525=AXIS2_PLACEMENT_3D('',#99646,#71707,#71708);
#62526=AXIS2_PLACEMENT_3D('',#99652,#71712,#71713);
#62527=AXIS2_PLACEMENT_3D('',#99658,#71717,#71718);
#62528=AXIS2_PLACEMENT_3D('',#99664,#71722,#71723);
#62529=AXIS2_PLACEMENT_3D('',#99670,#71727,#71728);
#62530=AXIS2_PLACEMENT_3D('',#99676,#71732,#71733);
#62531=AXIS2_PLACEMENT_3D('',#99682,#71737,#71738);
#62532=AXIS2_PLACEMENT_3D('',#99688,#71742,#71743);
#62533=AXIS2_PLACEMENT_3D('',#99694,#71747,#71748);
#62534=AXIS2_PLACEMENT_3D('',#99700,#71752,#71753);
#62535=AXIS2_PLACEMENT_3D('',#99706,#71757,#71758);
#62536=AXIS2_PLACEMENT_3D('',#99712,#71762,#71763);
#62537=AXIS2_PLACEMENT_3D('',#99718,#71767,#71768);
#62538=AXIS2_PLACEMENT_3D('',#99724,#71772,#71773);
#62539=AXIS2_PLACEMENT_3D('',#99730,#71777,#71778);
#62540=AXIS2_PLACEMENT_3D('',#99736,#71782,#71783);
#62541=AXIS2_PLACEMENT_3D('',#99742,#71787,#71788);
#62542=AXIS2_PLACEMENT_3D('',#99748,#71792,#71793);
#62543=AXIS2_PLACEMENT_3D('',#99754,#71797,#71798);
#62544=AXIS2_PLACEMENT_3D('',#99760,#71802,#71803);
#62545=AXIS2_PLACEMENT_3D('',#99766,#71807,#71808);
#62546=AXIS2_PLACEMENT_3D('',#99772,#71812,#71813);
#62547=AXIS2_PLACEMENT_3D('',#99778,#71817,#71818);
#62548=AXIS2_PLACEMENT_3D('',#99784,#71822,#71823);
#62549=AXIS2_PLACEMENT_3D('',#99790,#71827,#71828);
#62550=AXIS2_PLACEMENT_3D('',#99796,#71832,#71833);
#62551=AXIS2_PLACEMENT_3D('',#99802,#71837,#71838);
#62552=AXIS2_PLACEMENT_3D('',#99808,#71842,#71843);
#62553=AXIS2_PLACEMENT_3D('',#99814,#71847,#71848);
#62554=AXIS2_PLACEMENT_3D('',#99820,#71852,#71853);
#62555=AXIS2_PLACEMENT_3D('',#99826,#71857,#71858);
#62556=AXIS2_PLACEMENT_3D('',#99832,#71862,#71863);
#62557=AXIS2_PLACEMENT_3D('',#99838,#71867,#71868);
#62558=AXIS2_PLACEMENT_3D('',#99844,#71872,#71873);
#62559=AXIS2_PLACEMENT_3D('',#99850,#71877,#71878);
#62560=AXIS2_PLACEMENT_3D('',#99856,#71882,#71883);
#62561=AXIS2_PLACEMENT_3D('',#99862,#71887,#71888);
#62562=AXIS2_PLACEMENT_3D('',#99868,#71892,#71893);
#62563=AXIS2_PLACEMENT_3D('',#99874,#71897,#71898);
#62564=AXIS2_PLACEMENT_3D('',#99880,#71902,#71903);
#62565=AXIS2_PLACEMENT_3D('',#99886,#71907,#71908);
#62566=AXIS2_PLACEMENT_3D('',#99892,#71912,#71913);
#62567=AXIS2_PLACEMENT_3D('',#99898,#71917,#71918);
#62568=AXIS2_PLACEMENT_3D('',#99904,#71922,#71923);
#62569=AXIS2_PLACEMENT_3D('',#99910,#71927,#71928);
#62570=AXIS2_PLACEMENT_3D('',#99916,#71932,#71933);
#62571=AXIS2_PLACEMENT_3D('',#99922,#71937,#71938);
#62572=AXIS2_PLACEMENT_3D('',#99928,#71942,#71943);
#62573=AXIS2_PLACEMENT_3D('',#99934,#71947,#71948);
#62574=AXIS2_PLACEMENT_3D('',#99940,#71952,#71953);
#62575=AXIS2_PLACEMENT_3D('',#99946,#71957,#71958);
#62576=AXIS2_PLACEMENT_3D('',#99952,#71962,#71963);
#62577=AXIS2_PLACEMENT_3D('',#99958,#71967,#71968);
#62578=AXIS2_PLACEMENT_3D('',#99964,#71972,#71973);
#62579=AXIS2_PLACEMENT_3D('',#99970,#71977,#71978);
#62580=AXIS2_PLACEMENT_3D('',#99976,#71982,#71983);
#62581=AXIS2_PLACEMENT_3D('',#99982,#71987,#71988);
#62582=AXIS2_PLACEMENT_3D('',#99988,#71992,#71993);
#62583=AXIS2_PLACEMENT_3D('',#99994,#71997,#71998);
#62584=AXIS2_PLACEMENT_3D('',#100000,#72002,#72003);
#62585=AXIS2_PLACEMENT_3D('',#100006,#72007,#72008);
#62586=AXIS2_PLACEMENT_3D('',#100012,#72012,#72013);
#62587=AXIS2_PLACEMENT_3D('',#100018,#72017,#72018);
#62588=AXIS2_PLACEMENT_3D('',#100024,#72022,#72023);
#62589=AXIS2_PLACEMENT_3D('',#100030,#72027,#72028);
#62590=AXIS2_PLACEMENT_3D('',#100036,#72032,#72033);
#62591=AXIS2_PLACEMENT_3D('',#100042,#72037,#72038);
#62592=AXIS2_PLACEMENT_3D('',#100048,#72042,#72043);
#62593=AXIS2_PLACEMENT_3D('',#100054,#72047,#72048);
#62594=AXIS2_PLACEMENT_3D('',#100060,#72052,#72053);
#62595=AXIS2_PLACEMENT_3D('',#100066,#72057,#72058);
#62596=AXIS2_PLACEMENT_3D('',#100072,#72062,#72063);
#62597=AXIS2_PLACEMENT_3D('',#100078,#72067,#72068);
#62598=AXIS2_PLACEMENT_3D('',#100084,#72072,#72073);
#62599=AXIS2_PLACEMENT_3D('',#100090,#72077,#72078);
#62600=AXIS2_PLACEMENT_3D('',#100096,#72082,#72083);
#62601=AXIS2_PLACEMENT_3D('',#100102,#72087,#72088);
#62602=AXIS2_PLACEMENT_3D('',#100108,#72092,#72093);
#62603=AXIS2_PLACEMENT_3D('',#100114,#72097,#72098);
#62604=AXIS2_PLACEMENT_3D('',#100120,#72102,#72103);
#62605=AXIS2_PLACEMENT_3D('',#100126,#72107,#72108);
#62606=AXIS2_PLACEMENT_3D('',#100132,#72112,#72113);
#62607=AXIS2_PLACEMENT_3D('',#100138,#72117,#72118);
#62608=AXIS2_PLACEMENT_3D('',#100144,#72122,#72123);
#62609=AXIS2_PLACEMENT_3D('',#100150,#72127,#72128);
#62610=AXIS2_PLACEMENT_3D('',#100156,#72132,#72133);
#62611=AXIS2_PLACEMENT_3D('',#100162,#72137,#72138);
#62612=AXIS2_PLACEMENT_3D('',#100168,#72142,#72143);
#62613=AXIS2_PLACEMENT_3D('',#100174,#72147,#72148);
#62614=AXIS2_PLACEMENT_3D('',#100180,#72152,#72153);
#62615=AXIS2_PLACEMENT_3D('',#100186,#72157,#72158);
#62616=AXIS2_PLACEMENT_3D('',#100192,#72162,#72163);
#62617=AXIS2_PLACEMENT_3D('',#100198,#72167,#72168);
#62618=AXIS2_PLACEMENT_3D('',#100204,#72172,#72173);
#62619=AXIS2_PLACEMENT_3D('',#100210,#72177,#72178);
#62620=AXIS2_PLACEMENT_3D('',#100216,#72182,#72183);
#62621=AXIS2_PLACEMENT_3D('',#100222,#72187,#72188);
#62622=AXIS2_PLACEMENT_3D('',#100228,#72192,#72193);
#62623=AXIS2_PLACEMENT_3D('',#100234,#72197,#72198);
#62624=AXIS2_PLACEMENT_3D('',#100240,#72202,#72203);
#62625=AXIS2_PLACEMENT_3D('',#100246,#72207,#72208);
#62626=AXIS2_PLACEMENT_3D('',#100252,#72212,#72213);
#62627=AXIS2_PLACEMENT_3D('',#100258,#72217,#72218);
#62628=AXIS2_PLACEMENT_3D('',#100264,#72222,#72223);
#62629=AXIS2_PLACEMENT_3D('',#100270,#72227,#72228);
#62630=AXIS2_PLACEMENT_3D('',#100276,#72232,#72233);
#62631=AXIS2_PLACEMENT_3D('',#100282,#72237,#72238);
#62632=AXIS2_PLACEMENT_3D('',#100288,#72242,#72243);
#62633=AXIS2_PLACEMENT_3D('',#100294,#72247,#72248);
#62634=AXIS2_PLACEMENT_3D('',#100300,#72252,#72253);
#62635=AXIS2_PLACEMENT_3D('',#100306,#72257,#72258);
#62636=AXIS2_PLACEMENT_3D('',#100312,#72262,#72263);
#62637=AXIS2_PLACEMENT_3D('',#100318,#72267,#72268);
#62638=AXIS2_PLACEMENT_3D('',#100324,#72272,#72273);
#62639=AXIS2_PLACEMENT_3D('',#100330,#72277,#72278);
#62640=AXIS2_PLACEMENT_3D('',#100336,#72282,#72283);
#62641=AXIS2_PLACEMENT_3D('',#100342,#72287,#72288);
#62642=AXIS2_PLACEMENT_3D('',#100348,#72292,#72293);
#62643=AXIS2_PLACEMENT_3D('',#100354,#72297,#72298);
#62644=AXIS2_PLACEMENT_3D('',#100360,#72302,#72303);
#62645=AXIS2_PLACEMENT_3D('',#100366,#72307,#72308);
#62646=AXIS2_PLACEMENT_3D('',#100372,#72312,#72313);
#62647=AXIS2_PLACEMENT_3D('',#100378,#72317,#72318);
#62648=AXIS2_PLACEMENT_3D('',#100384,#72322,#72323);
#62649=AXIS2_PLACEMENT_3D('',#100390,#72327,#72328);
#62650=AXIS2_PLACEMENT_3D('',#100396,#72332,#72333);
#62651=AXIS2_PLACEMENT_3D('',#100402,#72337,#72338);
#62652=AXIS2_PLACEMENT_3D('',#100408,#72342,#72343);
#62653=AXIS2_PLACEMENT_3D('',#100414,#72347,#72348);
#62654=AXIS2_PLACEMENT_3D('',#100420,#72352,#72353);
#62655=AXIS2_PLACEMENT_3D('',#100426,#72357,#72358);
#62656=AXIS2_PLACEMENT_3D('',#100432,#72362,#72363);
#62657=AXIS2_PLACEMENT_3D('',#100438,#72367,#72368);
#62658=AXIS2_PLACEMENT_3D('',#100444,#72372,#72373);
#62659=AXIS2_PLACEMENT_3D('',#100450,#72377,#72378);
#62660=AXIS2_PLACEMENT_3D('',#100456,#72382,#72383);
#62661=AXIS2_PLACEMENT_3D('',#100462,#72387,#72388);
#62662=AXIS2_PLACEMENT_3D('',#100468,#72392,#72393);
#62663=AXIS2_PLACEMENT_3D('',#100474,#72397,#72398);
#62664=AXIS2_PLACEMENT_3D('',#100480,#72402,#72403);
#62665=AXIS2_PLACEMENT_3D('',#100486,#72407,#72408);
#62666=AXIS2_PLACEMENT_3D('',#100492,#72412,#72413);
#62667=AXIS2_PLACEMENT_3D('',#100498,#72417,#72418);
#62668=AXIS2_PLACEMENT_3D('',#100504,#72422,#72423);
#62669=AXIS2_PLACEMENT_3D('',#100510,#72427,#72428);
#62670=AXIS2_PLACEMENT_3D('',#100516,#72432,#72433);
#62671=AXIS2_PLACEMENT_3D('',#100522,#72437,#72438);
#62672=AXIS2_PLACEMENT_3D('',#100528,#72442,#72443);
#62673=AXIS2_PLACEMENT_3D('',#100534,#72447,#72448);
#62674=AXIS2_PLACEMENT_3D('',#100540,#72452,#72453);
#62675=AXIS2_PLACEMENT_3D('',#100546,#72457,#72458);
#62676=AXIS2_PLACEMENT_3D('',#100552,#72462,#72463);
#62677=AXIS2_PLACEMENT_3D('',#100558,#72467,#72468);
#62678=AXIS2_PLACEMENT_3D('',#100564,#72472,#72473);
#62679=AXIS2_PLACEMENT_3D('',#100570,#72477,#72478);
#62680=AXIS2_PLACEMENT_3D('',#100576,#72482,#72483);
#62681=AXIS2_PLACEMENT_3D('',#100582,#72487,#72488);
#62682=AXIS2_PLACEMENT_3D('',#100588,#72492,#72493);
#62683=AXIS2_PLACEMENT_3D('',#100594,#72497,#72498);
#62684=AXIS2_PLACEMENT_3D('',#100600,#72502,#72503);
#62685=AXIS2_PLACEMENT_3D('',#100606,#72507,#72508);
#62686=AXIS2_PLACEMENT_3D('',#100612,#72512,#72513);
#62687=AXIS2_PLACEMENT_3D('',#100618,#72517,#72518);
#62688=AXIS2_PLACEMENT_3D('',#100624,#72522,#72523);
#62689=AXIS2_PLACEMENT_3D('',#100630,#72527,#72528);
#62690=AXIS2_PLACEMENT_3D('',#100636,#72532,#72533);
#62691=AXIS2_PLACEMENT_3D('',#100642,#72537,#72538);
#62692=AXIS2_PLACEMENT_3D('',#100648,#72542,#72543);
#62693=AXIS2_PLACEMENT_3D('',#100654,#72547,#72548);
#62694=AXIS2_PLACEMENT_3D('',#100660,#72552,#72553);
#62695=AXIS2_PLACEMENT_3D('',#100666,#72557,#72558);
#62696=AXIS2_PLACEMENT_3D('',#100672,#72562,#72563);
#62697=AXIS2_PLACEMENT_3D('',#100678,#72567,#72568);
#62698=AXIS2_PLACEMENT_3D('',#100684,#72572,#72573);
#62699=AXIS2_PLACEMENT_3D('',#100690,#72577,#72578);
#62700=AXIS2_PLACEMENT_3D('',#100696,#72582,#72583);
#62701=AXIS2_PLACEMENT_3D('',#100702,#72587,#72588);
#62702=AXIS2_PLACEMENT_3D('',#100708,#72592,#72593);
#62703=AXIS2_PLACEMENT_3D('',#100714,#72597,#72598);
#62704=AXIS2_PLACEMENT_3D('',#100720,#72602,#72603);
#62705=AXIS2_PLACEMENT_3D('',#100726,#72607,#72608);
#62706=AXIS2_PLACEMENT_3D('',#100732,#72612,#72613);
#62707=AXIS2_PLACEMENT_3D('',#100738,#72617,#72618);
#62708=AXIS2_PLACEMENT_3D('',#100744,#72622,#72623);
#62709=AXIS2_PLACEMENT_3D('',#100750,#72627,#72628);
#62710=AXIS2_PLACEMENT_3D('',#100756,#72632,#72633);
#62711=AXIS2_PLACEMENT_3D('',#100762,#72637,#72638);
#62712=AXIS2_PLACEMENT_3D('',#100768,#72642,#72643);
#62713=AXIS2_PLACEMENT_3D('',#100774,#72647,#72648);
#62714=AXIS2_PLACEMENT_3D('',#100780,#72652,#72653);
#62715=AXIS2_PLACEMENT_3D('',#100786,#72657,#72658);
#62716=AXIS2_PLACEMENT_3D('',#100792,#72662,#72663);
#62717=AXIS2_PLACEMENT_3D('',#100798,#72667,#72668);
#62718=AXIS2_PLACEMENT_3D('',#100804,#72672,#72673);
#62719=AXIS2_PLACEMENT_3D('',#100810,#72677,#72678);
#62720=AXIS2_PLACEMENT_3D('',#100816,#72682,#72683);
#62721=AXIS2_PLACEMENT_3D('',#100822,#72687,#72688);
#62722=AXIS2_PLACEMENT_3D('',#100828,#72692,#72693);
#62723=AXIS2_PLACEMENT_3D('',#100834,#72697,#72698);
#62724=AXIS2_PLACEMENT_3D('',#100840,#72702,#72703);
#62725=AXIS2_PLACEMENT_3D('',#100846,#72707,#72708);
#62726=AXIS2_PLACEMENT_3D('',#100852,#72712,#72713);
#62727=AXIS2_PLACEMENT_3D('',#100858,#72717,#72718);
#62728=AXIS2_PLACEMENT_3D('',#100864,#72722,#72723);
#62729=AXIS2_PLACEMENT_3D('',#100870,#72727,#72728);
#62730=AXIS2_PLACEMENT_3D('',#100876,#72732,#72733);
#62731=AXIS2_PLACEMENT_3D('',#100882,#72737,#72738);
#62732=AXIS2_PLACEMENT_3D('',#100888,#72742,#72743);
#62733=AXIS2_PLACEMENT_3D('',#100894,#72747,#72748);
#62734=AXIS2_PLACEMENT_3D('',#100900,#72752,#72753);
#62735=AXIS2_PLACEMENT_3D('',#100906,#72757,#72758);
#62736=AXIS2_PLACEMENT_3D('',#100912,#72762,#72763);
#62737=AXIS2_PLACEMENT_3D('',#100918,#72767,#72768);
#62738=AXIS2_PLACEMENT_3D('',#100924,#72772,#72773);
#62739=AXIS2_PLACEMENT_3D('',#100930,#72777,#72778);
#62740=AXIS2_PLACEMENT_3D('',#100936,#72782,#72783);
#62741=AXIS2_PLACEMENT_3D('',#100942,#72787,#72788);
#62742=AXIS2_PLACEMENT_3D('',#100948,#72792,#72793);
#62743=AXIS2_PLACEMENT_3D('',#100954,#72797,#72798);
#62744=AXIS2_PLACEMENT_3D('',#100960,#72802,#72803);
#62745=AXIS2_PLACEMENT_3D('',#100966,#72807,#72808);
#62746=AXIS2_PLACEMENT_3D('',#100972,#72812,#72813);
#62747=AXIS2_PLACEMENT_3D('',#100978,#72817,#72818);
#62748=AXIS2_PLACEMENT_3D('',#100984,#72822,#72823);
#62749=AXIS2_PLACEMENT_3D('',#100990,#72827,#72828);
#62750=AXIS2_PLACEMENT_3D('',#100996,#72832,#72833);
#62751=AXIS2_PLACEMENT_3D('',#101002,#72837,#72838);
#62752=AXIS2_PLACEMENT_3D('',#101008,#72842,#72843);
#62753=AXIS2_PLACEMENT_3D('',#101014,#72847,#72848);
#62754=AXIS2_PLACEMENT_3D('',#101020,#72852,#72853);
#62755=AXIS2_PLACEMENT_3D('',#101026,#72857,#72858);
#62756=AXIS2_PLACEMENT_3D('',#101032,#72862,#72863);
#62757=AXIS2_PLACEMENT_3D('',#101038,#72867,#72868);
#62758=AXIS2_PLACEMENT_3D('',#101044,#72872,#72873);
#62759=AXIS2_PLACEMENT_3D('',#101050,#72877,#72878);
#62760=AXIS2_PLACEMENT_3D('',#101056,#72882,#72883);
#62761=AXIS2_PLACEMENT_3D('',#101062,#72887,#72888);
#62762=AXIS2_PLACEMENT_3D('',#101068,#72892,#72893);
#62763=AXIS2_PLACEMENT_3D('',#101074,#72897,#72898);
#62764=AXIS2_PLACEMENT_3D('',#101080,#72902,#72903);
#62765=AXIS2_PLACEMENT_3D('',#101086,#72907,#72908);
#62766=AXIS2_PLACEMENT_3D('',#101092,#72912,#72913);
#62767=AXIS2_PLACEMENT_3D('',#101098,#72917,#72918);
#62768=AXIS2_PLACEMENT_3D('',#101104,#72922,#72923);
#62769=AXIS2_PLACEMENT_3D('',#101110,#72927,#72928);
#62770=AXIS2_PLACEMENT_3D('',#101116,#72932,#72933);
#62771=AXIS2_PLACEMENT_3D('',#101122,#72937,#72938);
#62772=AXIS2_PLACEMENT_3D('',#101128,#72942,#72943);
#62773=AXIS2_PLACEMENT_3D('',#101134,#72947,#72948);
#62774=AXIS2_PLACEMENT_3D('',#101140,#72952,#72953);
#62775=AXIS2_PLACEMENT_3D('',#101146,#72957,#72958);
#62776=AXIS2_PLACEMENT_3D('',#101152,#72962,#72963);
#62777=AXIS2_PLACEMENT_3D('',#101158,#72967,#72968);
#62778=AXIS2_PLACEMENT_3D('',#101164,#72972,#72973);
#62779=AXIS2_PLACEMENT_3D('',#101170,#72977,#72978);
#62780=AXIS2_PLACEMENT_3D('',#101176,#72982,#72983);
#62781=AXIS2_PLACEMENT_3D('',#101182,#72987,#72988);
#62782=AXIS2_PLACEMENT_3D('',#101188,#72992,#72993);
#62783=AXIS2_PLACEMENT_3D('',#101194,#72997,#72998);
#62784=AXIS2_PLACEMENT_3D('',#101200,#73002,#73003);
#62785=AXIS2_PLACEMENT_3D('',#101206,#73007,#73008);
#62786=AXIS2_PLACEMENT_3D('',#101212,#73012,#73013);
#62787=AXIS2_PLACEMENT_3D('',#101218,#73017,#73018);
#62788=AXIS2_PLACEMENT_3D('',#101224,#73022,#73023);
#62789=AXIS2_PLACEMENT_3D('',#101230,#73027,#73028);
#62790=AXIS2_PLACEMENT_3D('',#101236,#73032,#73033);
#62791=AXIS2_PLACEMENT_3D('',#101242,#73037,#73038);
#62792=AXIS2_PLACEMENT_3D('',#101248,#73042,#73043);
#62793=AXIS2_PLACEMENT_3D('',#101254,#73047,#73048);
#62794=AXIS2_PLACEMENT_3D('',#101260,#73052,#73053);
#62795=AXIS2_PLACEMENT_3D('',#101266,#73057,#73058);
#62796=AXIS2_PLACEMENT_3D('',#101272,#73062,#73063);
#62797=AXIS2_PLACEMENT_3D('',#101278,#73067,#73068);
#62798=AXIS2_PLACEMENT_3D('',#101284,#73072,#73073);
#62799=AXIS2_PLACEMENT_3D('',#101290,#73077,#73078);
#62800=AXIS2_PLACEMENT_3D('',#101296,#73082,#73083);
#62801=AXIS2_PLACEMENT_3D('',#101302,#73087,#73088);
#62802=AXIS2_PLACEMENT_3D('',#101308,#73092,#73093);
#62803=AXIS2_PLACEMENT_3D('',#101314,#73097,#73098);
#62804=AXIS2_PLACEMENT_3D('',#101320,#73102,#73103);
#62805=AXIS2_PLACEMENT_3D('',#101326,#73107,#73108);
#62806=AXIS2_PLACEMENT_3D('',#101332,#73112,#73113);
#62807=AXIS2_PLACEMENT_3D('',#101338,#73117,#73118);
#62808=AXIS2_PLACEMENT_3D('',#101344,#73122,#73123);
#62809=AXIS2_PLACEMENT_3D('',#101350,#73127,#73128);
#62810=AXIS2_PLACEMENT_3D('',#101356,#73132,#73133);
#62811=AXIS2_PLACEMENT_3D('',#101362,#73137,#73138);
#62812=AXIS2_PLACEMENT_3D('',#101368,#73142,#73143);
#62813=AXIS2_PLACEMENT_3D('',#101374,#73147,#73148);
#62814=AXIS2_PLACEMENT_3D('',#101380,#73152,#73153);
#62815=AXIS2_PLACEMENT_3D('',#101386,#73157,#73158);
#62816=AXIS2_PLACEMENT_3D('',#101392,#73162,#73163);
#62817=AXIS2_PLACEMENT_3D('',#101398,#73167,#73168);
#62818=AXIS2_PLACEMENT_3D('',#101404,#73172,#73173);
#62819=AXIS2_PLACEMENT_3D('',#101410,#73177,#73178);
#62820=AXIS2_PLACEMENT_3D('',#101416,#73182,#73183);
#62821=AXIS2_PLACEMENT_3D('',#101422,#73187,#73188);
#62822=AXIS2_PLACEMENT_3D('',#101428,#73192,#73193);
#62823=AXIS2_PLACEMENT_3D('',#101434,#73197,#73198);
#62824=AXIS2_PLACEMENT_3D('',#101440,#73202,#73203);
#62825=AXIS2_PLACEMENT_3D('',#101446,#73207,#73208);
#62826=AXIS2_PLACEMENT_3D('',#101452,#73212,#73213);
#62827=AXIS2_PLACEMENT_3D('',#101458,#73217,#73218);
#62828=AXIS2_PLACEMENT_3D('',#101464,#73222,#73223);
#62829=AXIS2_PLACEMENT_3D('',#101470,#73227,#73228);
#62830=AXIS2_PLACEMENT_3D('',#101476,#73232,#73233);
#62831=AXIS2_PLACEMENT_3D('',#101482,#73237,#73238);
#62832=AXIS2_PLACEMENT_3D('',#101488,#73242,#73243);
#62833=AXIS2_PLACEMENT_3D('',#101494,#73247,#73248);
#62834=AXIS2_PLACEMENT_3D('',#101500,#73252,#73253);
#62835=AXIS2_PLACEMENT_3D('',#101506,#73257,#73258);
#62836=AXIS2_PLACEMENT_3D('',#101512,#73262,#73263);
#62837=AXIS2_PLACEMENT_3D('',#101518,#73267,#73268);
#62838=AXIS2_PLACEMENT_3D('',#101524,#73272,#73273);
#62839=AXIS2_PLACEMENT_3D('',#101530,#73277,#73278);
#62840=AXIS2_PLACEMENT_3D('',#101536,#73282,#73283);
#62841=AXIS2_PLACEMENT_3D('',#101542,#73287,#73288);
#62842=AXIS2_PLACEMENT_3D('',#101548,#73292,#73293);
#62843=AXIS2_PLACEMENT_3D('',#101554,#73297,#73298);
#62844=AXIS2_PLACEMENT_3D('',#101560,#73302,#73303);
#62845=AXIS2_PLACEMENT_3D('',#101566,#73307,#73308);
#62846=AXIS2_PLACEMENT_3D('',#101572,#73312,#73313);
#62847=AXIS2_PLACEMENT_3D('',#101578,#73317,#73318);
#62848=AXIS2_PLACEMENT_3D('',#101584,#73322,#73323);
#62849=AXIS2_PLACEMENT_3D('',#101590,#73327,#73328);
#62850=AXIS2_PLACEMENT_3D('',#101596,#73332,#73333);
#62851=AXIS2_PLACEMENT_3D('',#101602,#73337,#73338);
#62852=AXIS2_PLACEMENT_3D('',#101608,#73342,#73343);
#62853=AXIS2_PLACEMENT_3D('',#101614,#73347,#73348);
#62854=AXIS2_PLACEMENT_3D('',#101620,#73352,#73353);
#62855=AXIS2_PLACEMENT_3D('',#101626,#73357,#73358);
#62856=AXIS2_PLACEMENT_3D('',#101632,#73362,#73363);
#62857=AXIS2_PLACEMENT_3D('',#101638,#73367,#73368);
#62858=AXIS2_PLACEMENT_3D('',#101644,#73372,#73373);
#62859=AXIS2_PLACEMENT_3D('',#101650,#73377,#73378);
#62860=AXIS2_PLACEMENT_3D('',#101656,#73382,#73383);
#62861=AXIS2_PLACEMENT_3D('',#101662,#73387,#73388);
#62862=AXIS2_PLACEMENT_3D('',#101668,#73392,#73393);
#62863=AXIS2_PLACEMENT_3D('',#101674,#73397,#73398);
#62864=AXIS2_PLACEMENT_3D('',#101680,#73402,#73403);
#62865=AXIS2_PLACEMENT_3D('',#101686,#73407,#73408);
#62866=AXIS2_PLACEMENT_3D('',#101692,#73412,#73413);
#62867=AXIS2_PLACEMENT_3D('',#101698,#73417,#73418);
#62868=AXIS2_PLACEMENT_3D('',#101704,#73422,#73423);
#62869=AXIS2_PLACEMENT_3D('',#101710,#73427,#73428);
#62870=AXIS2_PLACEMENT_3D('',#101716,#73432,#73433);
#62871=AXIS2_PLACEMENT_3D('',#101722,#73437,#73438);
#62872=AXIS2_PLACEMENT_3D('',#101728,#73442,#73443);
#62873=AXIS2_PLACEMENT_3D('',#101734,#73447,#73448);
#62874=AXIS2_PLACEMENT_3D('',#101740,#73452,#73453);
#62875=AXIS2_PLACEMENT_3D('',#101746,#73457,#73458);
#62876=AXIS2_PLACEMENT_3D('',#101752,#73462,#73463);
#62877=AXIS2_PLACEMENT_3D('',#101758,#73467,#73468);
#62878=AXIS2_PLACEMENT_3D('',#101764,#73472,#73473);
#62879=AXIS2_PLACEMENT_3D('',#101770,#73477,#73478);
#62880=AXIS2_PLACEMENT_3D('',#101776,#73482,#73483);
#62881=AXIS2_PLACEMENT_3D('',#101782,#73487,#73488);
#62882=AXIS2_PLACEMENT_3D('',#101788,#73492,#73493);
#62883=AXIS2_PLACEMENT_3D('',#101794,#73497,#73498);
#62884=AXIS2_PLACEMENT_3D('',#101800,#73502,#73503);
#62885=AXIS2_PLACEMENT_3D('',#101806,#73507,#73508);
#62886=AXIS2_PLACEMENT_3D('',#101812,#73512,#73513);
#62887=AXIS2_PLACEMENT_3D('',#101818,#73517,#73518);
#62888=AXIS2_PLACEMENT_3D('',#101824,#73522,#73523);
#62889=AXIS2_PLACEMENT_3D('',#101830,#73527,#73528);
#62890=AXIS2_PLACEMENT_3D('',#101836,#73532,#73533);
#62891=AXIS2_PLACEMENT_3D('',#101842,#73537,#73538);
#62892=AXIS2_PLACEMENT_3D('',#101848,#73542,#73543);
#62893=AXIS2_PLACEMENT_3D('',#101854,#73547,#73548);
#62894=AXIS2_PLACEMENT_3D('',#101860,#73552,#73553);
#62895=AXIS2_PLACEMENT_3D('',#101866,#73557,#73558);
#62896=AXIS2_PLACEMENT_3D('',#101872,#73562,#73563);
#62897=AXIS2_PLACEMENT_3D('',#101878,#73567,#73568);
#62898=AXIS2_PLACEMENT_3D('',#101884,#73572,#73573);
#62899=AXIS2_PLACEMENT_3D('',#101890,#73577,#73578);
#62900=AXIS2_PLACEMENT_3D('',#101896,#73582,#73583);
#62901=AXIS2_PLACEMENT_3D('',#101902,#73587,#73588);
#62902=AXIS2_PLACEMENT_3D('',#101908,#73592,#73593);
#62903=AXIS2_PLACEMENT_3D('',#101914,#73597,#73598);
#62904=AXIS2_PLACEMENT_3D('',#101920,#73602,#73603);
#62905=AXIS2_PLACEMENT_3D('',#101926,#73607,#73608);
#62906=AXIS2_PLACEMENT_3D('',#101932,#73612,#73613);
#62907=AXIS2_PLACEMENT_3D('',#101938,#73617,#73618);
#62908=AXIS2_PLACEMENT_3D('',#101944,#73622,#73623);
#62909=AXIS2_PLACEMENT_3D('',#101950,#73627,#73628);
#62910=AXIS2_PLACEMENT_3D('',#101956,#73632,#73633);
#62911=AXIS2_PLACEMENT_3D('',#101962,#73637,#73638);
#62912=AXIS2_PLACEMENT_3D('',#101968,#73642,#73643);
#62913=AXIS2_PLACEMENT_3D('',#101974,#73647,#73648);
#62914=AXIS2_PLACEMENT_3D('',#101980,#73652,#73653);
#62915=AXIS2_PLACEMENT_3D('',#101986,#73657,#73658);
#62916=AXIS2_PLACEMENT_3D('',#101992,#73662,#73663);
#62917=AXIS2_PLACEMENT_3D('',#101998,#73667,#73668);
#62918=AXIS2_PLACEMENT_3D('',#102004,#73672,#73673);
#62919=AXIS2_PLACEMENT_3D('',#102010,#73677,#73678);
#62920=AXIS2_PLACEMENT_3D('',#102013,#73681,#73682);
#62921=AXIS2_PLACEMENT_3D('',#102016,#73685,#73686);
#62922=AXIS2_PLACEMENT_3D('',#102017,#73687,#73688);
#71111=DIRECTION('axis',(0.,0.,1.));
#71112=DIRECTION('refdir',(1.,0.,0.));
#71113=DIRECTION('center_axis',(0.,1.,0.));
#71114=DIRECTION('ref_axis',(1.,0.,0.));
#71115=DIRECTION('center_axis',(0.,1.,0.));
#71116=DIRECTION('ref_axis',(1.,0.,0.));
#71117=DIRECTION('',(0.707106781186561,-0.707106781186534,-8.65956056235509E-17));
#71118=DIRECTION('center_axis',(0.,-1.,0.));
#71119=DIRECTION('ref_axis',(1.,0.,0.));
#71120=DIRECTION('center_axis',(0.,-1.,0.));
#71121=DIRECTION('ref_axis',(1.,0.,0.));
#71122=DIRECTION('',(0.,-1.,0.));
#71123=DIRECTION('center_axis',(0.,-1.,0.));
#71124=DIRECTION('ref_axis',(1.,0.,0.));
#71125=DIRECTION('center_axis',(0.,1.,0.));
#71126=DIRECTION('ref_axis',(-1.,0.,0.));
#71127=DIRECTION('',(-1.,0.,0.));
#71128=DIRECTION('',(0.,0.,1.));
#71129=DIRECTION('',(-1.,0.,0.));
#71130=DIRECTION('',(0.,0.,1.));
#71131=DIRECTION('center_axis',(0.,1.,0.));
#71132=DIRECTION('ref_axis',(1.,0.,0.));
#71133=DIRECTION('center_axis',(0.,1.,0.));
#71134=DIRECTION('ref_axis',(1.,0.,0.));
#71135=DIRECTION('',(0.707106781186548,-0.707106781186548,-8.65956056235493E-17));
#71136=DIRECTION('center_axis',(0.,-1.,0.));
#71137=DIRECTION('ref_axis',(1.,0.,0.));
#71138=DIRECTION('center_axis',(0.,-1.,0.));
#71139=DIRECTION('ref_axis',(1.,0.,0.));
#71140=DIRECTION('',(0.,-1.,0.));
#71141=DIRECTION('center_axis',(0.,-1.,0.));
#71142=DIRECTION('ref_axis',(1.,0.,0.));
#71143=DIRECTION('center_axis',(0.,1.,0.));
#71144=DIRECTION('ref_axis',(-1.,0.,0.));
#71145=DIRECTION('',(-1.,0.,0.));
#71146=DIRECTION('',(0.,0.,1.));
#71147=DIRECTION('',(-1.,0.,0.));
#71148=DIRECTION('',(0.,0.,1.));
#71149=DIRECTION('center_axis',(0.,1.,0.));
#71150=DIRECTION('ref_axis',(1.,0.,0.));
#71151=DIRECTION('center_axis',(0.,1.,0.));
#71152=DIRECTION('ref_axis',(1.,0.,0.));
#71153=DIRECTION('center_axis',(0.,1.,0.));
#71154=DIRECTION('ref_axis',(1.,0.,0.));
#71155=DIRECTION('center_axis',(0.,1.,0.));
#71156=DIRECTION('ref_axis',(1.,0.,0.));
#71157=DIRECTION('center_axis',(0.,-1.,0.));
#71158=DIRECTION('ref_axis',(1.,0.,0.));
#71159=DIRECTION('',(0.,-1.,0.));
#71160=DIRECTION('center_axis',(0.,1.,0.));
#71161=DIRECTION('ref_axis',(1.,0.,0.));
#71162=DIRECTION('center_axis',(0.,-1.,0.));
#71163=DIRECTION('ref_axis',(1.,0.,0.));
#71164=DIRECTION('',(0.,-1.,0.));
#71165=DIRECTION('center_axis',(0.,1.,0.));
#71166=DIRECTION('ref_axis',(1.,0.,0.));
#71167=DIRECTION('center_axis',(0.,-0.707106781186545,0.70710678118655));
#71168=DIRECTION('ref_axis',(1.,0.,0.));
#71169=DIRECTION('',(0.,0.70710678118655,0.707106781186545));
#71170=DIRECTION('',(-1.,0.,0.));
#71171=DIRECTION('',(0.,-0.70710678118655,-0.707106781186545));
#71172=DIRECTION('',(1.,0.,0.));
#71173=DIRECTION('center_axis',(1.,0.,0.));
#71174=DIRECTION('ref_axis',(0.,1.,0.));
#71175=DIRECTION('',(0.,0.,1.));
#71176=DIRECTION('',(0.,-0.70710678118655,0.707106781186545));
#71177=DIRECTION('',(0.,1.,0.));
#71178=DIRECTION('',(0.,1.,0.));
#71179=DIRECTION('center_axis',(0.,-1.,0.));
#71180=DIRECTION('ref_axis',(1.,0.,0.));
#71181=DIRECTION('',(0.,0.,1.));
#71182=DIRECTION('',(-1.,0.,0.));
#71183=DIRECTION('center_axis',(0.,-0.707106781186545,-0.70710678118655));
#71184=DIRECTION('ref_axis',(-1.,0.,0.));
#71185=DIRECTION('',(0.,0.70710678118655,-0.707106781186545));
#71186=DIRECTION('',(1.,0.,0.));
#71187=DIRECTION('center_axis',(0.939692620785909,0.342020143325668,0.));
#71188=DIRECTION('ref_axis',(-0.342020143325668,0.939692620785909,0.));
#71189=DIRECTION('',(-0.342020143325668,0.939692620785909,0.));
#71190=DIRECTION('',(-0.342020143325668,0.939692620785909,0.));
#71191=DIRECTION('',(0.,0.,1.));
#71192=DIRECTION('center_axis',(0.,1.,0.));
#71193=DIRECTION('ref_axis',(-1.,0.,0.));
#71194=DIRECTION('',(-1.,0.,0.));
#71195=DIRECTION('',(-1.,0.,0.));
#71196=DIRECTION('',(0.,0.,1.));
#71197=DIRECTION('center_axis',(-0.939692620785909,0.342020143325668,0.));
#71198=DIRECTION('ref_axis',(-0.342020143325668,-0.939692620785909,0.));
#71199=DIRECTION('',(-0.342020143325668,-0.939692620785909,0.));
#71200=DIRECTION('',(-0.342020143325668,-0.939692620785909,0.));
#71201=DIRECTION('',(0.,0.,1.));
#71202=DIRECTION('center_axis',(0.,1.,0.));
#71203=DIRECTION('ref_axis',(-1.,0.,0.));
#71204=DIRECTION('',(-1.,0.,0.));
#71205=DIRECTION('',(-1.,0.,0.));
#71206=DIRECTION('',(0.,0.,1.));
#71207=DIRECTION('center_axis',(0.939692620785909,0.342020143325668,0.));
#71208=DIRECTION('ref_axis',(-0.342020143325668,0.939692620785909,0.));
#71209=DIRECTION('',(-0.342020143325668,0.939692620785909,0.));
#71210=DIRECTION('',(-0.342020143325668,0.939692620785909,0.));
#71211=DIRECTION('',(0.,0.,1.));
#71212=DIRECTION('center_axis',(0.,1.,0.));
#71213=DIRECTION('ref_axis',(-1.,0.,0.));
#71214=DIRECTION('',(-1.,0.,0.));
#71215=DIRECTION('',(-1.,0.,0.));
#71216=DIRECTION('',(0.,0.,1.));
#71217=DIRECTION('center_axis',(-0.939692620785909,0.342020143325668,0.));
#71218=DIRECTION('ref_axis',(-0.342020143325668,-0.939692620785909,0.));
#71219=DIRECTION('',(-0.342020143325668,-0.939692620785909,0.));
#71220=DIRECTION('',(-0.342020143325668,-0.939692620785909,0.));
#71221=DIRECTION('',(0.,0.,1.));
#71222=DIRECTION('center_axis',(0.,1.,0.));
#71223=DIRECTION('ref_axis',(-1.,0.,0.));
#71224=DIRECTION('',(-1.,0.,0.));
#71225=DIRECTION('',(-1.,0.,0.));
#71226=DIRECTION('',(0.,0.,1.));
#71227=DIRECTION('center_axis',(0.939692620785909,0.342020143325668,0.));
#71228=DIRECTION('ref_axis',(-0.342020143325668,0.939692620785909,0.));
#71229=DIRECTION('',(-0.342020143325668,0.939692620785909,0.));
#71230=DIRECTION('',(-0.342020143325668,0.939692620785909,0.));
#71231=DIRECTION('',(0.,0.,1.));
#71232=DIRECTION('center_axis',(0.,1.,0.));
#71233=DIRECTION('ref_axis',(-1.,0.,0.));
#71234=DIRECTION('',(-1.,0.,0.));
#71235=DIRECTION('',(-1.,0.,0.));
#71236=DIRECTION('',(0.,0.,1.));
#71237=DIRECTION('center_axis',(-0.939692620785909,0.342020143325668,0.));
#71238=DIRECTION('ref_axis',(-0.342020143325668,-0.939692620785909,0.));
#71239=DIRECTION('',(-0.342020143325668,-0.939692620785909,0.));
#71240=DIRECTION('',(-0.342020143325668,-0.939692620785909,0.));
#71241=DIRECTION('',(0.,0.,1.));
#71242=DIRECTION('center_axis',(0.,1.,0.));
#71243=DIRECTION('ref_axis',(-1.,0.,0.));
#71244=DIRECTION('',(-1.,0.,0.));
#71245=DIRECTION('',(-1.,0.,0.));
#71246=DIRECTION('',(0.,0.,1.));
#71247=DIRECTION('center_axis',(0.939692620785909,0.342020143325668,0.));
#71248=DIRECTION('ref_axis',(-0.342020143325668,0.939692620785909,0.));
#71249=DIRECTION('',(-0.342020143325668,0.939692620785909,0.));
#71250=DIRECTION('',(-0.342020143325668,0.939692620785909,0.));
#71251=DIRECTION('',(0.,0.,1.));
#71252=DIRECTION('center_axis',(0.,1.,0.));
#71253=DIRECTION('ref_axis',(-1.,0.,0.));
#71254=DIRECTION('',(-1.,0.,0.));
#71255=DIRECTION('',(-1.,0.,0.));
#71256=DIRECTION('',(0.,0.,1.));
#71257=DIRECTION('center_axis',(-0.939692620785909,0.342020143325668,0.));
#71258=DIRECTION('ref_axis',(-0.342020143325668,-0.939692620785909,0.));
#71259=DIRECTION('',(-0.342020143325668,-0.939692620785909,0.));
#71260=DIRECTION('',(-0.342020143325668,-0.939692620785909,0.));
#71261=DIRECTION('',(0.,0.,1.));
#71262=DIRECTION('center_axis',(0.,1.,0.));
#71263=DIRECTION('ref_axis',(-1.,0.,0.));
#71264=DIRECTION('',(-1.,0.,0.));
#71265=DIRECTION('',(-1.,0.,0.));
#71266=DIRECTION('',(0.,0.,1.));
#71267=DIRECTION('center_axis',(0.939692620785909,0.342020143325668,0.));
#71268=DIRECTION('ref_axis',(-0.342020143325668,0.939692620785909,0.));
#71269=DIRECTION('',(-0.342020143325668,0.939692620785909,0.));
#71270=DIRECTION('',(-0.342020143325668,0.939692620785909,0.));
#71271=DIRECTION('',(0.,0.,1.));
#71272=DIRECTION('center_axis',(0.,1.,0.));
#71273=DIRECTION('ref_axis',(-1.,0.,0.));
#71274=DIRECTION('',(-1.,0.,0.));
#71275=DIRECTION('',(-1.,0.,0.));
#71276=DIRECTION('',(0.,0.,1.));
#71277=DIRECTION('center_axis',(-0.939692620785909,0.342020143325668,0.));
#71278=DIRECTION('ref_axis',(-0.342020143325668,-0.939692620785909,0.));
#71279=DIRECTION('',(-0.342020143325668,-0.939692620785909,0.));
#71280=DIRECTION('',(-0.342020143325668,-0.939692620785909,0.));
#71281=DIRECTION('',(0.,0.,1.));
#71282=DIRECTION('center_axis',(0.,1.,0.));
#71283=DIRECTION('ref_axis',(-1.,0.,0.));
#71284=DIRECTION('',(-1.,0.,0.));
#71285=DIRECTION('',(-1.,0.,0.));
#71286=DIRECTION('',(0.,0.,1.));
#71287=DIRECTION('center_axis',(0.939692620785909,0.342020143325668,0.));
#71288=DIRECTION('ref_axis',(-0.342020143325668,0.939692620785909,0.));
#71289=DIRECTION('',(-0.342020143325668,0.939692620785909,0.));
#71290=DIRECTION('',(-0.342020143325668,0.939692620785909,0.));
#71291=DIRECTION('',(0.,0.,1.));
#71292=DIRECTION('center_axis',(0.,1.,0.));
#71293=DIRECTION('ref_axis',(-1.,0.,0.));
#71294=DIRECTION('',(-1.,0.,0.));
#71295=DIRECTION('',(-1.,0.,0.));
#71296=DIRECTION('',(0.,0.,1.));
#71297=DIRECTION('center_axis',(-0.939692620785909,0.342020143325668,0.));
#71298=DIRECTION('ref_axis',(-0.342020143325668,-0.939692620785909,0.));
#71299=DIRECTION('',(-0.342020143325668,-0.939692620785909,0.));
#71300=DIRECTION('',(-0.342020143325668,-0.939692620785909,0.));
#71301=DIRECTION('',(0.,0.,1.));
#71302=DIRECTION('center_axis',(0.,1.,0.));
#71303=DIRECTION('ref_axis',(-1.,0.,0.));
#71304=DIRECTION('',(-1.,0.,0.));
#71305=DIRECTION('',(-1.,0.,0.));
#71306=DIRECTION('',(0.,0.,1.));
#71307=DIRECTION('center_axis',(0.939692620785909,0.342020143325668,0.));
#71308=DIRECTION('ref_axis',(-0.342020143325668,0.939692620785909,0.));
#71309=DIRECTION('',(-0.342020143325668,0.939692620785909,0.));
#71310=DIRECTION('',(-0.342020143325668,0.939692620785909,0.));
#71311=DIRECTION('',(0.,0.,1.));
#71312=DIRECTION('center_axis',(0.,1.,0.));
#71313=DIRECTION('ref_axis',(-1.,0.,0.));
#71314=DIRECTION('',(-1.,0.,0.));
#71315=DIRECTION('',(-1.,0.,0.));
#71316=DIRECTION('',(0.,0.,1.));
#71317=DIRECTION('center_axis',(-0.939692620785909,0.342020143325668,0.));
#71318=DIRECTION('ref_axis',(-0.342020143325668,-0.939692620785909,0.));
#71319=DIRECTION('',(-0.342020143325668,-0.939692620785909,0.));
#71320=DIRECTION('',(-0.342020143325668,-0.939692620785909,0.));
#71321=DIRECTION('',(0.,0.,1.));
#71322=DIRECTION('center_axis',(0.,1.,0.));
#71323=DIRECTION('ref_axis',(-1.,0.,0.));
#71324=DIRECTION('',(-1.,0.,0.));
#71325=DIRECTION('',(-1.,0.,0.));
#71326=DIRECTION('',(0.,0.,1.));
#71327=DIRECTION('center_axis',(0.939692620785909,0.342020143325668,0.));
#71328=DIRECTION('ref_axis',(-0.342020143325668,0.939692620785909,0.));
#71329=DIRECTION('',(-0.342020143325668,0.939692620785909,0.));
#71330=DIRECTION('',(-0.342020143325668,0.939692620785909,0.));
#71331=DIRECTION('',(0.,0.,1.));
#71332=DIRECTION('center_axis',(0.,1.,0.));
#71333=DIRECTION('ref_axis',(-1.,0.,0.));
#71334=DIRECTION('',(-1.,0.,0.));
#71335=DIRECTION('',(-1.,0.,0.));
#71336=DIRECTION('',(0.,0.,1.));
#71337=DIRECTION('center_axis',(-0.939692620785909,0.342020143325668,0.));
#71338=DIRECTION('ref_axis',(-0.342020143325668,-0.939692620785909,0.));
#71339=DIRECTION('',(-0.342020143325668,-0.939692620785909,0.));
#71340=DIRECTION('',(-0.342020143325668,-0.939692620785909,0.));
#71341=DIRECTION('',(0.,0.,1.));
#71342=DIRECTION('center_axis',(0.,1.,0.));
#71343=DIRECTION('ref_axis',(-1.,0.,0.));
#71344=DIRECTION('',(-1.,0.,0.));
#71345=DIRECTION('',(-1.,0.,0.));
#71346=DIRECTION('',(0.,0.,1.));
#71347=DIRECTION('center_axis',(0.939692620785909,0.342020143325668,0.));
#71348=DIRECTION('ref_axis',(-0.342020143325668,0.939692620785909,0.));
#71349=DIRECTION('',(-0.342020143325668,0.939692620785909,0.));
#71350=DIRECTION('',(-0.342020143325668,0.939692620785909,0.));
#71351=DIRECTION('',(0.,0.,1.));
#71352=DIRECTION('center_axis',(0.,1.,0.));
#71353=DIRECTION('ref_axis',(-1.,0.,0.));
#71354=DIRECTION('',(-1.,0.,0.));
#71355=DIRECTION('',(-1.,0.,0.));
#71356=DIRECTION('',(0.,0.,1.));
#71357=DIRECTION('center_axis',(-0.939692620785909,0.342020143325668,0.));
#71358=DIRECTION('ref_axis',(-0.342020143325668,-0.939692620785909,0.));
#71359=DIRECTION('',(-0.342020143325668,-0.939692620785909,0.));
#71360=DIRECTION('',(-0.342020143325668,-0.939692620785909,0.));
#71361=DIRECTION('',(0.,0.,1.));
#71362=DIRECTION('center_axis',(0.,1.,0.));
#71363=DIRECTION('ref_axis',(-1.,0.,0.));
#71364=DIRECTION('',(-1.,0.,0.));
#71365=DIRECTION('',(-1.,0.,0.));
#71366=DIRECTION('',(0.,0.,1.));
#71367=DIRECTION('center_axis',(0.939692620785909,0.342020143325668,0.));
#71368=DIRECTION('ref_axis',(-0.342020143325668,0.939692620785909,0.));
#71369=DIRECTION('',(-0.342020143325668,0.939692620785909,0.));
#71370=DIRECTION('',(-0.342020143325668,0.939692620785909,0.));
#71371=DIRECTION('',(0.,0.,1.));
#71372=DIRECTION('center_axis',(0.,1.,0.));
#71373=DIRECTION('ref_axis',(-1.,0.,0.));
#71374=DIRECTION('',(-1.,0.,0.));
#71375=DIRECTION('',(-1.,0.,0.));
#71376=DIRECTION('',(0.,0.,1.));
#71377=DIRECTION('center_axis',(-0.939692620785909,0.342020143325668,0.));
#71378=DIRECTION('ref_axis',(-0.342020143325668,-0.939692620785909,0.));
#71379=DIRECTION('',(-0.342020143325668,-0.939692620785909,0.));
#71380=DIRECTION('',(-0.342020143325668,-0.939692620785909,0.));
#71381=DIRECTION('',(0.,0.,1.));
#71382=DIRECTION('center_axis',(0.,1.,0.));
#71383=DIRECTION('ref_axis',(-1.,0.,0.));
#71384=DIRECTION('',(-1.,0.,0.));
#71385=DIRECTION('',(-1.,0.,0.));
#71386=DIRECTION('',(0.,0.,1.));
#71387=DIRECTION('center_axis',(0.939692620785909,0.342020143325668,0.));
#71388=DIRECTION('ref_axis',(-0.342020143325668,0.939692620785909,0.));
#71389=DIRECTION('',(-0.342020143325668,0.939692620785909,0.));
#71390=DIRECTION('',(-0.342020143325668,0.939692620785909,0.));
#71391=DIRECTION('',(0.,0.,1.));
#71392=DIRECTION('center_axis',(0.,1.,0.));
#71393=DIRECTION('ref_axis',(-1.,0.,0.));
#71394=DIRECTION('',(-1.,0.,0.));
#71395=DIRECTION('',(-1.,0.,0.));
#71396=DIRECTION('',(0.,0.,1.));
#71397=DIRECTION('center_axis',(-0.939692620785909,0.342020143325668,0.));
#71398=DIRECTION('ref_axis',(-0.342020143325668,-0.939692620785909,0.));
#71399=DIRECTION('',(-0.342020143325668,-0.939692620785909,0.));
#71400=DIRECTION('',(-0.342020143325668,-0.939692620785909,0.));
#71401=DIRECTION('',(0.,0.,1.));
#71402=DIRECTION('center_axis',(0.,1.,0.));
#71403=DIRECTION('ref_axis',(-1.,0.,0.));
#71404=DIRECTION('',(-1.,0.,0.));
#71405=DIRECTION('',(-1.,0.,0.));
#71406=DIRECTION('',(0.,0.,1.));
#71407=DIRECTION('center_axis',(0.939692620785909,0.342020143325668,0.));
#71408=DIRECTION('ref_axis',(-0.342020143325668,0.939692620785909,0.));
#71409=DIRECTION('',(-0.342020143325668,0.939692620785909,0.));
#71410=DIRECTION('',(-0.342020143325668,0.939692620785909,0.));
#71411=DIRECTION('',(0.,0.,1.));
#71412=DIRECTION('center_axis',(0.,1.,0.));
#71413=DIRECTION('ref_axis',(-1.,0.,0.));
#71414=DIRECTION('',(-1.,0.,0.));
#71415=DIRECTION('',(-1.,0.,0.));
#71416=DIRECTION('',(0.,0.,1.));
#71417=DIRECTION('center_axis',(-0.939692620785909,0.342020143325668,0.));
#71418=DIRECTION('ref_axis',(-0.342020143325668,-0.939692620785909,0.));
#71419=DIRECTION('',(-0.342020143325668,-0.939692620785909,0.));
#71420=DIRECTION('',(-0.342020143325668,-0.939692620785909,0.));
#71421=DIRECTION('',(0.,0.,1.));
#71422=DIRECTION('center_axis',(0.,1.,0.));
#71423=DIRECTION('ref_axis',(-1.,0.,0.));
#71424=DIRECTION('',(-1.,0.,0.));
#71425=DIRECTION('',(-1.,0.,0.));
#71426=DIRECTION('',(0.,0.,1.));
#71427=DIRECTION('center_axis',(0.939692620785909,0.342020143325668,0.));
#71428=DIRECTION('ref_axis',(-0.342020143325668,0.939692620785909,0.));
#71429=DIRECTION('',(-0.342020143325668,0.939692620785909,0.));
#71430=DIRECTION('',(-0.342020143325668,0.939692620785909,0.));
#71431=DIRECTION('',(0.,0.,1.));
#71432=DIRECTION('center_axis',(0.,1.,0.));
#71433=DIRECTION('ref_axis',(-1.,0.,0.));
#71434=DIRECTION('',(-1.,0.,0.));
#71435=DIRECTION('',(-1.,0.,0.));
#71436=DIRECTION('',(0.,0.,1.));
#71437=DIRECTION('center_axis',(-0.939692620785909,0.342020143325668,0.));
#71438=DIRECTION('ref_axis',(-0.342020143325668,-0.939692620785909,0.));
#71439=DIRECTION('',(-0.342020143325668,-0.939692620785909,0.));
#71440=DIRECTION('',(-0.342020143325668,-0.939692620785909,0.));
#71441=DIRECTION('',(0.,0.,1.));
#71442=DIRECTION('center_axis',(0.,1.,0.));
#71443=DIRECTION('ref_axis',(-1.,0.,0.));
#71444=DIRECTION('',(-1.,0.,0.));
#71445=DIRECTION('',(-1.,0.,0.));
#71446=DIRECTION('',(0.,0.,1.));
#71447=DIRECTION('center_axis',(0.939692620785909,0.342020143325668,0.));
#71448=DIRECTION('ref_axis',(-0.342020143325668,0.939692620785909,0.));
#71449=DIRECTION('',(-0.342020143325668,0.939692620785909,0.));
#71450=DIRECTION('',(-0.342020143325668,0.939692620785909,0.));
#71451=DIRECTION('',(0.,0.,1.));
#71452=DIRECTION('center_axis',(0.,1.,0.));
#71453=DIRECTION('ref_axis',(-1.,0.,0.));
#71454=DIRECTION('',(-1.,0.,0.));
#71455=DIRECTION('',(-1.,0.,0.));
#71456=DIRECTION('',(0.,0.,1.));
#71457=DIRECTION('center_axis',(-0.939692620785909,0.342020143325668,0.));
#71458=DIRECTION('ref_axis',(-0.342020143325668,-0.939692620785909,0.));
#71459=DIRECTION('',(-0.342020143325668,-0.939692620785909,0.));
#71460=DIRECTION('',(-0.342020143325668,-0.939692620785909,0.));
#71461=DIRECTION('',(0.,0.,1.));
#71462=DIRECTION('center_axis',(0.,1.,0.));
#71463=DIRECTION('ref_axis',(-1.,0.,0.));
#71464=DIRECTION('',(-1.,0.,0.));
#71465=DIRECTION('',(-1.,0.,0.));
#71466=DIRECTION('',(0.,0.,1.));
#71467=DIRECTION('center_axis',(0.939692620785909,0.342020143325668,0.));
#71468=DIRECTION('ref_axis',(-0.342020143325668,0.939692620785909,0.));
#71469=DIRECTION('',(-0.342020143325668,0.939692620785909,0.));
#71470=DIRECTION('',(-0.342020143325668,0.939692620785909,0.));
#71471=DIRECTION('',(0.,0.,1.));
#71472=DIRECTION('center_axis',(0.,1.,0.));
#71473=DIRECTION('ref_axis',(-1.,0.,0.));
#71474=DIRECTION('',(-1.,0.,0.));
#71475=DIRECTION('',(-1.,0.,0.));
#71476=DIRECTION('',(0.,0.,1.));
#71477=DIRECTION('center_axis',(-0.939692620785909,0.342020143325668,0.));
#71478=DIRECTION('ref_axis',(-0.342020143325668,-0.939692620785909,0.));
#71479=DIRECTION('',(-0.342020143325668,-0.939692620785909,0.));
#71480=DIRECTION('',(-0.342020143325668,-0.939692620785909,0.));
#71481=DIRECTION('',(0.,0.,1.));
#71482=DIRECTION('center_axis',(0.,1.,0.));
#71483=DIRECTION('ref_axis',(-1.,0.,0.));
#71484=DIRECTION('',(-1.,0.,0.));
#71485=DIRECTION('',(-1.,0.,0.));
#71486=DIRECTION('',(0.,0.,1.));
#71487=DIRECTION('center_axis',(0.939692620785909,0.342020143325668,0.));
#71488=DIRECTION('ref_axis',(-0.342020143325668,0.939692620785909,0.));
#71489=DIRECTION('',(-0.342020143325668,0.939692620785909,0.));
#71490=DIRECTION('',(-0.342020143325668,0.939692620785909,0.));
#71491=DIRECTION('',(0.,0.,1.));
#71492=DIRECTION('center_axis',(0.,1.,0.));
#71493=DIRECTION('ref_axis',(-1.,0.,0.));
#71494=DIRECTION('',(-1.,0.,0.));
#71495=DIRECTION('',(-1.,0.,0.));
#71496=DIRECTION('',(0.,0.,1.));
#71497=DIRECTION('center_axis',(-0.939692620785909,0.342020143325668,0.));
#71498=DIRECTION('ref_axis',(-0.342020143325668,-0.939692620785909,0.));
#71499=DIRECTION('',(-0.342020143325668,-0.939692620785909,0.));
#71500=DIRECTION('',(-0.342020143325668,-0.939692620785909,0.));
#71501=DIRECTION('',(0.,0.,1.));
#71502=DIRECTION('center_axis',(0.,1.,0.));
#71503=DIRECTION('ref_axis',(-1.,0.,0.));
#71504=DIRECTION('',(-1.,0.,0.));
#71505=DIRECTION('',(-1.,0.,0.));
#71506=DIRECTION('',(0.,0.,1.));
#71507=DIRECTION('center_axis',(0.939692620785909,0.342020143325668,0.));
#71508=DIRECTION('ref_axis',(-0.342020143325668,0.939692620785909,0.));
#71509=DIRECTION('',(-0.342020143325668,0.939692620785909,0.));
#71510=DIRECTION('',(-0.342020143325668,0.939692620785909,0.));
#71511=DIRECTION('',(0.,0.,1.));
#71512=DIRECTION('center_axis',(0.,1.,0.));
#71513=DIRECTION('ref_axis',(-1.,0.,0.));
#71514=DIRECTION('',(-1.,0.,0.));
#71515=DIRECTION('',(-1.,0.,0.));
#71516=DIRECTION('',(0.,0.,1.));
#71517=DIRECTION('center_axis',(-0.939692620785909,0.342020143325668,0.));
#71518=DIRECTION('ref_axis',(-0.342020143325668,-0.939692620785909,0.));
#71519=DIRECTION('',(-0.342020143325668,-0.939692620785909,0.));
#71520=DIRECTION('',(-0.342020143325668,-0.939692620785909,0.));
#71521=DIRECTION('',(0.,0.,1.));
#71522=DIRECTION('center_axis',(0.,1.,0.));
#71523=DIRECTION('ref_axis',(-1.,0.,0.));
#71524=DIRECTION('',(-1.,0.,0.));
#71525=DIRECTION('',(-1.,0.,0.));
#71526=DIRECTION('',(0.,0.,1.));
#71527=DIRECTION('center_axis',(0.939692620785909,0.342020143325668,0.));
#71528=DIRECTION('ref_axis',(-0.342020143325668,0.939692620785909,0.));
#71529=DIRECTION('',(-0.342020143325668,0.939692620785909,0.));
#71530=DIRECTION('',(-0.342020143325668,0.939692620785909,0.));
#71531=DIRECTION('',(0.,0.,1.));
#71532=DIRECTION('center_axis',(0.,1.,0.));
#71533=DIRECTION('ref_axis',(-1.,0.,0.));
#71534=DIRECTION('',(-1.,0.,0.));
#71535=DIRECTION('',(-1.,0.,0.));
#71536=DIRECTION('',(0.,0.,1.));
#71537=DIRECTION('center_axis',(-0.939692620785909,0.342020143325668,0.));
#71538=DIRECTION('ref_axis',(-0.342020143325668,-0.939692620785909,0.));
#71539=DIRECTION('',(-0.342020143325668,-0.939692620785909,0.));
#71540=DIRECTION('',(-0.342020143325668,-0.939692620785909,0.));
#71541=DIRECTION('',(0.,0.,1.));
#71542=DIRECTION('center_axis',(0.,1.,0.));
#71543=DIRECTION('ref_axis',(-1.,0.,0.));
#71544=DIRECTION('',(-1.,0.,0.));
#71545=DIRECTION('',(-1.,0.,0.));
#71546=DIRECTION('',(0.,0.,1.));
#71547=DIRECTION('center_axis',(0.939692620785909,0.342020143325668,0.));
#71548=DIRECTION('ref_axis',(-0.342020143325668,0.939692620785909,0.));
#71549=DIRECTION('',(-0.342020143325668,0.939692620785909,0.));
#71550=DIRECTION('',(-0.342020143325668,0.939692620785909,0.));
#71551=DIRECTION('',(0.,0.,1.));
#71552=DIRECTION('center_axis',(0.,1.,0.));
#71553=DIRECTION('ref_axis',(-1.,0.,0.));
#71554=DIRECTION('',(-1.,0.,0.));
#71555=DIRECTION('',(-1.,0.,0.));
#71556=DIRECTION('',(0.,0.,1.));
#71557=DIRECTION('center_axis',(-0.939692620785909,0.342020143325668,0.));
#71558=DIRECTION('ref_axis',(-0.342020143325668,-0.939692620785909,0.));
#71559=DIRECTION('',(-0.342020143325668,-0.939692620785909,0.));
#71560=DIRECTION('',(-0.342020143325668,-0.939692620785909,0.));
#71561=DIRECTION('',(0.,0.,1.));
#71562=DIRECTION('center_axis',(0.,1.,0.));
#71563=DIRECTION('ref_axis',(-1.,0.,0.));
#71564=DIRECTION('',(-1.,0.,0.));
#71565=DIRECTION('',(-1.,0.,0.));
#71566=DIRECTION('',(0.,0.,1.));
#71567=DIRECTION('center_axis',(0.939692620785909,0.342020143325668,0.));
#71568=DIRECTION('ref_axis',(-0.342020143325668,0.939692620785909,0.));
#71569=DIRECTION('',(-0.342020143325668,0.939692620785909,0.));
#71570=DIRECTION('',(-0.342020143325668,0.939692620785909,0.));
#71571=DIRECTION('',(0.,0.,1.));
#71572=DIRECTION('center_axis',(0.,1.,0.));
#71573=DIRECTION('ref_axis',(-1.,0.,0.));
#71574=DIRECTION('',(-1.,0.,0.));
#71575=DIRECTION('',(-1.,0.,0.));
#71576=DIRECTION('',(0.,0.,1.));
#71577=DIRECTION('center_axis',(-0.939692620785909,0.342020143325668,0.));
#71578=DIRECTION('ref_axis',(-0.342020143325668,-0.939692620785909,0.));
#71579=DIRECTION('',(-0.342020143325668,-0.939692620785909,0.));
#71580=DIRECTION('',(-0.342020143325668,-0.939692620785909,0.));
#71581=DIRECTION('',(0.,0.,1.));
#71582=DIRECTION('center_axis',(0.,1.,0.));
#71583=DIRECTION('ref_axis',(-1.,0.,0.));
#71584=DIRECTION('',(-1.,0.,0.));
#71585=DIRECTION('',(-1.,0.,0.));
#71586=DIRECTION('',(0.,0.,1.));
#71587=DIRECTION('center_axis',(0.939692620785909,0.342020143325668,0.));
#71588=DIRECTION('ref_axis',(-0.342020143325668,0.939692620785909,0.));
#71589=DIRECTION('',(-0.342020143325668,0.939692620785909,0.));
#71590=DIRECTION('',(-0.342020143325668,0.939692620785909,0.));
#71591=DIRECTION('',(0.,0.,1.));
#71592=DIRECTION('center_axis',(0.,1.,0.));
#71593=DIRECTION('ref_axis',(-1.,0.,0.));
#71594=DIRECTION('',(-1.,0.,0.));
#71595=DIRECTION('',(-1.,0.,0.));
#71596=DIRECTION('',(0.,0.,1.));
#71597=DIRECTION('center_axis',(-0.939692620785909,0.342020143325668,0.));
#71598=DIRECTION('ref_axis',(-0.342020143325668,-0.939692620785909,0.));
#71599=DIRECTION('',(-0.342020143325668,-0.939692620785909,0.));
#71600=DIRECTION('',(-0.342020143325668,-0.939692620785909,0.));
#71601=DIRECTION('',(0.,0.,1.));
#71602=DIRECTION('center_axis',(0.,1.,0.));
#71603=DIRECTION('ref_axis',(-1.,0.,0.));
#71604=DIRECTION('',(-1.,0.,0.));
#71605=DIRECTION('',(-1.,0.,0.));
#71606=DIRECTION('',(0.,0.,1.));
#71607=DIRECTION('center_axis',(0.939692620785909,0.342020143325668,0.));
#71608=DIRECTION('ref_axis',(-0.342020143325668,0.939692620785909,0.));
#71609=DIRECTION('',(-0.342020143325668,0.939692620785909,0.));
#71610=DIRECTION('',(-0.342020143325668,0.939692620785909,0.));
#71611=DIRECTION('',(0.,0.,1.));
#71612=DIRECTION('center_axis',(0.,1.,0.));
#71613=DIRECTION('ref_axis',(-1.,0.,0.));
#71614=DIRECTION('',(-1.,0.,0.));
#71615=DIRECTION('',(-1.,0.,0.));
#71616=DIRECTION('',(0.,0.,1.));
#71617=DIRECTION('center_axis',(-0.939692620785909,0.342020143325668,0.));
#71618=DIRECTION('ref_axis',(-0.342020143325668,-0.939692620785909,0.));
#71619=DIRECTION('',(-0.342020143325668,-0.939692620785909,0.));
#71620=DIRECTION('',(-0.342020143325668,-0.939692620785909,0.));
#71621=DIRECTION('',(0.,0.,1.));
#71622=DIRECTION('center_axis',(0.,1.,0.));
#71623=DIRECTION('ref_axis',(-1.,0.,0.));
#71624=DIRECTION('',(-1.,0.,0.));
#71625=DIRECTION('',(-1.,0.,0.));
#71626=DIRECTION('',(0.,0.,1.));
#71627=DIRECTION('center_axis',(0.939692620785909,0.342020143325668,0.));
#71628=DIRECTION('ref_axis',(-0.342020143325668,0.939692620785909,0.));
#71629=DIRECTION('',(-0.342020143325668,0.939692620785909,0.));
#71630=DIRECTION('',(-0.342020143325668,0.939692620785909,0.));
#71631=DIRECTION('',(0.,0.,1.));
#71632=DIRECTION('center_axis',(0.,1.,0.));
#71633=DIRECTION('ref_axis',(-1.,0.,0.));
#71634=DIRECTION('',(-1.,0.,0.));
#71635=DIRECTION('',(-1.,0.,0.));
#71636=DIRECTION('',(0.,0.,1.));
#71637=DIRECTION('center_axis',(-0.939692620785909,0.342020143325668,0.));
#71638=DIRECTION('ref_axis',(-0.342020143325668,-0.939692620785909,0.));
#71639=DIRECTION('',(-0.342020143325668,-0.939692620785909,0.));
#71640=DIRECTION('',(-0.342020143325668,-0.939692620785909,0.));
#71641=DIRECTION('',(0.,0.,1.));
#71642=DIRECTION('center_axis',(0.,1.,0.));
#71643=DIRECTION('ref_axis',(-1.,0.,0.));
#71644=DIRECTION('',(-1.,0.,0.));
#71645=DIRECTION('',(-1.,0.,0.));
#71646=DIRECTION('',(0.,0.,1.));
#71647=DIRECTION('center_axis',(0.939692620785909,0.342020143325668,0.));
#71648=DIRECTION('ref_axis',(-0.342020143325668,0.939692620785909,0.));
#71649=DIRECTION('',(-0.342020143325668,0.939692620785909,0.));
#71650=DIRECTION('',(-0.342020143325668,0.939692620785909,0.));
#71651=DIRECTION('',(0.,0.,1.));
#71652=DIRECTION('center_axis',(0.,1.,0.));
#71653=DIRECTION('ref_axis',(-1.,0.,0.));
#71654=DIRECTION('',(-1.,0.,0.));
#71655=DIRECTION('',(-1.,0.,0.));
#71656=DIRECTION('',(0.,0.,1.));
#71657=DIRECTION('center_axis',(-0.939692620785909,0.342020143325668,0.));
#71658=DIRECTION('ref_axis',(-0.342020143325668,-0.939692620785909,0.));
#71659=DIRECTION('',(-0.342020143325668,-0.939692620785909,0.));
#71660=DIRECTION('',(-0.342020143325668,-0.939692620785909,0.));
#71661=DIRECTION('',(0.,0.,1.));
#71662=DIRECTION('center_axis',(0.,1.,0.));
#71663=DIRECTION('ref_axis',(-1.,0.,0.));
#71664=DIRECTION('',(-1.,0.,0.));
#71665=DIRECTION('',(-1.,0.,0.));
#71666=DIRECTION('',(0.,0.,1.));
#71667=DIRECTION('center_axis',(0.939692620785909,0.342020143325668,0.));
#71668=DIRECTION('ref_axis',(-0.342020143325668,0.939692620785909,0.));
#71669=DIRECTION('',(-0.342020143325668,0.939692620785909,0.));
#71670=DIRECTION('',(-0.342020143325668,0.939692620785909,0.));
#71671=DIRECTION('',(0.,0.,1.));
#71672=DIRECTION('center_axis',(0.,1.,0.));
#71673=DIRECTION('ref_axis',(-1.,0.,0.));
#71674=DIRECTION('',(-1.,0.,0.));
#71675=DIRECTION('',(-1.,0.,0.));
#71676=DIRECTION('',(0.,0.,1.));
#71677=DIRECTION('center_axis',(-0.939692620785909,0.342020143325668,0.));
#71678=DIRECTION('ref_axis',(-0.342020143325668,-0.939692620785909,0.));
#71679=DIRECTION('',(-0.342020143325668,-0.939692620785909,0.));
#71680=DIRECTION('',(-0.342020143325668,-0.939692620785909,0.));
#71681=DIRECTION('',(0.,0.,1.));
#71682=DIRECTION('center_axis',(0.,1.,0.));
#71683=DIRECTION('ref_axis',(-1.,0.,0.));
#71684=DIRECTION('',(-1.,0.,0.));
#71685=DIRECTION('',(-1.,0.,0.));
#71686=DIRECTION('',(0.,0.,1.));
#71687=DIRECTION('center_axis',(0.939692620785909,0.342020143325668,0.));
#71688=DIRECTION('ref_axis',(-0.342020143325668,0.939692620785909,0.));
#71689=DIRECTION('',(-0.342020143325668,0.939692620785909,0.));
#71690=DIRECTION('',(-0.342020143325668,0.939692620785909,0.));
#71691=DIRECTION('',(0.,0.,1.));
#71692=DIRECTION('center_axis',(0.,1.,0.));
#71693=DIRECTION('ref_axis',(-1.,0.,0.));
#71694=DIRECTION('',(-1.,0.,0.));
#71695=DIRECTION('',(-1.,0.,0.));
#71696=DIRECTION('',(0.,0.,1.));
#71697=DIRECTION('center_axis',(-0.939692620785909,0.342020143325668,0.));
#71698=DIRECTION('ref_axis',(-0.342020143325668,-0.939692620785909,0.));
#71699=DIRECTION('',(-0.342020143325668,-0.939692620785909,0.));
#71700=DIRECTION('',(-0.342020143325668,-0.939692620785909,0.));
#71701=DIRECTION('',(0.,0.,1.));
#71702=DIRECTION('center_axis',(0.,1.,0.));
#71703=DIRECTION('ref_axis',(-1.,0.,0.));
#71704=DIRECTION('',(-1.,0.,0.));
#71705=DIRECTION('',(-1.,0.,0.));
#71706=DIRECTION('',(0.,0.,1.));
#71707=DIRECTION('center_axis',(0.939692620785909,0.342020143325668,0.));
#71708=DIRECTION('ref_axis',(-0.342020143325668,0.939692620785909,0.));
#71709=DIRECTION('',(-0.342020143325668,0.939692620785909,0.));
#71710=DIRECTION('',(-0.342020143325668,0.939692620785909,0.));
#71711=DIRECTION('',(0.,0.,1.));
#71712=DIRECTION('center_axis',(0.,1.,0.));
#71713=DIRECTION('ref_axis',(-1.,0.,0.));
#71714=DIRECTION('',(-1.,0.,0.));
#71715=DIRECTION('',(-1.,0.,0.));
#71716=DIRECTION('',(0.,0.,1.));
#71717=DIRECTION('center_axis',(-0.939692620785909,0.342020143325668,0.));
#71718=DIRECTION('ref_axis',(-0.342020143325668,-0.939692620785909,0.));
#71719=DIRECTION('',(-0.342020143325668,-0.939692620785909,0.));
#71720=DIRECTION('',(-0.342020143325668,-0.939692620785909,0.));
#71721=DIRECTION('',(0.,0.,1.));
#71722=DIRECTION('center_axis',(0.,1.,0.));
#71723=DIRECTION('ref_axis',(-1.,0.,0.));
#71724=DIRECTION('',(-1.,0.,0.));
#71725=DIRECTION('',(-1.,0.,0.));
#71726=DIRECTION('',(0.,0.,1.));
#71727=DIRECTION('center_axis',(0.939692620785909,0.342020143325668,0.));
#71728=DIRECTION('ref_axis',(-0.342020143325668,0.939692620785909,0.));
#71729=DIRECTION('',(-0.342020143325668,0.939692620785909,0.));
#71730=DIRECTION('',(-0.342020143325668,0.939692620785909,0.));
#71731=DIRECTION('',(0.,0.,1.));
#71732=DIRECTION('center_axis',(0.,1.,0.));
#71733=DIRECTION('ref_axis',(-1.,0.,0.));
#71734=DIRECTION('',(-1.,0.,0.));
#71735=DIRECTION('',(-1.,0.,0.));
#71736=DIRECTION('',(0.,0.,1.));
#71737=DIRECTION('center_axis',(-0.939692620785909,0.342020143325668,0.));
#71738=DIRECTION('ref_axis',(-0.342020143325668,-0.939692620785909,0.));
#71739=DIRECTION('',(-0.342020143325668,-0.939692620785909,0.));
#71740=DIRECTION('',(-0.342020143325668,-0.939692620785909,0.));
#71741=DIRECTION('',(0.,0.,1.));
#71742=DIRECTION('center_axis',(0.,1.,0.));
#71743=DIRECTION('ref_axis',(-1.,0.,0.));
#71744=DIRECTION('',(-1.,0.,0.));
#71745=DIRECTION('',(-1.,0.,0.));
#71746=DIRECTION('',(0.,0.,1.));
#71747=DIRECTION('center_axis',(0.939692620785909,0.342020143325668,0.));
#71748=DIRECTION('ref_axis',(-0.342020143325668,0.939692620785909,0.));
#71749=DIRECTION('',(-0.342020143325668,0.939692620785909,0.));
#71750=DIRECTION('',(-0.342020143325668,0.939692620785909,0.));
#71751=DIRECTION('',(0.,0.,1.));
#71752=DIRECTION('center_axis',(0.,1.,0.));
#71753=DIRECTION('ref_axis',(-1.,0.,0.));
#71754=DIRECTION('',(-1.,0.,0.));
#71755=DIRECTION('',(-1.,0.,0.));
#71756=DIRECTION('',(0.,0.,1.));
#71757=DIRECTION('center_axis',(-0.939692620785909,0.342020143325668,0.));
#71758=DIRECTION('ref_axis',(-0.342020143325668,-0.939692620785909,0.));
#71759=DIRECTION('',(-0.342020143325668,-0.939692620785909,0.));
#71760=DIRECTION('',(-0.342020143325668,-0.939692620785909,0.));
#71761=DIRECTION('',(0.,0.,1.));
#71762=DIRECTION('center_axis',(0.,1.,0.));
#71763=DIRECTION('ref_axis',(-1.,0.,0.));
#71764=DIRECTION('',(-1.,0.,0.));
#71765=DIRECTION('',(-1.,0.,0.));
#71766=DIRECTION('',(0.,0.,1.));
#71767=DIRECTION('center_axis',(0.939692620785909,0.342020143325668,0.));
#71768=DIRECTION('ref_axis',(-0.342020143325668,0.939692620785909,0.));
#71769=DIRECTION('',(-0.342020143325668,0.939692620785909,0.));
#71770=DIRECTION('',(-0.342020143325668,0.939692620785909,0.));
#71771=DIRECTION('',(0.,0.,1.));
#71772=DIRECTION('center_axis',(0.,1.,0.));
#71773=DIRECTION('ref_axis',(-1.,0.,0.));
#71774=DIRECTION('',(-1.,0.,0.));
#71775=DIRECTION('',(-1.,0.,0.));
#71776=DIRECTION('',(0.,0.,1.));
#71777=DIRECTION('center_axis',(-0.939692620785909,0.342020143325668,0.));
#71778=DIRECTION('ref_axis',(-0.342020143325668,-0.939692620785909,0.));
#71779=DIRECTION('',(-0.342020143325668,-0.939692620785909,0.));
#71780=DIRECTION('',(-0.342020143325668,-0.939692620785909,0.));
#71781=DIRECTION('',(0.,0.,1.));
#71782=DIRECTION('center_axis',(0.,1.,0.));
#71783=DIRECTION('ref_axis',(-1.,0.,0.));
#71784=DIRECTION('',(-1.,0.,0.));
#71785=DIRECTION('',(-1.,0.,0.));
#71786=DIRECTION('',(0.,0.,1.));
#71787=DIRECTION('center_axis',(0.939692620785909,0.342020143325668,0.));
#71788=DIRECTION('ref_axis',(-0.342020143325668,0.939692620785909,0.));
#71789=DIRECTION('',(-0.342020143325668,0.939692620785909,0.));
#71790=DIRECTION('',(-0.342020143325668,0.939692620785909,0.));
#71791=DIRECTION('',(0.,0.,1.));
#71792=DIRECTION('center_axis',(0.,1.,0.));
#71793=DIRECTION('ref_axis',(-1.,0.,0.));
#71794=DIRECTION('',(-1.,0.,0.));
#71795=DIRECTION('',(-1.,0.,0.));
#71796=DIRECTION('',(0.,0.,1.));
#71797=DIRECTION('center_axis',(-0.939692620785909,0.342020143325668,0.));
#71798=DIRECTION('ref_axis',(-0.342020143325668,-0.939692620785909,0.));
#71799=DIRECTION('',(-0.342020143325668,-0.939692620785909,0.));
#71800=DIRECTION('',(-0.342020143325668,-0.939692620785909,0.));
#71801=DIRECTION('',(0.,0.,1.));
#71802=DIRECTION('center_axis',(0.,1.,0.));
#71803=DIRECTION('ref_axis',(-1.,0.,0.));
#71804=DIRECTION('',(-1.,0.,0.));
#71805=DIRECTION('',(-1.,0.,0.));
#71806=DIRECTION('',(0.,0.,1.));
#71807=DIRECTION('center_axis',(0.939692620785909,0.342020143325668,0.));
#71808=DIRECTION('ref_axis',(-0.342020143325668,0.939692620785909,0.));
#71809=DIRECTION('',(-0.342020143325668,0.939692620785909,0.));
#71810=DIRECTION('',(-0.342020143325668,0.939692620785909,0.));
#71811=DIRECTION('',(0.,0.,1.));
#71812=DIRECTION('center_axis',(0.,1.,0.));
#71813=DIRECTION('ref_axis',(-1.,0.,0.));
#71814=DIRECTION('',(-1.,0.,0.));
#71815=DIRECTION('',(-1.,0.,0.));
#71816=DIRECTION('',(0.,0.,1.));
#71817=DIRECTION('center_axis',(-0.939692620785909,0.342020143325668,0.));
#71818=DIRECTION('ref_axis',(-0.342020143325668,-0.939692620785909,0.));
#71819=DIRECTION('',(-0.342020143325668,-0.939692620785909,0.));
#71820=DIRECTION('',(-0.342020143325668,-0.939692620785909,0.));
#71821=DIRECTION('',(0.,0.,1.));
#71822=DIRECTION('center_axis',(0.,1.,0.));
#71823=DIRECTION('ref_axis',(-1.,0.,0.));
#71824=DIRECTION('',(-1.,0.,0.));
#71825=DIRECTION('',(-1.,0.,0.));
#71826=DIRECTION('',(0.,0.,1.));
#71827=DIRECTION('center_axis',(0.939692620785909,0.342020143325668,0.));
#71828=DIRECTION('ref_axis',(-0.342020143325668,0.939692620785909,0.));
#71829=DIRECTION('',(-0.342020143325668,0.939692620785909,0.));
#71830=DIRECTION('',(-0.342020143325668,0.939692620785909,0.));
#71831=DIRECTION('',(0.,0.,1.));
#71832=DIRECTION('center_axis',(0.,1.,0.));
#71833=DIRECTION('ref_axis',(-1.,0.,0.));
#71834=DIRECTION('',(-1.,0.,0.));
#71835=DIRECTION('',(-1.,0.,0.));
#71836=DIRECTION('',(0.,0.,1.));
#71837=DIRECTION('center_axis',(-0.939692620785909,0.342020143325668,0.));
#71838=DIRECTION('ref_axis',(-0.342020143325668,-0.939692620785909,0.));
#71839=DIRECTION('',(-0.342020143325668,-0.939692620785909,0.));
#71840=DIRECTION('',(-0.342020143325668,-0.939692620785909,0.));
#71841=DIRECTION('',(0.,0.,1.));
#71842=DIRECTION('center_axis',(0.,1.,0.));
#71843=DIRECTION('ref_axis',(-1.,0.,0.));
#71844=DIRECTION('',(-1.,0.,0.));
#71845=DIRECTION('',(-1.,0.,0.));
#71846=DIRECTION('',(0.,0.,1.));
#71847=DIRECTION('center_axis',(0.939692620785909,0.342020143325668,0.));
#71848=DIRECTION('ref_axis',(-0.342020143325668,0.939692620785909,0.));
#71849=DIRECTION('',(-0.342020143325668,0.939692620785909,0.));
#71850=DIRECTION('',(-0.342020143325668,0.939692620785909,0.));
#71851=DIRECTION('',(0.,0.,1.));
#71852=DIRECTION('center_axis',(0.,1.,0.));
#71853=DIRECTION('ref_axis',(-1.,0.,0.));
#71854=DIRECTION('',(-1.,0.,0.));
#71855=DIRECTION('',(-1.,0.,0.));
#71856=DIRECTION('',(0.,0.,1.));
#71857=DIRECTION('center_axis',(-0.939692620785909,0.342020143325668,0.));
#71858=DIRECTION('ref_axis',(-0.342020143325668,-0.939692620785909,0.));
#71859=DIRECTION('',(-0.342020143325668,-0.939692620785909,0.));
#71860=DIRECTION('',(-0.342020143325668,-0.939692620785909,0.));
#71861=DIRECTION('',(0.,0.,1.));
#71862=DIRECTION('center_axis',(0.,1.,0.));
#71863=DIRECTION('ref_axis',(-1.,0.,0.));
#71864=DIRECTION('',(-1.,0.,0.));
#71865=DIRECTION('',(-1.,0.,0.));
#71866=DIRECTION('',(0.,0.,1.));
#71867=DIRECTION('center_axis',(0.939692620785909,0.342020143325668,0.));
#71868=DIRECTION('ref_axis',(-0.342020143325668,0.939692620785909,0.));
#71869=DIRECTION('',(-0.342020143325668,0.939692620785909,0.));
#71870=DIRECTION('',(-0.342020143325668,0.939692620785909,0.));
#71871=DIRECTION('',(0.,0.,1.));
#71872=DIRECTION('center_axis',(0.,1.,0.));
#71873=DIRECTION('ref_axis',(-1.,0.,0.));
#71874=DIRECTION('',(-1.,0.,0.));
#71875=DIRECTION('',(-1.,0.,0.));
#71876=DIRECTION('',(0.,0.,1.));
#71877=DIRECTION('center_axis',(-0.939692620785909,0.342020143325668,0.));
#71878=DIRECTION('ref_axis',(-0.342020143325668,-0.939692620785909,0.));
#71879=DIRECTION('',(-0.342020143325668,-0.939692620785909,0.));
#71880=DIRECTION('',(-0.342020143325668,-0.939692620785909,0.));
#71881=DIRECTION('',(0.,0.,1.));
#71882=DIRECTION('center_axis',(0.,1.,0.));
#71883=DIRECTION('ref_axis',(-1.,0.,0.));
#71884=DIRECTION('',(-1.,0.,0.));
#71885=DIRECTION('',(-1.,0.,0.));
#71886=DIRECTION('',(0.,0.,1.));
#71887=DIRECTION('center_axis',(0.939692620785909,0.342020143325668,0.));
#71888=DIRECTION('ref_axis',(-0.342020143325668,0.939692620785909,0.));
#71889=DIRECTION('',(-0.342020143325668,0.939692620785909,0.));
#71890=DIRECTION('',(-0.342020143325668,0.939692620785909,0.));
#71891=DIRECTION('',(0.,0.,1.));
#71892=DIRECTION('center_axis',(0.,1.,0.));
#71893=DIRECTION('ref_axis',(-1.,0.,0.));
#71894=DIRECTION('',(-1.,0.,0.));
#71895=DIRECTION('',(-1.,0.,0.));
#71896=DIRECTION('',(0.,0.,1.));
#71897=DIRECTION('center_axis',(-0.939692620785909,0.342020143325668,0.));
#71898=DIRECTION('ref_axis',(-0.342020143325668,-0.939692620785909,0.));
#71899=DIRECTION('',(-0.342020143325668,-0.939692620785909,0.));
#71900=DIRECTION('',(-0.342020143325668,-0.939692620785909,0.));
#71901=DIRECTION('',(0.,0.,1.));
#71902=DIRECTION('center_axis',(0.,1.,0.));
#71903=DIRECTION('ref_axis',(-1.,0.,0.));
#71904=DIRECTION('',(-1.,0.,0.));
#71905=DIRECTION('',(-1.,0.,0.));
#71906=DIRECTION('',(0.,0.,1.));
#71907=DIRECTION('center_axis',(0.939692620785909,0.342020143325668,0.));
#71908=DIRECTION('ref_axis',(-0.342020143325668,0.939692620785909,0.));
#71909=DIRECTION('',(-0.342020143325668,0.939692620785909,0.));
#71910=DIRECTION('',(-0.342020143325668,0.939692620785909,0.));
#71911=DIRECTION('',(0.,0.,1.));
#71912=DIRECTION('center_axis',(0.,1.,0.));
#71913=DIRECTION('ref_axis',(-1.,0.,0.));
#71914=DIRECTION('',(-1.,0.,0.));
#71915=DIRECTION('',(-1.,0.,0.));
#71916=DIRECTION('',(0.,0.,1.));
#71917=DIRECTION('center_axis',(-0.939692620785909,0.342020143325668,0.));
#71918=DIRECTION('ref_axis',(-0.342020143325668,-0.939692620785909,0.));
#71919=DIRECTION('',(-0.342020143325668,-0.939692620785909,0.));
#71920=DIRECTION('',(-0.342020143325668,-0.939692620785909,0.));
#71921=DIRECTION('',(0.,0.,1.));
#71922=DIRECTION('center_axis',(0.,1.,0.));
#71923=DIRECTION('ref_axis',(-1.,0.,0.));
#71924=DIRECTION('',(-1.,0.,0.));
#71925=DIRECTION('',(-1.,0.,0.));
#71926=DIRECTION('',(0.,0.,1.));
#71927=DIRECTION('center_axis',(0.939692620785909,0.342020143325668,0.));
#71928=DIRECTION('ref_axis',(-0.342020143325668,0.939692620785909,0.));
#71929=DIRECTION('',(-0.342020143325668,0.939692620785909,0.));
#71930=DIRECTION('',(-0.342020143325668,0.939692620785909,0.));
#71931=DIRECTION('',(0.,0.,1.));
#71932=DIRECTION('center_axis',(0.,1.,0.));
#71933=DIRECTION('ref_axis',(-1.,0.,0.));
#71934=DIRECTION('',(-1.,0.,0.));
#71935=DIRECTION('',(-1.,0.,0.));
#71936=DIRECTION('',(0.,0.,1.));
#71937=DIRECTION('center_axis',(-0.939692620785909,0.342020143325668,0.));
#71938=DIRECTION('ref_axis',(-0.342020143325668,-0.939692620785909,0.));
#71939=DIRECTION('',(-0.342020143325668,-0.939692620785909,0.));
#71940=DIRECTION('',(-0.342020143325668,-0.939692620785909,0.));
#71941=DIRECTION('',(0.,0.,1.));
#71942=DIRECTION('center_axis',(0.,1.,0.));
#71943=DIRECTION('ref_axis',(-1.,0.,0.));
#71944=DIRECTION('',(-1.,0.,0.));
#71945=DIRECTION('',(-1.,0.,0.));
#71946=DIRECTION('',(0.,0.,1.));
#71947=DIRECTION('center_axis',(0.939692620785909,0.342020143325668,0.));
#71948=DIRECTION('ref_axis',(-0.342020143325668,0.939692620785909,0.));
#71949=DIRECTION('',(-0.342020143325668,0.939692620785909,0.));
#71950=DIRECTION('',(-0.342020143325668,0.939692620785909,0.));
#71951=DIRECTION('',(0.,0.,1.));
#71952=DIRECTION('center_axis',(0.,1.,0.));
#71953=DIRECTION('ref_axis',(-1.,0.,0.));
#71954=DIRECTION('',(-1.,0.,0.));
#71955=DIRECTION('',(-1.,0.,0.));
#71956=DIRECTION('',(0.,0.,1.));
#71957=DIRECTION('center_axis',(-0.939692620785909,0.342020143325668,0.));
#71958=DIRECTION('ref_axis',(-0.342020143325668,-0.939692620785909,0.));
#71959=DIRECTION('',(-0.342020143325668,-0.939692620785909,0.));
#71960=DIRECTION('',(-0.342020143325668,-0.939692620785909,0.));
#71961=DIRECTION('',(0.,0.,1.));
#71962=DIRECTION('center_axis',(0.,1.,0.));
#71963=DIRECTION('ref_axis',(-1.,0.,0.));
#71964=DIRECTION('',(-1.,0.,0.));
#71965=DIRECTION('',(-1.,0.,0.));
#71966=DIRECTION('',(0.,0.,1.));
#71967=DIRECTION('center_axis',(0.939692620785909,0.342020143325668,0.));
#71968=DIRECTION('ref_axis',(-0.342020143325668,0.939692620785909,0.));
#71969=DIRECTION('',(-0.342020143325668,0.939692620785909,0.));
#71970=DIRECTION('',(-0.342020143325668,0.939692620785909,0.));
#71971=DIRECTION('',(0.,0.,1.));
#71972=DIRECTION('center_axis',(0.,1.,0.));
#71973=DIRECTION('ref_axis',(-1.,0.,0.));
#71974=DIRECTION('',(-1.,0.,0.));
#71975=DIRECTION('',(-1.,0.,0.));
#71976=DIRECTION('',(0.,0.,1.));
#71977=DIRECTION('center_axis',(-0.939692620785909,0.342020143325668,0.));
#71978=DIRECTION('ref_axis',(-0.342020143325668,-0.939692620785909,0.));
#71979=DIRECTION('',(-0.342020143325668,-0.939692620785909,0.));
#71980=DIRECTION('',(-0.342020143325668,-0.939692620785909,0.));
#71981=DIRECTION('',(0.,0.,1.));
#71982=DIRECTION('center_axis',(0.,1.,0.));
#71983=DIRECTION('ref_axis',(-1.,0.,0.));
#71984=DIRECTION('',(-1.,0.,0.));
#71985=DIRECTION('',(-1.,0.,0.));
#71986=DIRECTION('',(0.,0.,1.));
#71987=DIRECTION('center_axis',(0.939692620785909,0.342020143325668,0.));
#71988=DIRECTION('ref_axis',(-0.342020143325668,0.939692620785909,0.));
#71989=DIRECTION('',(-0.342020143325668,0.939692620785909,0.));
#71990=DIRECTION('',(-0.342020143325668,0.939692620785909,0.));
#71991=DIRECTION('',(0.,0.,1.));
#71992=DIRECTION('center_axis',(0.,1.,0.));
#71993=DIRECTION('ref_axis',(-1.,0.,0.));
#71994=DIRECTION('',(-1.,0.,0.));
#71995=DIRECTION('',(-1.,0.,0.));
#71996=DIRECTION('',(0.,0.,1.));
#71997=DIRECTION('center_axis',(-0.939692620785909,0.342020143325668,0.));
#71998=DIRECTION('ref_axis',(-0.342020143325668,-0.939692620785909,0.));
#71999=DIRECTION('',(-0.342020143325668,-0.939692620785909,0.));
#72000=DIRECTION('',(-0.342020143325668,-0.939692620785909,0.));
#72001=DIRECTION('',(0.,0.,1.));
#72002=DIRECTION('center_axis',(0.,1.,0.));
#72003=DIRECTION('ref_axis',(-1.,0.,0.));
#72004=DIRECTION('',(-1.,0.,0.));
#72005=DIRECTION('',(-1.,0.,0.));
#72006=DIRECTION('',(0.,0.,1.));
#72007=DIRECTION('center_axis',(0.939692620785909,0.342020143325668,0.));
#72008=DIRECTION('ref_axis',(-0.342020143325668,0.939692620785909,0.));
#72009=DIRECTION('',(-0.342020143325668,0.939692620785909,0.));
#72010=DIRECTION('',(-0.342020143325668,0.939692620785909,0.));
#72011=DIRECTION('',(0.,0.,1.));
#72012=DIRECTION('center_axis',(0.,1.,0.));
#72013=DIRECTION('ref_axis',(-1.,0.,0.));
#72014=DIRECTION('',(-1.,0.,0.));
#72015=DIRECTION('',(-1.,0.,0.));
#72016=DIRECTION('',(0.,0.,1.));
#72017=DIRECTION('center_axis',(-0.939692620785909,0.342020143325668,0.));
#72018=DIRECTION('ref_axis',(-0.342020143325668,-0.939692620785909,0.));
#72019=DIRECTION('',(-0.342020143325668,-0.939692620785909,0.));
#72020=DIRECTION('',(-0.342020143325668,-0.939692620785909,0.));
#72021=DIRECTION('',(0.,0.,1.));
#72022=DIRECTION('center_axis',(0.,1.,0.));
#72023=DIRECTION('ref_axis',(-1.,0.,0.));
#72024=DIRECTION('',(-1.,0.,0.));
#72025=DIRECTION('',(-1.,0.,0.));
#72026=DIRECTION('',(0.,0.,1.));
#72027=DIRECTION('center_axis',(0.939692620785909,0.342020143325668,0.));
#72028=DIRECTION('ref_axis',(-0.342020143325668,0.939692620785909,0.));
#72029=DIRECTION('',(-0.342020143325668,0.939692620785909,0.));
#72030=DIRECTION('',(-0.342020143325668,0.939692620785909,0.));
#72031=DIRECTION('',(0.,0.,1.));
#72032=DIRECTION('center_axis',(0.,1.,0.));
#72033=DIRECTION('ref_axis',(-1.,0.,0.));
#72034=DIRECTION('',(-1.,0.,0.));
#72035=DIRECTION('',(-1.,0.,0.));
#72036=DIRECTION('',(0.,0.,1.));
#72037=DIRECTION('center_axis',(-0.939692620785909,0.342020143325668,0.));
#72038=DIRECTION('ref_axis',(-0.342020143325668,-0.939692620785909,0.));
#72039=DIRECTION('',(-0.342020143325668,-0.939692620785909,0.));
#72040=DIRECTION('',(-0.342020143325668,-0.939692620785909,0.));
#72041=DIRECTION('',(0.,0.,1.));
#72042=DIRECTION('center_axis',(0.,1.,0.));
#72043=DIRECTION('ref_axis',(-1.,0.,0.));
#72044=DIRECTION('',(-1.,0.,0.));
#72045=DIRECTION('',(-1.,0.,0.));
#72046=DIRECTION('',(0.,0.,1.));
#72047=DIRECTION('center_axis',(0.939692620785909,0.342020143325668,0.));
#72048=DIRECTION('ref_axis',(-0.342020143325668,0.939692620785909,0.));
#72049=DIRECTION('',(-0.342020143325668,0.939692620785909,0.));
#72050=DIRECTION('',(-0.342020143325668,0.939692620785909,0.));
#72051=DIRECTION('',(0.,0.,1.));
#72052=DIRECTION('center_axis',(0.,1.,0.));
#72053=DIRECTION('ref_axis',(-1.,0.,0.));
#72054=DIRECTION('',(-1.,0.,0.));
#72055=DIRECTION('',(-1.,0.,0.));
#72056=DIRECTION('',(0.,0.,1.));
#72057=DIRECTION('center_axis',(-0.939692620785909,0.342020143325668,0.));
#72058=DIRECTION('ref_axis',(-0.342020143325668,-0.939692620785909,0.));
#72059=DIRECTION('',(-0.342020143325668,-0.939692620785909,0.));
#72060=DIRECTION('',(-0.342020143325668,-0.939692620785909,0.));
#72061=DIRECTION('',(0.,0.,1.));
#72062=DIRECTION('center_axis',(0.,1.,0.));
#72063=DIRECTION('ref_axis',(-1.,0.,0.));
#72064=DIRECTION('',(-1.,0.,0.));
#72065=DIRECTION('',(-1.,0.,0.));
#72066=DIRECTION('',(0.,0.,1.));
#72067=DIRECTION('center_axis',(0.939692620785909,0.342020143325668,0.));
#72068=DIRECTION('ref_axis',(-0.342020143325668,0.939692620785909,0.));
#72069=DIRECTION('',(-0.342020143325668,0.939692620785909,0.));
#72070=DIRECTION('',(-0.342020143325668,0.939692620785909,0.));
#72071=DIRECTION('',(0.,0.,1.));
#72072=DIRECTION('center_axis',(0.,1.,0.));
#72073=DIRECTION('ref_axis',(-1.,0.,0.));
#72074=DIRECTION('',(-1.,0.,0.));
#72075=DIRECTION('',(-1.,0.,0.));
#72076=DIRECTION('',(0.,0.,1.));
#72077=DIRECTION('center_axis',(-0.939692620785909,0.342020143325668,0.));
#72078=DIRECTION('ref_axis',(-0.342020143325668,-0.939692620785909,0.));
#72079=DIRECTION('',(-0.342020143325668,-0.939692620785909,0.));
#72080=DIRECTION('',(-0.342020143325668,-0.939692620785909,0.));
#72081=DIRECTION('',(0.,0.,1.));
#72082=DIRECTION('center_axis',(0.,1.,0.));
#72083=DIRECTION('ref_axis',(-1.,0.,0.));
#72084=DIRECTION('',(-1.,0.,0.));
#72085=DIRECTION('',(-1.,0.,0.));
#72086=DIRECTION('',(0.,0.,1.));
#72087=DIRECTION('center_axis',(0.939692620785909,0.342020143325668,0.));
#72088=DIRECTION('ref_axis',(-0.342020143325668,0.939692620785909,0.));
#72089=DIRECTION('',(-0.342020143325668,0.939692620785909,0.));
#72090=DIRECTION('',(-0.342020143325668,0.939692620785909,0.));
#72091=DIRECTION('',(0.,0.,1.));
#72092=DIRECTION('center_axis',(0.,1.,0.));
#72093=DIRECTION('ref_axis',(-1.,0.,0.));
#72094=DIRECTION('',(-1.,0.,0.));
#72095=DIRECTION('',(-1.,0.,0.));
#72096=DIRECTION('',(0.,0.,1.));
#72097=DIRECTION('center_axis',(-0.939692620785909,0.342020143325668,0.));
#72098=DIRECTION('ref_axis',(-0.342020143325668,-0.939692620785909,0.));
#72099=DIRECTION('',(-0.342020143325668,-0.939692620785909,0.));
#72100=DIRECTION('',(-0.342020143325668,-0.939692620785909,0.));
#72101=DIRECTION('',(0.,0.,1.));
#72102=DIRECTION('center_axis',(0.,1.,0.));
#72103=DIRECTION('ref_axis',(-1.,0.,0.));
#72104=DIRECTION('',(-1.,0.,0.));
#72105=DIRECTION('',(-1.,0.,0.));
#72106=DIRECTION('',(0.,0.,1.));
#72107=DIRECTION('center_axis',(0.939692620785909,0.342020143325668,0.));
#72108=DIRECTION('ref_axis',(-0.342020143325668,0.939692620785909,0.));
#72109=DIRECTION('',(-0.342020143325668,0.939692620785909,0.));
#72110=DIRECTION('',(-0.342020143325668,0.939692620785909,0.));
#72111=DIRECTION('',(0.,0.,1.));
#72112=DIRECTION('center_axis',(0.,1.,0.));
#72113=DIRECTION('ref_axis',(-1.,0.,0.));
#72114=DIRECTION('',(-1.,0.,0.));
#72115=DIRECTION('',(-1.,0.,0.));
#72116=DIRECTION('',(0.,0.,1.));
#72117=DIRECTION('center_axis',(-0.939692620785909,0.342020143325668,0.));
#72118=DIRECTION('ref_axis',(-0.342020143325668,-0.939692620785909,0.));
#72119=DIRECTION('',(-0.342020143325668,-0.939692620785909,0.));
#72120=DIRECTION('',(-0.342020143325668,-0.939692620785909,0.));
#72121=DIRECTION('',(0.,0.,1.));
#72122=DIRECTION('center_axis',(0.,1.,0.));
#72123=DIRECTION('ref_axis',(-1.,0.,0.));
#72124=DIRECTION('',(-1.,0.,0.));
#72125=DIRECTION('',(-1.,0.,0.));
#72126=DIRECTION('',(0.,0.,1.));
#72127=DIRECTION('center_axis',(0.939692620785909,0.342020143325668,0.));
#72128=DIRECTION('ref_axis',(-0.342020143325668,0.939692620785909,0.));
#72129=DIRECTION('',(-0.342020143325668,0.939692620785909,0.));
#72130=DIRECTION('',(-0.342020143325668,0.939692620785909,0.));
#72131=DIRECTION('',(0.,0.,1.));
#72132=DIRECTION('center_axis',(0.,1.,0.));
#72133=DIRECTION('ref_axis',(-1.,0.,0.));
#72134=DIRECTION('',(-1.,0.,0.));
#72135=DIRECTION('',(-1.,0.,0.));
#72136=DIRECTION('',(0.,0.,1.));
#72137=DIRECTION('center_axis',(-0.939692620785909,0.342020143325668,0.));
#72138=DIRECTION('ref_axis',(-0.342020143325668,-0.939692620785909,0.));
#72139=DIRECTION('',(-0.342020143325668,-0.939692620785909,0.));
#72140=DIRECTION('',(-0.342020143325668,-0.939692620785909,0.));
#72141=DIRECTION('',(0.,0.,1.));
#72142=DIRECTION('center_axis',(0.,1.,0.));
#72143=DIRECTION('ref_axis',(-1.,0.,0.));
#72144=DIRECTION('',(-1.,0.,0.));
#72145=DIRECTION('',(-1.,0.,0.));
#72146=DIRECTION('',(0.,0.,1.));
#72147=DIRECTION('center_axis',(0.939692620785909,0.342020143325668,0.));
#72148=DIRECTION('ref_axis',(-0.342020143325668,0.939692620785909,0.));
#72149=DIRECTION('',(-0.342020143325668,0.939692620785909,0.));
#72150=DIRECTION('',(-0.342020143325668,0.939692620785909,0.));
#72151=DIRECTION('',(0.,0.,1.));
#72152=DIRECTION('center_axis',(0.,1.,0.));
#72153=DIRECTION('ref_axis',(-1.,0.,0.));
#72154=DIRECTION('',(-1.,0.,0.));
#72155=DIRECTION('',(-1.,0.,0.));
#72156=DIRECTION('',(0.,0.,1.));
#72157=DIRECTION('center_axis',(-0.939692620785909,0.342020143325668,0.));
#72158=DIRECTION('ref_axis',(-0.342020143325668,-0.939692620785909,0.));
#72159=DIRECTION('',(-0.342020143325668,-0.939692620785909,0.));
#72160=DIRECTION('',(-0.342020143325668,-0.939692620785909,0.));
#72161=DIRECTION('',(0.,0.,1.));
#72162=DIRECTION('center_axis',(0.,1.,0.));
#72163=DIRECTION('ref_axis',(-1.,0.,0.));
#72164=DIRECTION('',(-1.,0.,0.));
#72165=DIRECTION('',(-1.,0.,0.));
#72166=DIRECTION('',(0.,0.,1.));
#72167=DIRECTION('center_axis',(0.939692620785909,0.342020143325668,0.));
#72168=DIRECTION('ref_axis',(-0.342020143325668,0.939692620785909,0.));
#72169=DIRECTION('',(-0.342020143325668,0.939692620785909,0.));
#72170=DIRECTION('',(-0.342020143325668,0.939692620785909,0.));
#72171=DIRECTION('',(0.,0.,1.));
#72172=DIRECTION('center_axis',(0.,1.,0.));
#72173=DIRECTION('ref_axis',(-1.,0.,0.));
#72174=DIRECTION('',(-1.,0.,0.));
#72175=DIRECTION('',(-1.,0.,0.));
#72176=DIRECTION('',(0.,0.,1.));
#72177=DIRECTION('center_axis',(-0.939692620785909,0.342020143325668,0.));
#72178=DIRECTION('ref_axis',(-0.342020143325668,-0.939692620785909,0.));
#72179=DIRECTION('',(-0.342020143325668,-0.939692620785909,0.));
#72180=DIRECTION('',(-0.342020143325668,-0.939692620785909,0.));
#72181=DIRECTION('',(0.,0.,1.));
#72182=DIRECTION('center_axis',(0.,1.,0.));
#72183=DIRECTION('ref_axis',(-1.,0.,0.));
#72184=DIRECTION('',(-1.,0.,0.));
#72185=DIRECTION('',(-1.,0.,0.));
#72186=DIRECTION('',(0.,0.,1.));
#72187=DIRECTION('center_axis',(0.939692620785909,0.342020143325668,0.));
#72188=DIRECTION('ref_axis',(-0.342020143325668,0.939692620785909,0.));
#72189=DIRECTION('',(-0.342020143325668,0.939692620785909,0.));
#72190=DIRECTION('',(-0.342020143325668,0.939692620785909,0.));
#72191=DIRECTION('',(0.,0.,1.));
#72192=DIRECTION('center_axis',(0.,1.,0.));
#72193=DIRECTION('ref_axis',(-1.,0.,0.));
#72194=DIRECTION('',(-1.,0.,0.));
#72195=DIRECTION('',(-1.,0.,0.));
#72196=DIRECTION('',(0.,0.,1.));
#72197=DIRECTION('center_axis',(-0.939692620785909,0.342020143325668,0.));
#72198=DIRECTION('ref_axis',(-0.342020143325668,-0.939692620785909,0.));
#72199=DIRECTION('',(-0.342020143325668,-0.939692620785909,0.));
#72200=DIRECTION('',(-0.342020143325668,-0.939692620785909,0.));
#72201=DIRECTION('',(0.,0.,1.));
#72202=DIRECTION('center_axis',(0.,1.,0.));
#72203=DIRECTION('ref_axis',(-1.,0.,0.));
#72204=DIRECTION('',(-1.,0.,0.));
#72205=DIRECTION('',(-1.,0.,0.));
#72206=DIRECTION('',(0.,0.,1.));
#72207=DIRECTION('center_axis',(0.939692620785909,0.342020143325668,0.));
#72208=DIRECTION('ref_axis',(-0.342020143325668,0.939692620785909,0.));
#72209=DIRECTION('',(-0.342020143325668,0.939692620785909,0.));
#72210=DIRECTION('',(-0.342020143325668,0.939692620785909,0.));
#72211=DIRECTION('',(0.,0.,1.));
#72212=DIRECTION('center_axis',(0.,1.,0.));
#72213=DIRECTION('ref_axis',(-1.,0.,0.));
#72214=DIRECTION('',(-1.,0.,0.));
#72215=DIRECTION('',(-1.,0.,0.));
#72216=DIRECTION('',(0.,0.,1.));
#72217=DIRECTION('center_axis',(-0.939692620785909,0.342020143325668,0.));
#72218=DIRECTION('ref_axis',(-0.342020143325668,-0.939692620785909,0.));
#72219=DIRECTION('',(-0.342020143325668,-0.939692620785909,0.));
#72220=DIRECTION('',(-0.342020143325668,-0.939692620785909,0.));
#72221=DIRECTION('',(0.,0.,1.));
#72222=DIRECTION('center_axis',(0.,1.,0.));
#72223=DIRECTION('ref_axis',(-1.,0.,0.));
#72224=DIRECTION('',(-1.,0.,0.));
#72225=DIRECTION('',(-1.,0.,0.));
#72226=DIRECTION('',(0.,0.,1.));
#72227=DIRECTION('center_axis',(0.939692620785909,0.342020143325668,0.));
#72228=DIRECTION('ref_axis',(-0.342020143325668,0.939692620785909,0.));
#72229=DIRECTION('',(-0.342020143325668,0.939692620785909,0.));
#72230=DIRECTION('',(-0.342020143325668,0.939692620785909,0.));
#72231=DIRECTION('',(0.,0.,1.));
#72232=DIRECTION('center_axis',(0.,1.,0.));
#72233=DIRECTION('ref_axis',(-1.,0.,0.));
#72234=DIRECTION('',(-1.,0.,0.));
#72235=DIRECTION('',(-1.,0.,0.));
#72236=DIRECTION('',(0.,0.,1.));
#72237=DIRECTION('center_axis',(-0.939692620785909,0.342020143325668,0.));
#72238=DIRECTION('ref_axis',(-0.342020143325668,-0.939692620785909,0.));
#72239=DIRECTION('',(-0.342020143325668,-0.939692620785909,0.));
#72240=DIRECTION('',(-0.342020143325668,-0.939692620785909,0.));
#72241=DIRECTION('',(0.,0.,1.));
#72242=DIRECTION('center_axis',(0.,1.,0.));
#72243=DIRECTION('ref_axis',(-1.,0.,0.));
#72244=DIRECTION('',(-1.,0.,0.));
#72245=DIRECTION('',(-1.,0.,0.));
#72246=DIRECTION('',(0.,0.,1.));
#72247=DIRECTION('center_axis',(0.939692620785909,0.342020143325668,0.));
#72248=DIRECTION('ref_axis',(-0.342020143325668,0.939692620785909,0.));
#72249=DIRECTION('',(-0.342020143325668,0.939692620785909,0.));
#72250=DIRECTION('',(-0.342020143325668,0.939692620785909,0.));
#72251=DIRECTION('',(0.,0.,1.));
#72252=DIRECTION('center_axis',(0.,1.,0.));
#72253=DIRECTION('ref_axis',(-1.,0.,0.));
#72254=DIRECTION('',(-1.,0.,0.));
#72255=DIRECTION('',(-1.,0.,0.));
#72256=DIRECTION('',(0.,0.,1.));
#72257=DIRECTION('center_axis',(-0.939692620785909,0.342020143325668,0.));
#72258=DIRECTION('ref_axis',(-0.342020143325668,-0.939692620785909,0.));
#72259=DIRECTION('',(-0.342020143325668,-0.939692620785909,0.));
#72260=DIRECTION('',(-0.342020143325668,-0.939692620785909,0.));
#72261=DIRECTION('',(0.,0.,1.));
#72262=DIRECTION('center_axis',(0.,1.,0.));
#72263=DIRECTION('ref_axis',(-1.,0.,0.));
#72264=DIRECTION('',(-1.,0.,0.));
#72265=DIRECTION('',(-1.,0.,0.));
#72266=DIRECTION('',(0.,0.,1.));
#72267=DIRECTION('center_axis',(0.939692620785909,0.342020143325668,0.));
#72268=DIRECTION('ref_axis',(-0.342020143325668,0.939692620785909,0.));
#72269=DIRECTION('',(-0.342020143325668,0.939692620785909,0.));
#72270=DIRECTION('',(-0.342020143325668,0.939692620785909,0.));
#72271=DIRECTION('',(0.,0.,1.));
#72272=DIRECTION('center_axis',(0.,1.,0.));
#72273=DIRECTION('ref_axis',(-1.,0.,0.));
#72274=DIRECTION('',(-1.,0.,0.));
#72275=DIRECTION('',(-1.,0.,0.));
#72276=DIRECTION('',(0.,0.,1.));
#72277=DIRECTION('center_axis',(-0.939692620785909,0.342020143325668,0.));
#72278=DIRECTION('ref_axis',(-0.342020143325668,-0.939692620785909,0.));
#72279=DIRECTION('',(-0.342020143325668,-0.939692620785909,0.));
#72280=DIRECTION('',(-0.342020143325668,-0.939692620785909,0.));
#72281=DIRECTION('',(0.,0.,1.));
#72282=DIRECTION('center_axis',(0.,1.,0.));
#72283=DIRECTION('ref_axis',(-1.,0.,0.));
#72284=DIRECTION('',(-1.,0.,0.));
#72285=DIRECTION('',(-1.,0.,0.));
#72286=DIRECTION('',(0.,0.,1.));
#72287=DIRECTION('center_axis',(0.939692620785909,0.342020143325668,0.));
#72288=DIRECTION('ref_axis',(-0.342020143325668,0.939692620785909,0.));
#72289=DIRECTION('',(-0.342020143325668,0.939692620785909,0.));
#72290=DIRECTION('',(-0.342020143325668,0.939692620785909,0.));
#72291=DIRECTION('',(0.,0.,1.));
#72292=DIRECTION('center_axis',(0.,1.,0.));
#72293=DIRECTION('ref_axis',(-1.,0.,0.));
#72294=DIRECTION('',(-1.,0.,0.));
#72295=DIRECTION('',(-1.,0.,0.));
#72296=DIRECTION('',(0.,0.,1.));
#72297=DIRECTION('center_axis',(-0.939692620785909,0.342020143325668,0.));
#72298=DIRECTION('ref_axis',(-0.342020143325668,-0.939692620785909,0.));
#72299=DIRECTION('',(-0.342020143325668,-0.939692620785909,0.));
#72300=DIRECTION('',(-0.342020143325668,-0.939692620785909,0.));
#72301=DIRECTION('',(0.,0.,1.));
#72302=DIRECTION('center_axis',(0.,1.,0.));
#72303=DIRECTION('ref_axis',(-1.,0.,0.));
#72304=DIRECTION('',(-1.,0.,0.));
#72305=DIRECTION('',(-1.,0.,0.));
#72306=DIRECTION('',(0.,0.,1.));
#72307=DIRECTION('center_axis',(0.939692620785909,0.342020143325668,0.));
#72308=DIRECTION('ref_axis',(-0.342020143325668,0.939692620785909,0.));
#72309=DIRECTION('',(-0.342020143325668,0.939692620785909,0.));
#72310=DIRECTION('',(-0.342020143325668,0.939692620785909,0.));
#72311=DIRECTION('',(0.,0.,1.));
#72312=DIRECTION('center_axis',(0.,1.,0.));
#72313=DIRECTION('ref_axis',(-1.,0.,0.));
#72314=DIRECTION('',(-1.,0.,0.));
#72315=DIRECTION('',(-1.,0.,0.));
#72316=DIRECTION('',(0.,0.,1.));
#72317=DIRECTION('center_axis',(-0.939692620785909,0.342020143325668,0.));
#72318=DIRECTION('ref_axis',(-0.342020143325668,-0.939692620785909,0.));
#72319=DIRECTION('',(-0.342020143325668,-0.939692620785909,0.));
#72320=DIRECTION('',(-0.342020143325668,-0.939692620785909,0.));
#72321=DIRECTION('',(0.,0.,1.));
#72322=DIRECTION('center_axis',(0.,1.,0.));
#72323=DIRECTION('ref_axis',(-1.,0.,0.));
#72324=DIRECTION('',(-1.,0.,0.));
#72325=DIRECTION('',(-1.,0.,0.));
#72326=DIRECTION('',(0.,0.,1.));
#72327=DIRECTION('center_axis',(0.939692620785909,0.342020143325668,0.));
#72328=DIRECTION('ref_axis',(-0.342020143325668,0.939692620785909,0.));
#72329=DIRECTION('',(-0.342020143325668,0.939692620785909,0.));
#72330=DIRECTION('',(-0.342020143325668,0.939692620785909,0.));
#72331=DIRECTION('',(0.,0.,1.));
#72332=DIRECTION('center_axis',(0.,1.,0.));
#72333=DIRECTION('ref_axis',(-1.,0.,0.));
#72334=DIRECTION('',(-1.,0.,0.));
#72335=DIRECTION('',(-1.,0.,0.));
#72336=DIRECTION('',(0.,0.,1.));
#72337=DIRECTION('center_axis',(-0.939692620785909,0.342020143325668,0.));
#72338=DIRECTION('ref_axis',(-0.342020143325668,-0.939692620785909,0.));
#72339=DIRECTION('',(-0.342020143325668,-0.939692620785909,0.));
#72340=DIRECTION('',(-0.342020143325668,-0.939692620785909,0.));
#72341=DIRECTION('',(0.,0.,1.));
#72342=DIRECTION('center_axis',(0.,1.,0.));
#72343=DIRECTION('ref_axis',(-1.,0.,0.));
#72344=DIRECTION('',(-1.,0.,0.));
#72345=DIRECTION('',(-1.,0.,0.));
#72346=DIRECTION('',(0.,0.,1.));
#72347=DIRECTION('center_axis',(0.939692620785909,0.342020143325668,0.));
#72348=DIRECTION('ref_axis',(-0.342020143325668,0.939692620785909,0.));
#72349=DIRECTION('',(-0.342020143325668,0.939692620785909,0.));
#72350=DIRECTION('',(-0.342020143325668,0.939692620785909,0.));
#72351=DIRECTION('',(0.,0.,1.));
#72352=DIRECTION('center_axis',(0.,1.,0.));
#72353=DIRECTION('ref_axis',(-1.,0.,0.));
#72354=DIRECTION('',(-1.,0.,0.));
#72355=DIRECTION('',(-1.,0.,0.));
#72356=DIRECTION('',(0.,0.,1.));
#72357=DIRECTION('center_axis',(-0.939692620785909,0.342020143325668,0.));
#72358=DIRECTION('ref_axis',(-0.342020143325668,-0.939692620785909,0.));
#72359=DIRECTION('',(-0.342020143325668,-0.939692620785909,0.));
#72360=DIRECTION('',(-0.342020143325668,-0.939692620785909,0.));
#72361=DIRECTION('',(0.,0.,1.));
#72362=DIRECTION('center_axis',(0.,1.,0.));
#72363=DIRECTION('ref_axis',(-1.,0.,0.));
#72364=DIRECTION('',(-1.,0.,0.));
#72365=DIRECTION('',(-1.,0.,0.));
#72366=DIRECTION('',(0.,0.,1.));
#72367=DIRECTION('center_axis',(0.939692620785909,0.342020143325668,0.));
#72368=DIRECTION('ref_axis',(-0.342020143325668,0.939692620785909,0.));
#72369=DIRECTION('',(-0.342020143325668,0.939692620785909,0.));
#72370=DIRECTION('',(-0.342020143325668,0.939692620785909,0.));
#72371=DIRECTION('',(0.,0.,1.));
#72372=DIRECTION('center_axis',(0.,1.,0.));
#72373=DIRECTION('ref_axis',(-1.,0.,0.));
#72374=DIRECTION('',(-1.,0.,0.));
#72375=DIRECTION('',(-1.,0.,0.));
#72376=DIRECTION('',(0.,0.,1.));
#72377=DIRECTION('center_axis',(-0.939692620785909,0.342020143325668,0.));
#72378=DIRECTION('ref_axis',(-0.342020143325668,-0.939692620785909,0.));
#72379=DIRECTION('',(-0.342020143325668,-0.939692620785909,0.));
#72380=DIRECTION('',(-0.342020143325668,-0.939692620785909,0.));
#72381=DIRECTION('',(0.,0.,1.));
#72382=DIRECTION('center_axis',(0.,1.,0.));
#72383=DIRECTION('ref_axis',(-1.,0.,0.));
#72384=DIRECTION('',(-1.,0.,0.));
#72385=DIRECTION('',(-1.,0.,0.));
#72386=DIRECTION('',(0.,0.,1.));
#72387=DIRECTION('center_axis',(0.939692620785909,0.342020143325668,0.));
#72388=DIRECTION('ref_axis',(-0.342020143325668,0.939692620785909,0.));
#72389=DIRECTION('',(-0.342020143325668,0.939692620785909,0.));
#72390=DIRECTION('',(-0.342020143325668,0.939692620785909,0.));
#72391=DIRECTION('',(0.,0.,1.));
#72392=DIRECTION('center_axis',(0.,1.,0.));
#72393=DIRECTION('ref_axis',(-1.,0.,0.));
#72394=DIRECTION('',(-1.,0.,0.));
#72395=DIRECTION('',(-1.,0.,0.));
#72396=DIRECTION('',(0.,0.,1.));
#72397=DIRECTION('center_axis',(-0.939692620785909,0.342020143325668,0.));
#72398=DIRECTION('ref_axis',(-0.342020143325668,-0.939692620785909,0.));
#72399=DIRECTION('',(-0.342020143325668,-0.939692620785909,0.));
#72400=DIRECTION('',(-0.342020143325668,-0.939692620785909,0.));
#72401=DIRECTION('',(0.,0.,1.));
#72402=DIRECTION('center_axis',(0.,1.,0.));
#72403=DIRECTION('ref_axis',(-1.,0.,0.));
#72404=DIRECTION('',(-1.,0.,0.));
#72405=DIRECTION('',(-1.,0.,0.));
#72406=DIRECTION('',(0.,0.,1.));
#72407=DIRECTION('center_axis',(0.939692620785909,0.342020143325668,0.));
#72408=DIRECTION('ref_axis',(-0.342020143325668,0.939692620785909,0.));
#72409=DIRECTION('',(-0.342020143325668,0.939692620785909,0.));
#72410=DIRECTION('',(-0.342020143325668,0.939692620785909,0.));
#72411=DIRECTION('',(0.,0.,1.));
#72412=DIRECTION('center_axis',(0.,1.,0.));
#72413=DIRECTION('ref_axis',(-1.,0.,0.));
#72414=DIRECTION('',(-1.,0.,0.));
#72415=DIRECTION('',(-1.,0.,0.));
#72416=DIRECTION('',(0.,0.,1.));
#72417=DIRECTION('center_axis',(-0.939692620785909,0.342020143325668,0.));
#72418=DIRECTION('ref_axis',(-0.342020143325668,-0.939692620785909,0.));
#72419=DIRECTION('',(-0.342020143325668,-0.939692620785909,0.));
#72420=DIRECTION('',(-0.342020143325668,-0.939692620785909,0.));
#72421=DIRECTION('',(0.,0.,1.));
#72422=DIRECTION('center_axis',(0.,1.,0.));
#72423=DIRECTION('ref_axis',(-1.,0.,0.));
#72424=DIRECTION('',(-1.,0.,0.));
#72425=DIRECTION('',(-1.,0.,0.));
#72426=DIRECTION('',(0.,0.,1.));
#72427=DIRECTION('center_axis',(0.939692620785909,0.342020143325668,0.));
#72428=DIRECTION('ref_axis',(-0.342020143325668,0.939692620785909,0.));
#72429=DIRECTION('',(-0.342020143325668,0.939692620785909,0.));
#72430=DIRECTION('',(-0.342020143325668,0.939692620785909,0.));
#72431=DIRECTION('',(0.,0.,1.));
#72432=DIRECTION('center_axis',(0.,1.,0.));
#72433=DIRECTION('ref_axis',(-1.,0.,0.));
#72434=DIRECTION('',(-1.,0.,0.));
#72435=DIRECTION('',(-1.,0.,0.));
#72436=DIRECTION('',(0.,0.,1.));
#72437=DIRECTION('center_axis',(-0.939692620785909,0.342020143325668,0.));
#72438=DIRECTION('ref_axis',(-0.342020143325668,-0.939692620785909,0.));
#72439=DIRECTION('',(-0.342020143325668,-0.939692620785909,0.));
#72440=DIRECTION('',(-0.342020143325668,-0.939692620785909,0.));
#72441=DIRECTION('',(0.,0.,1.));
#72442=DIRECTION('center_axis',(0.,1.,0.));
#72443=DIRECTION('ref_axis',(-1.,0.,0.));
#72444=DIRECTION('',(-1.,0.,0.));
#72445=DIRECTION('',(-1.,0.,0.));
#72446=DIRECTION('',(0.,0.,1.));
#72447=DIRECTION('center_axis',(0.939692620785909,0.342020143325668,0.));
#72448=DIRECTION('ref_axis',(-0.342020143325668,0.939692620785909,0.));
#72449=DIRECTION('',(-0.342020143325668,0.939692620785909,0.));
#72450=DIRECTION('',(-0.342020143325668,0.939692620785909,0.));
#72451=DIRECTION('',(0.,0.,1.));
#72452=DIRECTION('center_axis',(0.,1.,0.));
#72453=DIRECTION('ref_axis',(-1.,0.,0.));
#72454=DIRECTION('',(-1.,0.,0.));
#72455=DIRECTION('',(-1.,0.,0.));
#72456=DIRECTION('',(0.,0.,1.));
#72457=DIRECTION('center_axis',(-0.939692620785909,0.342020143325668,0.));
#72458=DIRECTION('ref_axis',(-0.342020143325668,-0.939692620785909,0.));
#72459=DIRECTION('',(-0.342020143325668,-0.939692620785909,0.));
#72460=DIRECTION('',(-0.342020143325668,-0.939692620785909,0.));
#72461=DIRECTION('',(0.,0.,1.));
#72462=DIRECTION('center_axis',(0.,1.,0.));
#72463=DIRECTION('ref_axis',(-1.,0.,0.));
#72464=DIRECTION('',(-1.,0.,0.));
#72465=DIRECTION('',(-1.,0.,0.));
#72466=DIRECTION('',(0.,0.,1.));
#72467=DIRECTION('center_axis',(0.939692620785909,0.342020143325668,0.));
#72468=DIRECTION('ref_axis',(-0.342020143325668,0.939692620785909,0.));
#72469=DIRECTION('',(-0.342020143325668,0.939692620785909,0.));
#72470=DIRECTION('',(-0.342020143325668,0.939692620785909,0.));
#72471=DIRECTION('',(0.,0.,1.));
#72472=DIRECTION('center_axis',(0.,1.,0.));
#72473=DIRECTION('ref_axis',(-1.,0.,0.));
#72474=DIRECTION('',(-1.,0.,0.));
#72475=DIRECTION('',(-1.,0.,0.));
#72476=DIRECTION('',(0.,0.,1.));
#72477=DIRECTION('center_axis',(-0.939692620785909,0.342020143325668,0.));
#72478=DIRECTION('ref_axis',(-0.342020143325668,-0.939692620785909,0.));
#72479=DIRECTION('',(-0.342020143325668,-0.939692620785909,0.));
#72480=DIRECTION('',(-0.342020143325668,-0.939692620785909,0.));
#72481=DIRECTION('',(0.,0.,1.));
#72482=DIRECTION('center_axis',(0.,1.,0.));
#72483=DIRECTION('ref_axis',(-1.,0.,0.));
#72484=DIRECTION('',(-1.,0.,0.));
#72485=DIRECTION('',(-1.,0.,0.));
#72486=DIRECTION('',(0.,0.,1.));
#72487=DIRECTION('center_axis',(0.939692620785909,0.342020143325668,0.));
#72488=DIRECTION('ref_axis',(-0.342020143325668,0.939692620785909,0.));
#72489=DIRECTION('',(-0.342020143325668,0.939692620785909,0.));
#72490=DIRECTION('',(-0.342020143325668,0.939692620785909,0.));
#72491=DIRECTION('',(0.,0.,1.));
#72492=DIRECTION('center_axis',(0.,1.,0.));
#72493=DIRECTION('ref_axis',(-1.,0.,0.));
#72494=DIRECTION('',(-1.,0.,0.));
#72495=DIRECTION('',(-1.,0.,0.));
#72496=DIRECTION('',(0.,0.,1.));
#72497=DIRECTION('center_axis',(-0.939692620785909,0.342020143325668,0.));
#72498=DIRECTION('ref_axis',(-0.342020143325668,-0.939692620785909,0.));
#72499=DIRECTION('',(-0.342020143325668,-0.939692620785909,0.));
#72500=DIRECTION('',(-0.342020143325668,-0.939692620785909,0.));
#72501=DIRECTION('',(0.,0.,1.));
#72502=DIRECTION('center_axis',(0.,1.,0.));
#72503=DIRECTION('ref_axis',(-1.,0.,0.));
#72504=DIRECTION('',(-1.,0.,0.));
#72505=DIRECTION('',(-1.,0.,0.));
#72506=DIRECTION('',(0.,0.,1.));
#72507=DIRECTION('center_axis',(0.939692620785909,0.342020143325668,0.));
#72508=DIRECTION('ref_axis',(-0.342020143325668,0.939692620785909,0.));
#72509=DIRECTION('',(-0.342020143325668,0.939692620785909,0.));
#72510=DIRECTION('',(-0.342020143325668,0.939692620785909,0.));
#72511=DIRECTION('',(0.,0.,1.));
#72512=DIRECTION('center_axis',(0.,1.,0.));
#72513=DIRECTION('ref_axis',(-1.,0.,0.));
#72514=DIRECTION('',(-1.,0.,0.));
#72515=DIRECTION('',(-1.,0.,0.));
#72516=DIRECTION('',(0.,0.,1.));
#72517=DIRECTION('center_axis',(-0.939692620785909,0.342020143325668,0.));
#72518=DIRECTION('ref_axis',(-0.342020143325668,-0.939692620785909,0.));
#72519=DIRECTION('',(-0.342020143325668,-0.939692620785909,0.));
#72520=DIRECTION('',(-0.342020143325668,-0.939692620785909,0.));
#72521=DIRECTION('',(0.,0.,1.));
#72522=DIRECTION('center_axis',(0.,1.,0.));
#72523=DIRECTION('ref_axis',(-1.,0.,0.));
#72524=DIRECTION('',(-1.,0.,0.));
#72525=DIRECTION('',(-1.,0.,0.));
#72526=DIRECTION('',(0.,0.,1.));
#72527=DIRECTION('center_axis',(0.939692620785909,0.342020143325668,0.));
#72528=DIRECTION('ref_axis',(-0.342020143325668,0.939692620785909,0.));
#72529=DIRECTION('',(-0.342020143325668,0.939692620785909,0.));
#72530=DIRECTION('',(-0.342020143325668,0.939692620785909,0.));
#72531=DIRECTION('',(0.,0.,1.));
#72532=DIRECTION('center_axis',(0.,1.,0.));
#72533=DIRECTION('ref_axis',(-1.,0.,0.));
#72534=DIRECTION('',(-1.,0.,0.));
#72535=DIRECTION('',(-1.,0.,0.));
#72536=DIRECTION('',(0.,0.,1.));
#72537=DIRECTION('center_axis',(-0.939692620785909,0.342020143325668,0.));
#72538=DIRECTION('ref_axis',(-0.342020143325668,-0.939692620785909,0.));
#72539=DIRECTION('',(-0.342020143325668,-0.939692620785909,0.));
#72540=DIRECTION('',(-0.342020143325668,-0.939692620785909,0.));
#72541=DIRECTION('',(0.,0.,1.));
#72542=DIRECTION('center_axis',(0.,1.,0.));
#72543=DIRECTION('ref_axis',(-1.,0.,0.));
#72544=DIRECTION('',(-1.,0.,0.));
#72545=DIRECTION('',(-1.,0.,0.));
#72546=DIRECTION('',(0.,0.,1.));
#72547=DIRECTION('center_axis',(0.939692620785909,0.342020143325668,0.));
#72548=DIRECTION('ref_axis',(-0.342020143325668,0.939692620785909,0.));
#72549=DIRECTION('',(-0.342020143325668,0.939692620785909,0.));
#72550=DIRECTION('',(-0.342020143325668,0.939692620785909,0.));
#72551=DIRECTION('',(0.,0.,1.));
#72552=DIRECTION('center_axis',(0.,1.,0.));
#72553=DIRECTION('ref_axis',(-1.,0.,0.));
#72554=DIRECTION('',(-1.,0.,0.));
#72555=DIRECTION('',(-1.,0.,0.));
#72556=DIRECTION('',(0.,0.,1.));
#72557=DIRECTION('center_axis',(-0.939692620785909,0.342020143325668,0.));
#72558=DIRECTION('ref_axis',(-0.342020143325668,-0.939692620785909,0.));
#72559=DIRECTION('',(-0.342020143325668,-0.939692620785909,0.));
#72560=DIRECTION('',(-0.342020143325668,-0.939692620785909,0.));
#72561=DIRECTION('',(0.,0.,1.));
#72562=DIRECTION('center_axis',(0.,1.,0.));
#72563=DIRECTION('ref_axis',(-1.,0.,0.));
#72564=DIRECTION('',(-1.,0.,0.));
#72565=DIRECTION('',(-1.,0.,0.));
#72566=DIRECTION('',(0.,0.,1.));
#72567=DIRECTION('center_axis',(0.939692620785909,0.342020143325668,0.));
#72568=DIRECTION('ref_axis',(-0.342020143325668,0.939692620785909,0.));
#72569=DIRECTION('',(-0.342020143325668,0.939692620785909,0.));
#72570=DIRECTION('',(-0.342020143325668,0.939692620785909,0.));
#72571=DIRECTION('',(0.,0.,1.));
#72572=DIRECTION('center_axis',(0.,1.,0.));
#72573=DIRECTION('ref_axis',(-1.,0.,0.));
#72574=DIRECTION('',(-1.,0.,0.));
#72575=DIRECTION('',(-1.,0.,0.));
#72576=DIRECTION('',(0.,0.,1.));
#72577=DIRECTION('center_axis',(-0.939692620785909,0.342020143325668,0.));
#72578=DIRECTION('ref_axis',(-0.342020143325668,-0.939692620785909,0.));
#72579=DIRECTION('',(-0.342020143325668,-0.939692620785909,0.));
#72580=DIRECTION('',(-0.342020143325668,-0.939692620785909,0.));
#72581=DIRECTION('',(0.,0.,1.));
#72582=DIRECTION('center_axis',(0.,1.,0.));
#72583=DIRECTION('ref_axis',(-1.,0.,0.));
#72584=DIRECTION('',(-1.,0.,0.));
#72585=DIRECTION('',(-1.,0.,0.));
#72586=DIRECTION('',(0.,0.,1.));
#72587=DIRECTION('center_axis',(0.939692620785909,0.342020143325668,0.));
#72588=DIRECTION('ref_axis',(-0.342020143325668,0.939692620785909,0.));
#72589=DIRECTION('',(-0.342020143325668,0.939692620785909,0.));
#72590=DIRECTION('',(-0.342020143325668,0.939692620785909,0.));
#72591=DIRECTION('',(0.,0.,1.));
#72592=DIRECTION('center_axis',(0.,1.,0.));
#72593=DIRECTION('ref_axis',(-1.,0.,0.));
#72594=DIRECTION('',(-1.,0.,0.));
#72595=DIRECTION('',(-1.,0.,0.));
#72596=DIRECTION('',(0.,0.,1.));
#72597=DIRECTION('center_axis',(-0.939692620785909,0.342020143325668,0.));
#72598=DIRECTION('ref_axis',(-0.342020143325668,-0.939692620785909,0.));
#72599=DIRECTION('',(-0.342020143325668,-0.939692620785909,0.));
#72600=DIRECTION('',(-0.342020143325668,-0.939692620785909,0.));
#72601=DIRECTION('',(0.,0.,1.));
#72602=DIRECTION('center_axis',(0.,1.,0.));
#72603=DIRECTION('ref_axis',(-1.,0.,0.));
#72604=DIRECTION('',(-1.,0.,0.));
#72605=DIRECTION('',(-1.,0.,0.));
#72606=DIRECTION('',(0.,0.,1.));
#72607=DIRECTION('center_axis',(0.939692620785909,0.342020143325668,0.));
#72608=DIRECTION('ref_axis',(-0.342020143325668,0.939692620785909,0.));
#72609=DIRECTION('',(-0.342020143325668,0.939692620785909,0.));
#72610=DIRECTION('',(-0.342020143325668,0.939692620785909,0.));
#72611=DIRECTION('',(0.,0.,1.));
#72612=DIRECTION('center_axis',(0.,1.,0.));
#72613=DIRECTION('ref_axis',(-1.,0.,0.));
#72614=DIRECTION('',(-1.,0.,0.));
#72615=DIRECTION('',(-1.,0.,0.));
#72616=DIRECTION('',(0.,0.,1.));
#72617=DIRECTION('center_axis',(-0.939692620785909,0.342020143325668,0.));
#72618=DIRECTION('ref_axis',(-0.342020143325668,-0.939692620785909,0.));
#72619=DIRECTION('',(-0.342020143325668,-0.939692620785909,0.));
#72620=DIRECTION('',(-0.342020143325668,-0.939692620785909,0.));
#72621=DIRECTION('',(0.,0.,1.));
#72622=DIRECTION('center_axis',(0.,1.,0.));
#72623=DIRECTION('ref_axis',(-1.,0.,0.));
#72624=DIRECTION('',(-1.,0.,0.));
#72625=DIRECTION('',(-1.,0.,0.));
#72626=DIRECTION('',(0.,0.,1.));
#72627=DIRECTION('center_axis',(0.939692620785909,0.342020143325668,0.));
#72628=DIRECTION('ref_axis',(-0.342020143325668,0.939692620785909,0.));
#72629=DIRECTION('',(-0.342020143325668,0.939692620785909,0.));
#72630=DIRECTION('',(-0.342020143325668,0.939692620785909,0.));
#72631=DIRECTION('',(0.,0.,1.));
#72632=DIRECTION('center_axis',(0.,1.,0.));
#72633=DIRECTION('ref_axis',(-1.,0.,0.));
#72634=DIRECTION('',(-1.,0.,0.));
#72635=DIRECTION('',(-1.,0.,0.));
#72636=DIRECTION('',(0.,0.,1.));
#72637=DIRECTION('center_axis',(-0.939692620785909,0.342020143325668,0.));
#72638=DIRECTION('ref_axis',(-0.342020143325668,-0.939692620785909,0.));
#72639=DIRECTION('',(-0.342020143325668,-0.939692620785909,0.));
#72640=DIRECTION('',(-0.342020143325668,-0.939692620785909,0.));
#72641=DIRECTION('',(0.,0.,1.));
#72642=DIRECTION('center_axis',(0.,1.,0.));
#72643=DIRECTION('ref_axis',(-1.,0.,0.));
#72644=DIRECTION('',(-1.,0.,0.));
#72645=DIRECTION('',(-1.,0.,0.));
#72646=DIRECTION('',(0.,0.,1.));
#72647=DIRECTION('center_axis',(0.939692620785909,0.342020143325668,0.));
#72648=DIRECTION('ref_axis',(-0.342020143325668,0.939692620785909,0.));
#72649=DIRECTION('',(-0.342020143325668,0.939692620785909,0.));
#72650=DIRECTION('',(-0.342020143325668,0.939692620785909,0.));
#72651=DIRECTION('',(0.,0.,1.));
#72652=DIRECTION('center_axis',(0.,1.,0.));
#72653=DIRECTION('ref_axis',(-1.,0.,0.));
#72654=DIRECTION('',(-1.,0.,0.));
#72655=DIRECTION('',(-1.,0.,0.));
#72656=DIRECTION('',(0.,0.,1.));
#72657=DIRECTION('center_axis',(-0.939692620785909,0.342020143325668,0.));
#72658=DIRECTION('ref_axis',(-0.342020143325668,-0.939692620785909,0.));
#72659=DIRECTION('',(-0.342020143325668,-0.939692620785909,0.));
#72660=DIRECTION('',(-0.342020143325668,-0.939692620785909,0.));
#72661=DIRECTION('',(0.,0.,1.));
#72662=DIRECTION('center_axis',(0.,1.,0.));
#72663=DIRECTION('ref_axis',(-1.,0.,0.));
#72664=DIRECTION('',(-1.,0.,0.));
#72665=DIRECTION('',(-1.,0.,0.));
#72666=DIRECTION('',(0.,0.,1.));
#72667=DIRECTION('center_axis',(0.939692620785914,0.342020143325655,0.));
#72668=DIRECTION('ref_axis',(-0.342020143325655,0.939692620785914,0.));
#72669=DIRECTION('',(-0.342020143325655,0.939692620785914,0.));
#72670=DIRECTION('',(-0.342020143325655,0.939692620785914,0.));
#72671=DIRECTION('',(0.,0.,1.));
#72672=DIRECTION('center_axis',(0.,1.,0.));
#72673=DIRECTION('ref_axis',(-1.,0.,0.));
#72674=DIRECTION('',(-1.,0.,0.));
#72675=DIRECTION('',(-1.,0.,0.));
#72676=DIRECTION('',(0.,0.,1.));
#72677=DIRECTION('center_axis',(-0.939692620785909,0.342020143325668,0.));
#72678=DIRECTION('ref_axis',(-0.342020143325668,-0.939692620785909,0.));
#72679=DIRECTION('',(-0.342020143325668,-0.939692620785909,0.));
#72680=DIRECTION('',(-0.342020143325668,-0.939692620785909,0.));
#72681=DIRECTION('',(0.,0.,1.));
#72682=DIRECTION('center_axis',(0.,1.,0.));
#72683=DIRECTION('ref_axis',(-1.,0.,0.));
#72684=DIRECTION('',(-1.,0.,0.));
#72685=DIRECTION('',(-1.,0.,0.));
#72686=DIRECTION('',(0.,0.,1.));
#72687=DIRECTION('center_axis',(0.939692620785914,0.342020143325655,0.));
#72688=DIRECTION('ref_axis',(-0.342020143325655,0.939692620785914,0.));
#72689=DIRECTION('',(-0.342020143325655,0.939692620785914,0.));
#72690=DIRECTION('',(-0.342020143325655,0.939692620785914,0.));
#72691=DIRECTION('',(0.,0.,1.));
#72692=DIRECTION('center_axis',(0.,1.,0.));
#72693=DIRECTION('ref_axis',(-1.,0.,0.));
#72694=DIRECTION('',(-1.,0.,0.));
#72695=DIRECTION('',(-1.,0.,0.));
#72696=DIRECTION('',(0.,0.,1.));
#72697=DIRECTION('center_axis',(-0.939692620785914,0.342020143325655,0.));
#72698=DIRECTION('ref_axis',(-0.342020143325655,-0.939692620785914,0.));
#72699=DIRECTION('',(-0.342020143325655,-0.939692620785914,0.));
#72700=DIRECTION('',(-0.342020143325655,-0.939692620785914,0.));
#72701=DIRECTION('',(0.,0.,1.));
#72702=DIRECTION('center_axis',(0.,1.,0.));
#72703=DIRECTION('ref_axis',(-1.,0.,0.));
#72704=DIRECTION('',(-1.,0.,0.));
#72705=DIRECTION('',(-1.,0.,0.));
#72706=DIRECTION('',(0.,0.,1.));
#72707=DIRECTION('center_axis',(0.939692620785914,0.342020143325655,0.));
#72708=DIRECTION('ref_axis',(-0.342020143325655,0.939692620785914,0.));
#72709=DIRECTION('',(-0.342020143325655,0.939692620785914,0.));
#72710=DIRECTION('',(-0.342020143325655,0.939692620785914,0.));
#72711=DIRECTION('',(0.,0.,1.));
#72712=DIRECTION('center_axis',(0.,1.,0.));
#72713=DIRECTION('ref_axis',(-1.,0.,0.));
#72714=DIRECTION('',(-1.,0.,0.));
#72715=DIRECTION('',(-1.,0.,0.));
#72716=DIRECTION('',(0.,0.,1.));
#72717=DIRECTION('center_axis',(-0.939692620785909,0.342020143325668,0.));
#72718=DIRECTION('ref_axis',(-0.342020143325668,-0.939692620785909,0.));
#72719=DIRECTION('',(-0.342020143325668,-0.939692620785909,0.));
#72720=DIRECTION('',(-0.342020143325668,-0.939692620785909,0.));
#72721=DIRECTION('',(0.,0.,1.));
#72722=DIRECTION('center_axis',(0.,1.,0.));
#72723=DIRECTION('ref_axis',(-1.,0.,0.));
#72724=DIRECTION('',(-1.,0.,0.));
#72725=DIRECTION('',(-1.,0.,0.));
#72726=DIRECTION('',(0.,0.,1.));
#72727=DIRECTION('center_axis',(0.939692620785914,0.342020143325655,0.));
#72728=DIRECTION('ref_axis',(-0.342020143325655,0.939692620785914,0.));
#72729=DIRECTION('',(-0.342020143325655,0.939692620785914,0.));
#72730=DIRECTION('',(-0.342020143325655,0.939692620785914,0.));
#72731=DIRECTION('',(0.,0.,1.));
#72732=DIRECTION('center_axis',(0.,1.,0.));
#72733=DIRECTION('ref_axis',(-1.,0.,0.));
#72734=DIRECTION('',(-1.,0.,0.));
#72735=DIRECTION('',(-1.,0.,0.));
#72736=DIRECTION('',(0.,0.,1.));
#72737=DIRECTION('center_axis',(-0.939692620785914,0.342020143325655,0.));
#72738=DIRECTION('ref_axis',(-0.342020143325655,-0.939692620785914,0.));
#72739=DIRECTION('',(-0.342020143325655,-0.939692620785914,0.));
#72740=DIRECTION('',(-0.342020143325655,-0.939692620785914,0.));
#72741=DIRECTION('',(0.,0.,1.));
#72742=DIRECTION('center_axis',(0.,1.,0.));
#72743=DIRECTION('ref_axis',(-1.,0.,0.));
#72744=DIRECTION('',(-1.,0.,0.));
#72745=DIRECTION('',(-1.,0.,0.));
#72746=DIRECTION('',(0.,0.,1.));
#72747=DIRECTION('center_axis',(0.939692620785914,0.342020143325655,0.));
#72748=DIRECTION('ref_axis',(-0.342020143325655,0.939692620785914,0.));
#72749=DIRECTION('',(-0.342020143325655,0.939692620785914,0.));
#72750=DIRECTION('',(-0.342020143325655,0.939692620785914,0.));
#72751=DIRECTION('',(0.,0.,1.));
#72752=DIRECTION('center_axis',(0.,1.,0.));
#72753=DIRECTION('ref_axis',(-1.,0.,0.));
#72754=DIRECTION('',(-1.,0.,0.));
#72755=DIRECTION('',(-1.,0.,0.));
#72756=DIRECTION('',(0.,0.,1.));
#72757=DIRECTION('center_axis',(-0.939692620785914,0.342020143325655,0.));
#72758=DIRECTION('ref_axis',(-0.342020143325655,-0.939692620785914,0.));
#72759=DIRECTION('',(-0.342020143325655,-0.939692620785914,0.));
#72760=DIRECTION('',(-0.342020143325655,-0.939692620785914,0.));
#72761=DIRECTION('',(0.,0.,1.));
#72762=DIRECTION('center_axis',(0.,1.,0.));
#72763=DIRECTION('ref_axis',(-1.,0.,0.));
#72764=DIRECTION('',(-1.,0.,0.));
#72765=DIRECTION('',(-1.,0.,0.));
#72766=DIRECTION('',(0.,0.,1.));
#72767=DIRECTION('center_axis',(0.939692620785914,0.342020143325655,0.));
#72768=DIRECTION('ref_axis',(-0.342020143325655,0.939692620785914,0.));
#72769=DIRECTION('',(-0.342020143325655,0.939692620785914,0.));
#72770=DIRECTION('',(-0.342020143325655,0.939692620785914,0.));
#72771=DIRECTION('',(0.,0.,1.));
#72772=DIRECTION('center_axis',(0.,1.,0.));
#72773=DIRECTION('ref_axis',(-1.,0.,0.));
#72774=DIRECTION('',(-1.,0.,0.));
#72775=DIRECTION('',(-1.,0.,0.));
#72776=DIRECTION('',(0.,0.,1.));
#72777=DIRECTION('center_axis',(-0.939692620785914,0.342020143325655,0.));
#72778=DIRECTION('ref_axis',(-0.342020143325655,-0.939692620785914,0.));
#72779=DIRECTION('',(-0.342020143325655,-0.939692620785914,0.));
#72780=DIRECTION('',(-0.342020143325655,-0.939692620785914,0.));
#72781=DIRECTION('',(0.,0.,1.));
#72782=DIRECTION('center_axis',(0.,1.,0.));
#72783=DIRECTION('ref_axis',(-1.,0.,0.));
#72784=DIRECTION('',(-1.,0.,0.));
#72785=DIRECTION('',(-1.,0.,0.));
#72786=DIRECTION('',(0.,0.,1.));
#72787=DIRECTION('center_axis',(0.939692620785909,0.342020143325668,0.));
#72788=DIRECTION('ref_axis',(-0.342020143325668,0.939692620785909,0.));
#72789=DIRECTION('',(-0.342020143325668,0.939692620785909,0.));
#72790=DIRECTION('',(-0.342020143325668,0.939692620785909,0.));
#72791=DIRECTION('',(0.,0.,1.));
#72792=DIRECTION('center_axis',(0.,1.,0.));
#72793=DIRECTION('ref_axis',(-1.,0.,0.));
#72794=DIRECTION('',(-1.,0.,0.));
#72795=DIRECTION('',(-1.,0.,0.));
#72796=DIRECTION('',(0.,0.,1.));
#72797=DIRECTION('center_axis',(-0.939692620785914,0.342020143325655,0.));
#72798=DIRECTION('ref_axis',(-0.342020143325655,-0.939692620785914,0.));
#72799=DIRECTION('',(-0.342020143325655,-0.939692620785914,0.));
#72800=DIRECTION('',(-0.342020143325655,-0.939692620785914,0.));
#72801=DIRECTION('',(0.,0.,1.));
#72802=DIRECTION('center_axis',(0.,1.,0.));
#72803=DIRECTION('ref_axis',(-1.,0.,0.));
#72804=DIRECTION('',(-1.,0.,0.));
#72805=DIRECTION('',(-1.,0.,0.));
#72806=DIRECTION('',(0.,0.,1.));
#72807=DIRECTION('center_axis',(0.939692620785914,0.342020143325655,0.));
#72808=DIRECTION('ref_axis',(-0.342020143325655,0.939692620785914,0.));
#72809=DIRECTION('',(-0.342020143325655,0.939692620785914,0.));
#72810=DIRECTION('',(-0.342020143325655,0.939692620785914,0.));
#72811=DIRECTION('',(0.,0.,1.));
#72812=DIRECTION('center_axis',(0.,1.,0.));
#72813=DIRECTION('ref_axis',(-1.,0.,0.));
#72814=DIRECTION('',(-1.,0.,0.));
#72815=DIRECTION('',(-1.,0.,0.));
#72816=DIRECTION('',(0.,0.,1.));
#72817=DIRECTION('center_axis',(-0.939692620785914,0.342020143325655,0.));
#72818=DIRECTION('ref_axis',(-0.342020143325655,-0.939692620785914,0.));
#72819=DIRECTION('',(-0.342020143325655,-0.939692620785914,0.));
#72820=DIRECTION('',(-0.342020143325655,-0.939692620785914,0.));
#72821=DIRECTION('',(0.,0.,1.));
#72822=DIRECTION('center_axis',(0.,1.,0.));
#72823=DIRECTION('ref_axis',(-1.,0.,0.));
#72824=DIRECTION('',(-1.,0.,0.));
#72825=DIRECTION('',(-1.,0.,0.));
#72826=DIRECTION('',(0.,0.,1.));
#72827=DIRECTION('center_axis',(0.939692620785909,0.342020143325668,0.));
#72828=DIRECTION('ref_axis',(-0.342020143325668,0.939692620785909,0.));
#72829=DIRECTION('',(-0.342020143325668,0.939692620785909,0.));
#72830=DIRECTION('',(-0.342020143325668,0.939692620785909,0.));
#72831=DIRECTION('',(0.,0.,1.));
#72832=DIRECTION('center_axis',(0.,1.,0.));
#72833=DIRECTION('ref_axis',(-1.,0.,0.));
#72834=DIRECTION('',(-1.,0.,0.));
#72835=DIRECTION('',(-1.,0.,0.));
#72836=DIRECTION('',(0.,0.,1.));
#72837=DIRECTION('center_axis',(-0.939692620785914,0.342020143325655,0.));
#72838=DIRECTION('ref_axis',(-0.342020143325655,-0.939692620785914,0.));
#72839=DIRECTION('',(-0.342020143325655,-0.939692620785914,0.));
#72840=DIRECTION('',(-0.342020143325655,-0.939692620785914,0.));
#72841=DIRECTION('',(0.,0.,1.));
#72842=DIRECTION('center_axis',(0.,1.,0.));
#72843=DIRECTION('ref_axis',(-1.,0.,0.));
#72844=DIRECTION('',(-1.,0.,0.));
#72845=DIRECTION('',(-1.,0.,0.));
#72846=DIRECTION('',(0.,0.,1.));
#72847=DIRECTION('center_axis',(0.939692620785914,0.342020143325655,0.));
#72848=DIRECTION('ref_axis',(-0.342020143325655,0.939692620785914,0.));
#72849=DIRECTION('',(-0.342020143325655,0.939692620785914,0.));
#72850=DIRECTION('',(-0.342020143325655,0.939692620785914,0.));
#72851=DIRECTION('',(0.,0.,1.));
#72852=DIRECTION('center_axis',(0.,1.,0.));
#72853=DIRECTION('ref_axis',(-1.,0.,0.));
#72854=DIRECTION('',(-1.,0.,0.));
#72855=DIRECTION('',(-1.,0.,0.));
#72856=DIRECTION('',(0.,0.,1.));
#72857=DIRECTION('center_axis',(-0.939692620785909,0.342020143325668,0.));
#72858=DIRECTION('ref_axis',(-0.342020143325668,-0.939692620785909,0.));
#72859=DIRECTION('',(-0.342020143325668,-0.939692620785909,0.));
#72860=DIRECTION('',(-0.342020143325668,-0.939692620785909,0.));
#72861=DIRECTION('',(0.,0.,1.));
#72862=DIRECTION('center_axis',(0.,1.,0.));
#72863=DIRECTION('ref_axis',(-1.,0.,0.));
#72864=DIRECTION('',(-1.,0.,0.));
#72865=DIRECTION('',(-1.,0.,0.));
#72866=DIRECTION('',(0.,0.,1.));
#72867=DIRECTION('center_axis',(0.939692620785914,0.342020143325655,0.));
#72868=DIRECTION('ref_axis',(-0.342020143325655,0.939692620785914,0.));
#72869=DIRECTION('',(-0.342020143325655,0.939692620785914,0.));
#72870=DIRECTION('',(-0.342020143325655,0.939692620785914,0.));
#72871=DIRECTION('',(0.,0.,1.));
#72872=DIRECTION('center_axis',(0.,1.,0.));
#72873=DIRECTION('ref_axis',(-1.,0.,0.));
#72874=DIRECTION('',(-1.,0.,0.));
#72875=DIRECTION('',(-1.,0.,0.));
#72876=DIRECTION('',(0.,0.,1.));
#72877=DIRECTION('center_axis',(-0.939692620785914,0.342020143325655,0.));
#72878=DIRECTION('ref_axis',(-0.342020143325655,-0.939692620785914,0.));
#72879=DIRECTION('',(-0.342020143325655,-0.939692620785914,0.));
#72880=DIRECTION('',(-0.342020143325655,-0.939692620785914,0.));
#72881=DIRECTION('',(0.,0.,1.));
#72882=DIRECTION('center_axis',(0.,1.,0.));
#72883=DIRECTION('ref_axis',(-1.,0.,0.));
#72884=DIRECTION('',(-1.,0.,0.));
#72885=DIRECTION('',(-1.,0.,0.));
#72886=DIRECTION('',(0.,0.,1.));
#72887=DIRECTION('center_axis',(0.939692620785914,0.342020143325655,0.));
#72888=DIRECTION('ref_axis',(-0.342020143325655,0.939692620785914,0.));
#72889=DIRECTION('',(-0.342020143325655,0.939692620785914,0.));
#72890=DIRECTION('',(-0.342020143325655,0.939692620785914,0.));
#72891=DIRECTION('',(0.,0.,1.));
#72892=DIRECTION('center_axis',(0.,1.,0.));
#72893=DIRECTION('ref_axis',(-1.,0.,0.));
#72894=DIRECTION('',(-1.,0.,0.));
#72895=DIRECTION('',(-1.,0.,0.));
#72896=DIRECTION('',(0.,0.,1.));
#72897=DIRECTION('center_axis',(-0.939692620785914,0.342020143325655,0.));
#72898=DIRECTION('ref_axis',(-0.342020143325655,-0.939692620785914,0.));
#72899=DIRECTION('',(-0.342020143325655,-0.939692620785914,0.));
#72900=DIRECTION('',(-0.342020143325655,-0.939692620785914,0.));
#72901=DIRECTION('',(0.,0.,1.));
#72902=DIRECTION('center_axis',(0.,1.,0.));
#72903=DIRECTION('ref_axis',(-1.,0.,0.));
#72904=DIRECTION('',(-1.,0.,0.));
#72905=DIRECTION('',(-1.,0.,0.));
#72906=DIRECTION('',(0.,0.,1.));
#72907=DIRECTION('center_axis',(0.939692620785914,0.342020143325655,0.));
#72908=DIRECTION('ref_axis',(-0.342020143325655,0.939692620785914,0.));
#72909=DIRECTION('',(-0.342020143325655,0.939692620785914,0.));
#72910=DIRECTION('',(-0.342020143325655,0.939692620785914,0.));
#72911=DIRECTION('',(0.,0.,1.));
#72912=DIRECTION('center_axis',(0.,1.,0.));
#72913=DIRECTION('ref_axis',(-1.,0.,0.));
#72914=DIRECTION('',(-1.,0.,0.));
#72915=DIRECTION('',(-1.,0.,0.));
#72916=DIRECTION('',(0.,0.,1.));
#72917=DIRECTION('center_axis',(-0.939692620785914,0.342020143325655,0.));
#72918=DIRECTION('ref_axis',(-0.342020143325655,-0.939692620785914,0.));
#72919=DIRECTION('',(-0.342020143325655,-0.939692620785914,0.));
#72920=DIRECTION('',(-0.342020143325655,-0.939692620785914,0.));
#72921=DIRECTION('',(0.,0.,1.));
#72922=DIRECTION('center_axis',(0.,1.,0.));
#72923=DIRECTION('ref_axis',(-1.,0.,0.));
#72924=DIRECTION('',(-1.,0.,0.));
#72925=DIRECTION('',(-1.,0.,0.));
#72926=DIRECTION('',(0.,0.,1.));
#72927=DIRECTION('center_axis',(0.939692620785914,0.342020143325655,0.));
#72928=DIRECTION('ref_axis',(-0.342020143325655,0.939692620785914,0.));
#72929=DIRECTION('',(-0.342020143325655,0.939692620785914,0.));
#72930=DIRECTION('',(-0.342020143325655,0.939692620785914,0.));
#72931=DIRECTION('',(0.,0.,1.));
#72932=DIRECTION('center_axis',(0.,1.,0.));
#72933=DIRECTION('ref_axis',(-1.,0.,0.));
#72934=DIRECTION('',(-1.,0.,0.));
#72935=DIRECTION('',(-1.,0.,0.));
#72936=DIRECTION('',(0.,0.,1.));
#72937=DIRECTION('center_axis',(-0.939692620785914,0.342020143325655,0.));
#72938=DIRECTION('ref_axis',(-0.342020143325655,-0.939692620785914,0.));
#72939=DIRECTION('',(-0.342020143325655,-0.939692620785914,0.));
#72940=DIRECTION('',(-0.342020143325655,-0.939692620785914,0.));
#72941=DIRECTION('',(0.,0.,1.));
#72942=DIRECTION('center_axis',(0.,1.,0.));
#72943=DIRECTION('ref_axis',(-1.,0.,0.));
#72944=DIRECTION('',(-1.,0.,0.));
#72945=DIRECTION('',(-1.,0.,0.));
#72946=DIRECTION('',(0.,0.,1.));
#72947=DIRECTION('center_axis',(0.939692620785914,0.342020143325655,0.));
#72948=DIRECTION('ref_axis',(-0.342020143325655,0.939692620785914,0.));
#72949=DIRECTION('',(-0.342020143325655,0.939692620785914,0.));
#72950=DIRECTION('',(-0.342020143325655,0.939692620785914,0.));
#72951=DIRECTION('',(0.,0.,1.));
#72952=DIRECTION('center_axis',(0.,1.,0.));
#72953=DIRECTION('ref_axis',(-1.,0.,0.));
#72954=DIRECTION('',(-1.,0.,0.));
#72955=DIRECTION('',(-1.,0.,0.));
#72956=DIRECTION('',(0.,0.,1.));
#72957=DIRECTION('center_axis',(-0.939692620785914,0.342020143325655,0.));
#72958=DIRECTION('ref_axis',(-0.342020143325655,-0.939692620785914,0.));
#72959=DIRECTION('',(-0.342020143325655,-0.939692620785914,0.));
#72960=DIRECTION('',(-0.342020143325655,-0.939692620785914,0.));
#72961=DIRECTION('',(0.,0.,1.));
#72962=DIRECTION('center_axis',(0.,1.,0.));
#72963=DIRECTION('ref_axis',(-1.,0.,0.));
#72964=DIRECTION('',(-1.,0.,0.));
#72965=DIRECTION('',(-1.,0.,0.));
#72966=DIRECTION('',(0.,0.,1.));
#72967=DIRECTION('center_axis',(0.939692620785909,0.342020143325668,0.));
#72968=DIRECTION('ref_axis',(-0.342020143325668,0.939692620785909,0.));
#72969=DIRECTION('',(-0.342020143325668,0.939692620785909,0.));
#72970=DIRECTION('',(-0.342020143325668,0.939692620785909,0.));
#72971=DIRECTION('',(0.,0.,1.));
#72972=DIRECTION('center_axis',(0.,1.,0.));
#72973=DIRECTION('ref_axis',(-1.,0.,0.));
#72974=DIRECTION('',(-1.,0.,0.));
#72975=DIRECTION('',(-1.,0.,0.));
#72976=DIRECTION('',(0.,0.,1.));
#72977=DIRECTION('center_axis',(-0.939692620785914,0.342020143325655,0.));
#72978=DIRECTION('ref_axis',(-0.342020143325655,-0.939692620785914,0.));
#72979=DIRECTION('',(-0.342020143325655,-0.939692620785914,0.));
#72980=DIRECTION('',(-0.342020143325655,-0.939692620785914,0.));
#72981=DIRECTION('',(0.,0.,1.));
#72982=DIRECTION('center_axis',(0.,1.,0.));
#72983=DIRECTION('ref_axis',(-1.,0.,0.));
#72984=DIRECTION('',(-1.,0.,0.));
#72985=DIRECTION('',(-1.,0.,0.));
#72986=DIRECTION('',(0.,0.,1.));
#72987=DIRECTION('center_axis',(0.939692620785914,0.342020143325655,0.));
#72988=DIRECTION('ref_axis',(-0.342020143325655,0.939692620785914,0.));
#72989=DIRECTION('',(-0.342020143325655,0.939692620785914,0.));
#72990=DIRECTION('',(-0.342020143325655,0.939692620785914,0.));
#72991=DIRECTION('',(0.,0.,1.));
#72992=DIRECTION('center_axis',(0.,1.,0.));
#72993=DIRECTION('ref_axis',(-1.,0.,0.));
#72994=DIRECTION('',(-1.,0.,0.));
#72995=DIRECTION('',(-1.,0.,0.));
#72996=DIRECTION('',(0.,0.,1.));
#72997=DIRECTION('center_axis',(-0.939692620785909,0.342020143325668,0.));
#72998=DIRECTION('ref_axis',(-0.342020143325668,-0.939692620785909,0.));
#72999=DIRECTION('',(-0.342020143325668,-0.939692620785909,0.));
#73000=DIRECTION('',(-0.342020143325668,-0.939692620785909,0.));
#73001=DIRECTION('',(0.,0.,1.));
#73002=DIRECTION('center_axis',(0.,1.,0.));
#73003=DIRECTION('ref_axis',(-1.,0.,0.));
#73004=DIRECTION('',(-1.,0.,0.));
#73005=DIRECTION('',(-1.,0.,0.));
#73006=DIRECTION('',(0.,0.,1.));
#73007=DIRECTION('center_axis',(0.939692620785909,0.342020143325668,0.));
#73008=DIRECTION('ref_axis',(-0.342020143325668,0.939692620785909,0.));
#73009=DIRECTION('',(-0.342020143325668,0.939692620785909,0.));
#73010=DIRECTION('',(-0.342020143325668,0.939692620785909,0.));
#73011=DIRECTION('',(0.,0.,1.));
#73012=DIRECTION('center_axis',(0.,1.,0.));
#73013=DIRECTION('ref_axis',(-1.,0.,0.));
#73014=DIRECTION('',(-1.,0.,0.));
#73015=DIRECTION('',(-1.,0.,0.));
#73016=DIRECTION('',(0.,0.,1.));
#73017=DIRECTION('center_axis',(-0.939692620785914,0.342020143325655,0.));
#73018=DIRECTION('ref_axis',(-0.342020143325655,-0.939692620785914,0.));
#73019=DIRECTION('',(-0.342020143325655,-0.939692620785914,0.));
#73020=DIRECTION('',(-0.342020143325655,-0.939692620785914,0.));
#73021=DIRECTION('',(0.,0.,1.));
#73022=DIRECTION('center_axis',(0.,1.,0.));
#73023=DIRECTION('ref_axis',(-1.,0.,0.));
#73024=DIRECTION('',(-1.,0.,0.));
#73025=DIRECTION('',(-1.,0.,0.));
#73026=DIRECTION('',(0.,0.,1.));
#73027=DIRECTION('center_axis',(0.939692620785914,0.342020143325655,0.));
#73028=DIRECTION('ref_axis',(-0.342020143325655,0.939692620785914,0.));
#73029=DIRECTION('',(-0.342020143325655,0.939692620785914,0.));
#73030=DIRECTION('',(-0.342020143325655,0.939692620785914,0.));
#73031=DIRECTION('',(0.,0.,1.));
#73032=DIRECTION('center_axis',(0.,1.,0.));
#73033=DIRECTION('ref_axis',(-1.,0.,0.));
#73034=DIRECTION('',(-1.,0.,0.));
#73035=DIRECTION('',(-1.,0.,0.));
#73036=DIRECTION('',(0.,0.,1.));
#73037=DIRECTION('center_axis',(-0.939692620785909,0.342020143325668,0.));
#73038=DIRECTION('ref_axis',(-0.342020143325668,-0.939692620785909,0.));
#73039=DIRECTION('',(-0.342020143325668,-0.939692620785909,0.));
#73040=DIRECTION('',(-0.342020143325668,-0.939692620785909,0.));
#73041=DIRECTION('',(0.,0.,1.));
#73042=DIRECTION('center_axis',(0.,1.,0.));
#73043=DIRECTION('ref_axis',(-1.,0.,0.));
#73044=DIRECTION('',(-1.,0.,0.));
#73045=DIRECTION('',(-1.,0.,0.));
#73046=DIRECTION('',(0.,0.,1.));
#73047=DIRECTION('center_axis',(0.939692620785914,0.342020143325655,0.));
#73048=DIRECTION('ref_axis',(-0.342020143325655,0.939692620785914,0.));
#73049=DIRECTION('',(-0.342020143325655,0.939692620785914,0.));
#73050=DIRECTION('',(-0.342020143325655,0.939692620785914,0.));
#73051=DIRECTION('',(0.,0.,1.));
#73052=DIRECTION('center_axis',(0.,1.,0.));
#73053=DIRECTION('ref_axis',(-1.,0.,0.));
#73054=DIRECTION('',(-1.,0.,0.));
#73055=DIRECTION('',(-1.,0.,0.));
#73056=DIRECTION('',(0.,0.,1.));
#73057=DIRECTION('center_axis',(-0.939692620785914,0.342020143325655,0.));
#73058=DIRECTION('ref_axis',(-0.342020143325655,-0.939692620785914,0.));
#73059=DIRECTION('',(-0.342020143325655,-0.939692620785914,0.));
#73060=DIRECTION('',(-0.342020143325655,-0.939692620785914,0.));
#73061=DIRECTION('',(0.,0.,1.));
#73062=DIRECTION('center_axis',(0.,1.,0.));
#73063=DIRECTION('ref_axis',(-1.,0.,0.));
#73064=DIRECTION('',(-1.,0.,0.));
#73065=DIRECTION('',(-1.,0.,0.));
#73066=DIRECTION('',(0.,0.,1.));
#73067=DIRECTION('center_axis',(0.939692620785909,0.342020143325668,0.));
#73068=DIRECTION('ref_axis',(-0.342020143325668,0.939692620785909,0.));
#73069=DIRECTION('',(-0.342020143325668,0.939692620785909,0.));
#73070=DIRECTION('',(-0.342020143325668,0.939692620785909,0.));
#73071=DIRECTION('',(0.,0.,1.));
#73072=DIRECTION('center_axis',(0.,1.,0.));
#73073=DIRECTION('ref_axis',(-1.,0.,0.));
#73074=DIRECTION('',(-1.,0.,0.));
#73075=DIRECTION('',(-1.,0.,0.));
#73076=DIRECTION('',(0.,0.,1.));
#73077=DIRECTION('center_axis',(-0.939692620785909,0.342020143325668,0.));
#73078=DIRECTION('ref_axis',(-0.342020143325668,-0.939692620785909,0.));
#73079=DIRECTION('',(-0.342020143325668,-0.939692620785909,0.));
#73080=DIRECTION('',(-0.342020143325668,-0.939692620785909,0.));
#73081=DIRECTION('',(0.,0.,1.));
#73082=DIRECTION('center_axis',(0.,1.,0.));
#73083=DIRECTION('ref_axis',(-1.,0.,0.));
#73084=DIRECTION('',(-1.,0.,0.));
#73085=DIRECTION('',(-1.,0.,0.));
#73086=DIRECTION('',(0.,0.,1.));
#73087=DIRECTION('center_axis',(0.939692620785919,0.342020143325641,0.));
#73088=DIRECTION('ref_axis',(-0.342020143325641,0.939692620785918,0.));
#73089=DIRECTION('',(-0.342020143325641,0.939692620785918,0.));
#73090=DIRECTION('',(-0.342020143325641,0.939692620785918,0.));
#73091=DIRECTION('',(0.,0.,1.));
#73092=DIRECTION('center_axis',(0.,1.,0.));
#73093=DIRECTION('ref_axis',(-1.,0.,0.));
#73094=DIRECTION('',(-1.,0.,0.));
#73095=DIRECTION('',(-1.,0.,0.));
#73096=DIRECTION('',(0.,0.,1.));
#73097=DIRECTION('center_axis',(-0.939692620785909,0.342020143325668,0.));
#73098=DIRECTION('ref_axis',(-0.342020143325668,-0.939692620785909,0.));
#73099=DIRECTION('',(-0.342020143325668,-0.939692620785909,0.));
#73100=DIRECTION('',(-0.342020143325668,-0.939692620785909,0.));
#73101=DIRECTION('',(0.,0.,1.));
#73102=DIRECTION('center_axis',(0.,1.,0.));
#73103=DIRECTION('ref_axis',(-1.,0.,0.));
#73104=DIRECTION('',(-1.,0.,0.));
#73105=DIRECTION('',(-1.,0.,0.));
#73106=DIRECTION('',(0.,0.,1.));
#73107=DIRECTION('center_axis',(0.939692620785909,0.342020143325668,0.));
#73108=DIRECTION('ref_axis',(-0.342020143325668,0.939692620785909,0.));
#73109=DIRECTION('',(-0.342020143325668,0.939692620785909,0.));
#73110=DIRECTION('',(-0.342020143325668,0.939692620785909,0.));
#73111=DIRECTION('',(0.,0.,1.));
#73112=DIRECTION('center_axis',(0.,1.,0.));
#73113=DIRECTION('ref_axis',(-1.,0.,0.));
#73114=DIRECTION('',(-1.,0.,0.));
#73115=DIRECTION('',(-1.,0.,0.));
#73116=DIRECTION('',(0.,0.,1.));
#73117=DIRECTION('center_axis',(-0.939692620785919,0.342020143325641,0.));
#73118=DIRECTION('ref_axis',(-0.342020143325641,-0.939692620785918,0.));
#73119=DIRECTION('',(-0.342020143325641,-0.939692620785918,0.));
#73120=DIRECTION('',(-0.342020143325641,-0.939692620785918,0.));
#73121=DIRECTION('',(0.,0.,1.));
#73122=DIRECTION('center_axis',(0.,1.,0.));
#73123=DIRECTION('ref_axis',(-1.,0.,0.));
#73124=DIRECTION('',(-1.,0.,0.));
#73125=DIRECTION('',(-1.,0.,0.));
#73126=DIRECTION('',(0.,0.,1.));
#73127=DIRECTION('center_axis',(0.939692620785919,0.342020143325641,0.));
#73128=DIRECTION('ref_axis',(-0.342020143325641,0.939692620785918,0.));
#73129=DIRECTION('',(-0.342020143325641,0.939692620785918,0.));
#73130=DIRECTION('',(-0.342020143325641,0.939692620785918,0.));
#73131=DIRECTION('',(0.,0.,1.));
#73132=DIRECTION('center_axis',(0.,1.,0.));
#73133=DIRECTION('ref_axis',(-1.,0.,0.));
#73134=DIRECTION('',(-1.,0.,0.));
#73135=DIRECTION('',(-1.,0.,0.));
#73136=DIRECTION('',(0.,0.,1.));
#73137=DIRECTION('center_axis',(-0.939692620785909,0.342020143325668,0.));
#73138=DIRECTION('ref_axis',(-0.342020143325668,-0.939692620785909,0.));
#73139=DIRECTION('',(-0.342020143325668,-0.939692620785909,0.));
#73140=DIRECTION('',(-0.342020143325668,-0.939692620785909,0.));
#73141=DIRECTION('',(0.,0.,1.));
#73142=DIRECTION('center_axis',(0.,1.,0.));
#73143=DIRECTION('ref_axis',(-1.,0.,0.));
#73144=DIRECTION('',(-1.,0.,0.));
#73145=DIRECTION('',(-1.,0.,0.));
#73146=DIRECTION('',(0.,0.,1.));
#73147=DIRECTION('center_axis',(0.939692620785909,0.342020143325668,0.));
#73148=DIRECTION('ref_axis',(-0.342020143325668,0.939692620785909,0.));
#73149=DIRECTION('',(-0.342020143325668,0.939692620785909,0.));
#73150=DIRECTION('',(-0.342020143325668,0.939692620785909,0.));
#73151=DIRECTION('',(0.,0.,1.));
#73152=DIRECTION('center_axis',(0.,1.,0.));
#73153=DIRECTION('ref_axis',(-1.,0.,0.));
#73154=DIRECTION('',(-1.,0.,0.));
#73155=DIRECTION('',(-1.,0.,0.));
#73156=DIRECTION('',(0.,0.,1.));
#73157=DIRECTION('center_axis',(-0.939692620785919,0.342020143325641,0.));
#73158=DIRECTION('ref_axis',(-0.342020143325641,-0.939692620785918,0.));
#73159=DIRECTION('',(-0.342020143325641,-0.939692620785918,0.));
#73160=DIRECTION('',(-0.342020143325641,-0.939692620785918,0.));
#73161=DIRECTION('',(0.,0.,1.));
#73162=DIRECTION('center_axis',(0.,1.,0.));
#73163=DIRECTION('ref_axis',(-1.,0.,0.));
#73164=DIRECTION('',(-1.,0.,0.));
#73165=DIRECTION('',(-1.,0.,0.));
#73166=DIRECTION('',(0.,0.,1.));
#73167=DIRECTION('center_axis',(0.939692620785919,0.342020143325641,0.));
#73168=DIRECTION('ref_axis',(-0.342020143325641,0.939692620785918,0.));
#73169=DIRECTION('',(-0.342020143325641,0.939692620785918,0.));
#73170=DIRECTION('',(-0.342020143325641,0.939692620785918,0.));
#73171=DIRECTION('',(0.,0.,1.));
#73172=DIRECTION('center_axis',(0.,1.,0.));
#73173=DIRECTION('ref_axis',(-1.,0.,0.));
#73174=DIRECTION('',(-1.,0.,0.));
#73175=DIRECTION('',(-1.,0.,0.));
#73176=DIRECTION('',(0.,0.,1.));
#73177=DIRECTION('center_axis',(-0.939692620785909,0.342020143325668,0.));
#73178=DIRECTION('ref_axis',(-0.342020143325668,-0.939692620785909,0.));
#73179=DIRECTION('',(-0.342020143325668,-0.939692620785909,0.));
#73180=DIRECTION('',(-0.342020143325668,-0.939692620785909,0.));
#73181=DIRECTION('',(0.,0.,1.));
#73182=DIRECTION('center_axis',(0.,1.,0.));
#73183=DIRECTION('ref_axis',(-1.,0.,0.));
#73184=DIRECTION('',(-1.,0.,0.));
#73185=DIRECTION('',(-1.,0.,0.));
#73186=DIRECTION('',(0.,0.,1.));
#73187=DIRECTION('center_axis',(0.939692620785909,0.342020143325668,0.));
#73188=DIRECTION('ref_axis',(-0.342020143325668,0.939692620785909,0.));
#73189=DIRECTION('',(-0.342020143325668,0.939692620785909,0.));
#73190=DIRECTION('',(-0.342020143325668,0.939692620785909,0.));
#73191=DIRECTION('',(0.,0.,1.));
#73192=DIRECTION('center_axis',(0.,1.,0.));
#73193=DIRECTION('ref_axis',(-1.,0.,0.));
#73194=DIRECTION('',(-1.,0.,0.));
#73195=DIRECTION('',(-1.,0.,0.));
#73196=DIRECTION('',(0.,0.,1.));
#73197=DIRECTION('center_axis',(-0.939692620785919,0.342020143325641,0.));
#73198=DIRECTION('ref_axis',(-0.342020143325641,-0.939692620785918,0.));
#73199=DIRECTION('',(-0.342020143325641,-0.939692620785918,0.));
#73200=DIRECTION('',(-0.342020143325641,-0.939692620785918,0.));
#73201=DIRECTION('',(0.,0.,1.));
#73202=DIRECTION('center_axis',(0.,1.,0.));
#73203=DIRECTION('ref_axis',(-1.,0.,0.));
#73204=DIRECTION('',(-1.,0.,0.));
#73205=DIRECTION('',(-1.,0.,0.));
#73206=DIRECTION('',(0.,0.,1.));
#73207=DIRECTION('center_axis',(0.939692620785909,0.342020143325668,0.));
#73208=DIRECTION('ref_axis',(-0.342020143325668,0.939692620785909,0.));
#73209=DIRECTION('',(-0.342020143325668,0.939692620785909,0.));
#73210=DIRECTION('',(-0.342020143325668,0.939692620785909,0.));
#73211=DIRECTION('',(0.,0.,1.));
#73212=DIRECTION('center_axis',(0.,1.,0.));
#73213=DIRECTION('ref_axis',(-1.,0.,0.));
#73214=DIRECTION('',(-1.,0.,0.));
#73215=DIRECTION('',(-1.,0.,0.));
#73216=DIRECTION('',(0.,0.,1.));
#73217=DIRECTION('center_axis',(-0.939692620785909,0.342020143325668,0.));
#73218=DIRECTION('ref_axis',(-0.342020143325668,-0.939692620785909,0.));
#73219=DIRECTION('',(-0.342020143325668,-0.939692620785909,0.));
#73220=DIRECTION('',(-0.342020143325668,-0.939692620785909,0.));
#73221=DIRECTION('',(0.,0.,1.));
#73222=DIRECTION('center_axis',(0.,1.,0.));
#73223=DIRECTION('ref_axis',(-1.,0.,0.));
#73224=DIRECTION('',(-1.,0.,0.));
#73225=DIRECTION('',(-1.,0.,0.));
#73226=DIRECTION('',(0.,0.,1.));
#73227=DIRECTION('center_axis',(0.939692620785909,0.342020143325668,0.));
#73228=DIRECTION('ref_axis',(-0.342020143325668,0.939692620785909,0.));
#73229=DIRECTION('',(-0.342020143325668,0.939692620785909,0.));
#73230=DIRECTION('',(-0.342020143325668,0.939692620785909,0.));
#73231=DIRECTION('',(0.,0.,1.));
#73232=DIRECTION('center_axis',(0.,1.,0.));
#73233=DIRECTION('ref_axis',(-1.,0.,0.));
#73234=DIRECTION('',(-1.,0.,0.));
#73235=DIRECTION('',(-1.,0.,0.));
#73236=DIRECTION('',(0.,0.,1.));
#73237=DIRECTION('center_axis',(-0.939692620785919,0.342020143325641,0.));
#73238=DIRECTION('ref_axis',(-0.342020143325641,-0.939692620785918,0.));
#73239=DIRECTION('',(-0.342020143325641,-0.939692620785918,0.));
#73240=DIRECTION('',(-0.342020143325641,-0.939692620785918,0.));
#73241=DIRECTION('',(0.,0.,1.));
#73242=DIRECTION('center_axis',(0.,1.,0.));
#73243=DIRECTION('ref_axis',(-1.,0.,0.));
#73244=DIRECTION('',(-1.,0.,0.));
#73245=DIRECTION('',(-1.,0.,0.));
#73246=DIRECTION('',(0.,0.,1.));
#73247=DIRECTION('center_axis',(0.939692620785909,0.342020143325668,0.));
#73248=DIRECTION('ref_axis',(-0.342020143325668,0.939692620785909,0.));
#73249=DIRECTION('',(-0.342020143325668,0.939692620785909,0.));
#73250=DIRECTION('',(-0.342020143325668,0.939692620785909,0.));
#73251=DIRECTION('',(0.,0.,1.));
#73252=DIRECTION('center_axis',(0.,1.,0.));
#73253=DIRECTION('ref_axis',(-1.,0.,0.));
#73254=DIRECTION('',(-1.,0.,0.));
#73255=DIRECTION('',(-1.,0.,0.));
#73256=DIRECTION('',(0.,0.,1.));
#73257=DIRECTION('center_axis',(-0.939692620785909,0.342020143325668,0.));
#73258=DIRECTION('ref_axis',(-0.342020143325668,-0.939692620785909,0.));
#73259=DIRECTION('',(-0.342020143325668,-0.939692620785909,0.));
#73260=DIRECTION('',(-0.342020143325668,-0.939692620785909,0.));
#73261=DIRECTION('',(0.,0.,1.));
#73262=DIRECTION('center_axis',(0.,1.,0.));
#73263=DIRECTION('ref_axis',(-1.,0.,0.));
#73264=DIRECTION('',(-1.,0.,0.));
#73265=DIRECTION('',(-1.,0.,0.));
#73266=DIRECTION('',(0.,0.,1.));
#73267=DIRECTION('center_axis',(0.939692620785919,0.342020143325641,0.));
#73268=DIRECTION('ref_axis',(-0.342020143325641,0.939692620785918,0.));
#73269=DIRECTION('',(-0.342020143325641,0.939692620785918,0.));
#73270=DIRECTION('',(-0.342020143325641,0.939692620785918,0.));
#73271=DIRECTION('',(0.,0.,1.));
#73272=DIRECTION('center_axis',(0.,1.,0.));
#73273=DIRECTION('ref_axis',(-1.,0.,0.));
#73274=DIRECTION('',(-1.,0.,0.));
#73275=DIRECTION('',(-1.,0.,0.));
#73276=DIRECTION('',(0.,0.,1.));
#73277=DIRECTION('center_axis',(-0.939692620785909,0.342020143325668,0.));
#73278=DIRECTION('ref_axis',(-0.342020143325668,-0.939692620785909,0.));
#73279=DIRECTION('',(-0.342020143325668,-0.939692620785909,0.));
#73280=DIRECTION('',(-0.342020143325668,-0.939692620785909,0.));
#73281=DIRECTION('',(0.,0.,1.));
#73282=DIRECTION('center_axis',(0.,1.,0.));
#73283=DIRECTION('ref_axis',(-1.,0.,0.));
#73284=DIRECTION('',(-1.,0.,0.));
#73285=DIRECTION('',(-1.,0.,0.));
#73286=DIRECTION('',(0.,0.,1.));
#73287=DIRECTION('center_axis',(0.939692620785909,0.342020143325668,0.));
#73288=DIRECTION('ref_axis',(-0.342020143325668,0.939692620785909,0.));
#73289=DIRECTION('',(-0.342020143325668,0.939692620785909,0.));
#73290=DIRECTION('',(-0.342020143325668,0.939692620785909,0.));
#73291=DIRECTION('',(0.,0.,1.));
#73292=DIRECTION('center_axis',(0.,1.,0.));
#73293=DIRECTION('ref_axis',(-1.,0.,0.));
#73294=DIRECTION('',(-1.,0.,0.));
#73295=DIRECTION('',(-1.,0.,0.));
#73296=DIRECTION('',(0.,0.,1.));
#73297=DIRECTION('center_axis',(-0.939692620785919,0.342020143325641,0.));
#73298=DIRECTION('ref_axis',(-0.342020143325641,-0.939692620785918,0.));
#73299=DIRECTION('',(-0.342020143325641,-0.939692620785918,0.));
#73300=DIRECTION('',(-0.342020143325641,-0.939692620785918,0.));
#73301=DIRECTION('',(0.,0.,1.));
#73302=DIRECTION('center_axis',(0.,1.,0.));
#73303=DIRECTION('ref_axis',(-1.,0.,0.));
#73304=DIRECTION('',(-1.,0.,0.));
#73305=DIRECTION('',(-1.,0.,0.));
#73306=DIRECTION('',(0.,0.,1.));
#73307=DIRECTION('center_axis',(0.939692620785919,0.342020143325641,0.));
#73308=DIRECTION('ref_axis',(-0.342020143325641,0.939692620785918,0.));
#73309=DIRECTION('',(-0.342020143325641,0.939692620785918,0.));
#73310=DIRECTION('',(-0.342020143325641,0.939692620785918,0.));
#73311=DIRECTION('',(0.,0.,1.));
#73312=DIRECTION('center_axis',(0.,1.,0.));
#73313=DIRECTION('ref_axis',(-1.,0.,0.));
#73314=DIRECTION('',(-1.,0.,0.));
#73315=DIRECTION('',(-1.,0.,0.));
#73316=DIRECTION('',(0.,0.,1.));
#73317=DIRECTION('center_axis',(-0.939692620785909,0.342020143325668,0.));
#73318=DIRECTION('ref_axis',(-0.342020143325668,-0.939692620785909,0.));
#73319=DIRECTION('',(-0.342020143325668,-0.939692620785909,0.));
#73320=DIRECTION('',(-0.342020143325668,-0.939692620785909,0.));
#73321=DIRECTION('',(0.,0.,1.));
#73322=DIRECTION('center_axis',(0.,1.,0.));
#73323=DIRECTION('ref_axis',(-1.,0.,0.));
#73324=DIRECTION('',(-1.,0.,0.));
#73325=DIRECTION('',(-1.,0.,0.));
#73326=DIRECTION('',(0.,0.,1.));
#73327=DIRECTION('center_axis',(0.939692620785909,0.342020143325668,0.));
#73328=DIRECTION('ref_axis',(-0.342020143325668,0.939692620785909,0.));
#73329=DIRECTION('',(-0.342020143325668,0.939692620785909,0.));
#73330=DIRECTION('',(-0.342020143325668,0.939692620785909,0.));
#73331=DIRECTION('',(0.,0.,1.));
#73332=DIRECTION('center_axis',(0.,1.,0.));
#73333=DIRECTION('ref_axis',(-1.,0.,0.));
#73334=DIRECTION('',(-1.,0.,0.));
#73335=DIRECTION('',(-1.,0.,0.));
#73336=DIRECTION('',(0.,0.,1.));
#73337=DIRECTION('center_axis',(-0.939692620785919,0.342020143325641,0.));
#73338=DIRECTION('ref_axis',(-0.342020143325641,-0.939692620785918,0.));
#73339=DIRECTION('',(-0.342020143325641,-0.939692620785918,0.));
#73340=DIRECTION('',(-0.342020143325641,-0.939692620785918,0.));
#73341=DIRECTION('',(0.,0.,1.));
#73342=DIRECTION('center_axis',(0.,1.,0.));
#73343=DIRECTION('ref_axis',(-1.,0.,0.));
#73344=DIRECTION('',(-1.,0.,0.));
#73345=DIRECTION('',(-1.,0.,0.));
#73346=DIRECTION('',(0.,0.,1.));
#73347=DIRECTION('center_axis',(0.939692620785909,0.342020143325668,0.));
#73348=DIRECTION('ref_axis',(-0.342020143325668,0.939692620785909,0.));
#73349=DIRECTION('',(-0.342020143325668,0.939692620785909,0.));
#73350=DIRECTION('',(-0.342020143325668,0.939692620785909,0.));
#73351=DIRECTION('',(0.,0.,1.));
#73352=DIRECTION('center_axis',(0.,1.,0.));
#73353=DIRECTION('ref_axis',(-1.,0.,0.));
#73354=DIRECTION('',(-1.,0.,0.));
#73355=DIRECTION('',(-1.,0.,0.));
#73356=DIRECTION('',(0.,0.,1.));
#73357=DIRECTION('center_axis',(-0.939692620785909,0.342020143325668,0.));
#73358=DIRECTION('ref_axis',(-0.342020143325668,-0.939692620785909,0.));
#73359=DIRECTION('',(-0.342020143325668,-0.939692620785909,0.));
#73360=DIRECTION('',(-0.342020143325668,-0.939692620785909,0.));
#73361=DIRECTION('',(0.,0.,1.));
#73362=DIRECTION('center_axis',(0.,1.,0.));
#73363=DIRECTION('ref_axis',(-1.,0.,0.));
#73364=DIRECTION('',(-1.,0.,0.));
#73365=DIRECTION('',(-1.,0.,0.));
#73366=DIRECTION('',(0.,0.,1.));
#73367=DIRECTION('center_axis',(0.939692620785909,0.342020143325668,0.));
#73368=DIRECTION('ref_axis',(-0.342020143325668,0.939692620785909,0.));
#73369=DIRECTION('',(-0.342020143325668,0.939692620785909,0.));
#73370=DIRECTION('',(-0.342020143325668,0.939692620785909,0.));
#73371=DIRECTION('',(0.,0.,1.));
#73372=DIRECTION('center_axis',(0.,1.,0.));
#73373=DIRECTION('ref_axis',(-1.,0.,0.));
#73374=DIRECTION('',(-1.,0.,0.));
#73375=DIRECTION('',(-1.,0.,0.));
#73376=DIRECTION('',(0.,0.,1.));
#73377=DIRECTION('center_axis',(-0.939692620785919,0.342020143325641,0.));
#73378=DIRECTION('ref_axis',(-0.342020143325641,-0.939692620785918,0.));
#73379=DIRECTION('',(-0.342020143325641,-0.939692620785918,0.));
#73380=DIRECTION('',(-0.342020143325641,-0.939692620785918,0.));
#73381=DIRECTION('',(0.,0.,1.));
#73382=DIRECTION('center_axis',(0.,1.,0.));
#73383=DIRECTION('ref_axis',(-1.,0.,0.));
#73384=DIRECTION('',(-1.,0.,0.));
#73385=DIRECTION('',(-1.,0.,0.));
#73386=DIRECTION('',(0.,0.,1.));
#73387=DIRECTION('center_axis',(0.939692620785909,0.342020143325668,0.));
#73388=DIRECTION('ref_axis',(-0.342020143325668,0.939692620785909,0.));
#73389=DIRECTION('',(-0.342020143325668,0.939692620785909,0.));
#73390=DIRECTION('',(-0.342020143325668,0.939692620785909,0.));
#73391=DIRECTION('',(0.,0.,1.));
#73392=DIRECTION('center_axis',(0.,1.,0.));
#73393=DIRECTION('ref_axis',(-1.,0.,0.));
#73394=DIRECTION('',(-1.,0.,0.));
#73395=DIRECTION('',(-1.,0.,0.));
#73396=DIRECTION('',(0.,0.,1.));
#73397=DIRECTION('center_axis',(-0.939692620785909,0.342020143325668,0.));
#73398=DIRECTION('ref_axis',(-0.342020143325668,-0.939692620785909,0.));
#73399=DIRECTION('',(-0.342020143325668,-0.939692620785909,0.));
#73400=DIRECTION('',(-0.342020143325668,-0.939692620785909,0.));
#73401=DIRECTION('',(0.,0.,1.));
#73402=DIRECTION('center_axis',(0.,1.,0.));
#73403=DIRECTION('ref_axis',(-1.,0.,0.));
#73404=DIRECTION('',(-1.,0.,0.));
#73405=DIRECTION('',(-1.,0.,0.));
#73406=DIRECTION('',(0.,0.,1.));
#73407=DIRECTION('center_axis',(0.939692620785919,0.342020143325641,0.));
#73408=DIRECTION('ref_axis',(-0.342020143325641,0.939692620785918,0.));
#73409=DIRECTION('',(-0.342020143325641,0.939692620785918,0.));
#73410=DIRECTION('',(-0.342020143325641,0.939692620785918,0.));
#73411=DIRECTION('',(0.,0.,1.));
#73412=DIRECTION('center_axis',(0.,1.,0.));
#73413=DIRECTION('ref_axis',(-1.,0.,0.));
#73414=DIRECTION('',(-1.,0.,0.));
#73415=DIRECTION('',(-1.,0.,0.));
#73416=DIRECTION('',(0.,0.,1.));
#73417=DIRECTION('center_axis',(-0.939692620785909,0.342020143325668,0.));
#73418=DIRECTION('ref_axis',(-0.342020143325668,-0.939692620785909,0.));
#73419=DIRECTION('',(-0.342020143325668,-0.939692620785909,0.));
#73420=DIRECTION('',(-0.342020143325668,-0.939692620785909,0.));
#73421=DIRECTION('',(0.,0.,1.));
#73422=DIRECTION('center_axis',(0.,1.,0.));
#73423=DIRECTION('ref_axis',(-1.,0.,0.));
#73424=DIRECTION('',(-1.,0.,0.));
#73425=DIRECTION('',(-1.,0.,0.));
#73426=DIRECTION('',(0.,0.,1.));
#73427=DIRECTION('center_axis',(0.939692620785909,0.342020143325668,0.));
#73428=DIRECTION('ref_axis',(-0.342020143325668,0.939692620785909,0.));
#73429=DIRECTION('',(-0.342020143325668,0.939692620785909,0.));
#73430=DIRECTION('',(-0.342020143325668,0.939692620785909,0.));
#73431=DIRECTION('',(0.,0.,1.));
#73432=DIRECTION('center_axis',(0.,1.,0.));
#73433=DIRECTION('ref_axis',(-1.,0.,0.));
#73434=DIRECTION('',(-1.,0.,0.));
#73435=DIRECTION('',(-1.,0.,0.));
#73436=DIRECTION('',(0.,0.,1.));
#73437=DIRECTION('center_axis',(-0.939692620785909,0.342020143325668,0.));
#73438=DIRECTION('ref_axis',(-0.342020143325668,-0.939692620785909,0.));
#73439=DIRECTION('',(-0.342020143325668,-0.939692620785909,0.));
#73440=DIRECTION('',(-0.342020143325668,-0.939692620785909,0.));
#73441=DIRECTION('',(0.,0.,1.));
#73442=DIRECTION('center_axis',(0.,1.,0.));
#73443=DIRECTION('ref_axis',(-1.,0.,0.));
#73444=DIRECTION('',(-1.,0.,0.));
#73445=DIRECTION('',(-1.,0.,0.));
#73446=DIRECTION('',(0.,0.,1.));
#73447=DIRECTION('center_axis',(0.939692620785919,0.342020143325641,0.));
#73448=DIRECTION('ref_axis',(-0.342020143325641,0.939692620785918,0.));
#73449=DIRECTION('',(-0.342020143325641,0.939692620785918,0.));
#73450=DIRECTION('',(-0.342020143325641,0.939692620785918,0.));
#73451=DIRECTION('',(0.,0.,1.));
#73452=DIRECTION('center_axis',(0.,1.,0.));
#73453=DIRECTION('ref_axis',(-1.,0.,0.));
#73454=DIRECTION('',(-1.,0.,0.));
#73455=DIRECTION('',(-1.,0.,0.));
#73456=DIRECTION('',(0.,0.,1.));
#73457=DIRECTION('center_axis',(-0.939692620785909,0.342020143325668,0.));
#73458=DIRECTION('ref_axis',(-0.342020143325668,-0.939692620785909,0.));
#73459=DIRECTION('',(-0.342020143325668,-0.939692620785909,0.));
#73460=DIRECTION('',(-0.342020143325668,-0.939692620785909,0.));
#73461=DIRECTION('',(0.,0.,1.));
#73462=DIRECTION('center_axis',(0.,1.,0.));
#73463=DIRECTION('ref_axis',(-1.,0.,0.));
#73464=DIRECTION('',(-1.,0.,0.));
#73465=DIRECTION('',(-1.,0.,0.));
#73466=DIRECTION('',(0.,0.,1.));
#73467=DIRECTION('center_axis',(0.939692620785909,0.342020143325668,0.));
#73468=DIRECTION('ref_axis',(-0.342020143325668,0.939692620785909,0.));
#73469=DIRECTION('',(-0.342020143325668,0.939692620785909,0.));
#73470=DIRECTION('',(-0.342020143325668,0.939692620785909,0.));
#73471=DIRECTION('',(0.,0.,1.));
#73472=DIRECTION('center_axis',(0.,1.,0.));
#73473=DIRECTION('ref_axis',(-1.,0.,0.));
#73474=DIRECTION('',(-1.,0.,0.));
#73475=DIRECTION('',(-1.,0.,0.));
#73476=DIRECTION('',(0.,0.,1.));
#73477=DIRECTION('center_axis',(-0.939692620785919,0.342020143325641,0.));
#73478=DIRECTION('ref_axis',(-0.342020143325641,-0.939692620785918,0.));
#73479=DIRECTION('',(-0.342020143325641,-0.939692620785918,0.));
#73480=DIRECTION('',(-0.342020143325641,-0.939692620785918,0.));
#73481=DIRECTION('',(0.,0.,1.));
#73482=DIRECTION('center_axis',(0.,1.,0.));
#73483=DIRECTION('ref_axis',(-1.,0.,0.));
#73484=DIRECTION('',(-1.,0.,0.));
#73485=DIRECTION('',(-1.,0.,0.));
#73486=DIRECTION('',(0.,0.,1.));
#73487=DIRECTION('center_axis',(0.939692620785919,0.342020143325641,0.));
#73488=DIRECTION('ref_axis',(-0.342020143325641,0.939692620785918,0.));
#73489=DIRECTION('',(-0.342020143325641,0.939692620785918,0.));
#73490=DIRECTION('',(-0.342020143325641,0.939692620785918,0.));
#73491=DIRECTION('',(0.,0.,1.));
#73492=DIRECTION('center_axis',(0.,1.,0.));
#73493=DIRECTION('ref_axis',(-1.,0.,0.));
#73494=DIRECTION('',(-1.,0.,0.));
#73495=DIRECTION('',(-1.,0.,0.));
#73496=DIRECTION('',(0.,0.,1.));
#73497=DIRECTION('center_axis',(-0.939692620785909,0.342020143325668,0.));
#73498=DIRECTION('ref_axis',(-0.342020143325668,-0.939692620785909,0.));
#73499=DIRECTION('',(-0.342020143325668,-0.939692620785909,0.));
#73500=DIRECTION('',(-0.342020143325668,-0.939692620785909,0.));
#73501=DIRECTION('',(0.,0.,1.));
#73502=DIRECTION('center_axis',(0.,1.,0.));
#73503=DIRECTION('ref_axis',(-1.,0.,0.));
#73504=DIRECTION('',(-1.,0.,0.));
#73505=DIRECTION('',(-1.,0.,0.));
#73506=DIRECTION('',(0.,0.,1.));
#73507=DIRECTION('center_axis',(0.939692620785909,0.342020143325668,0.));
#73508=DIRECTION('ref_axis',(-0.342020143325668,0.939692620785909,0.));
#73509=DIRECTION('',(-0.342020143325668,0.939692620785909,0.));
#73510=DIRECTION('',(-0.342020143325668,0.939692620785909,0.));
#73511=DIRECTION('',(0.,0.,1.));
#73512=DIRECTION('center_axis',(0.,1.,0.));
#73513=DIRECTION('ref_axis',(-1.,0.,0.));
#73514=DIRECTION('',(-1.,0.,0.));
#73515=DIRECTION('',(-1.,0.,0.));
#73516=DIRECTION('',(0.,0.,1.));
#73517=DIRECTION('center_axis',(-0.939692620785919,0.342020143325641,0.));
#73518=DIRECTION('ref_axis',(-0.342020143325641,-0.939692620785918,0.));
#73519=DIRECTION('',(-0.342020143325641,-0.939692620785918,0.));
#73520=DIRECTION('',(-0.342020143325641,-0.939692620785918,0.));
#73521=DIRECTION('',(0.,0.,1.));
#73522=DIRECTION('center_axis',(0.,1.,0.));
#73523=DIRECTION('ref_axis',(-1.,0.,0.));
#73524=DIRECTION('',(-1.,0.,0.));
#73525=DIRECTION('',(-1.,0.,0.));
#73526=DIRECTION('',(0.,0.,1.));
#73527=DIRECTION('center_axis',(0.939692620785909,0.342020143325668,0.));
#73528=DIRECTION('ref_axis',(-0.342020143325668,0.939692620785909,0.));
#73529=DIRECTION('',(-0.342020143325668,0.939692620785909,0.));
#73530=DIRECTION('',(-0.342020143325668,0.939692620785909,0.));
#73531=DIRECTION('',(0.,0.,1.));
#73532=DIRECTION('center_axis',(0.,1.,0.));
#73533=DIRECTION('ref_axis',(-1.,0.,0.));
#73534=DIRECTION('',(-1.,0.,0.));
#73535=DIRECTION('',(-1.,0.,0.));
#73536=DIRECTION('',(0.,0.,1.));
#73537=DIRECTION('center_axis',(-0.939692620785909,0.342020143325668,0.));
#73538=DIRECTION('ref_axis',(-0.342020143325668,-0.939692620785909,0.));
#73539=DIRECTION('',(-0.342020143325668,-0.939692620785909,0.));
#73540=DIRECTION('',(-0.342020143325668,-0.939692620785909,0.));
#73541=DIRECTION('',(0.,0.,1.));
#73542=DIRECTION('center_axis',(0.,1.,0.));
#73543=DIRECTION('ref_axis',(-1.,0.,0.));
#73544=DIRECTION('',(-1.,0.,0.));
#73545=DIRECTION('',(-1.,0.,0.));
#73546=DIRECTION('',(0.,0.,1.));
#73547=DIRECTION('center_axis',(0.939692620785919,0.342020143325641,0.));
#73548=DIRECTION('ref_axis',(-0.342020143325641,0.939692620785918,0.));
#73549=DIRECTION('',(-0.342020143325641,0.939692620785918,0.));
#73550=DIRECTION('',(-0.342020143325641,0.939692620785918,0.));
#73551=DIRECTION('',(0.,0.,1.));
#73552=DIRECTION('center_axis',(0.,1.,0.));
#73553=DIRECTION('ref_axis',(-1.,0.,0.));
#73554=DIRECTION('',(-1.,0.,0.));
#73555=DIRECTION('',(-1.,0.,0.));
#73556=DIRECTION('',(0.,0.,1.));
#73557=DIRECTION('center_axis',(-0.939692620785909,0.342020143325668,0.));
#73558=DIRECTION('ref_axis',(-0.342020143325668,-0.939692620785909,0.));
#73559=DIRECTION('',(-0.342020143325668,-0.939692620785909,0.));
#73560=DIRECTION('',(-0.342020143325668,-0.939692620785909,0.));
#73561=DIRECTION('',(0.,0.,1.));
#73562=DIRECTION('center_axis',(0.,1.,0.));
#73563=DIRECTION('ref_axis',(-1.,0.,0.));
#73564=DIRECTION('',(-1.,0.,0.));
#73565=DIRECTION('',(-1.,0.,0.));
#73566=DIRECTION('',(0.,0.,1.));
#73567=DIRECTION('center_axis',(0.939692620785909,0.342020143325668,0.));
#73568=DIRECTION('ref_axis',(-0.342020143325668,0.939692620785909,0.));
#73569=DIRECTION('',(-0.342020143325668,0.939692620785909,0.));
#73570=DIRECTION('',(-0.342020143325668,0.939692620785909,0.));
#73571=DIRECTION('',(0.,0.,1.));
#73572=DIRECTION('center_axis',(0.,1.,0.));
#73573=DIRECTION('ref_axis',(-1.,0.,0.));
#73574=DIRECTION('',(-1.,0.,0.));
#73575=DIRECTION('',(-1.,0.,0.));
#73576=DIRECTION('',(0.,0.,1.));
#73577=DIRECTION('center_axis',(-0.939692620785919,0.342020143325641,0.));
#73578=DIRECTION('ref_axis',(-0.342020143325641,-0.939692620785918,0.));
#73579=DIRECTION('',(-0.342020143325641,-0.939692620785918,0.));
#73580=DIRECTION('',(-0.342020143325641,-0.939692620785918,0.));
#73581=DIRECTION('',(0.,0.,1.));
#73582=DIRECTION('center_axis',(0.,1.,0.));
#73583=DIRECTION('ref_axis',(-1.,0.,0.));
#73584=DIRECTION('',(-1.,0.,0.));
#73585=DIRECTION('',(-1.,0.,0.));
#73586=DIRECTION('',(0.,0.,1.));
#73587=DIRECTION('center_axis',(0.939692620785919,0.342020143325641,0.));
#73588=DIRECTION('ref_axis',(-0.342020143325641,0.939692620785918,0.));
#73589=DIRECTION('',(-0.342020143325641,0.939692620785918,0.));
#73590=DIRECTION('',(-0.342020143325641,0.939692620785918,0.));
#73591=DIRECTION('',(0.,0.,1.));
#73592=DIRECTION('center_axis',(0.,1.,0.));
#73593=DIRECTION('ref_axis',(-1.,0.,0.));
#73594=DIRECTION('',(-1.,0.,0.));
#73595=DIRECTION('',(-1.,0.,0.));
#73596=DIRECTION('',(0.,0.,1.));
#73597=DIRECTION('center_axis',(-0.939692620785909,0.342020143325668,0.));
#73598=DIRECTION('ref_axis',(-0.342020143325668,-0.939692620785909,0.));
#73599=DIRECTION('',(-0.342020143325668,-0.939692620785909,0.));
#73600=DIRECTION('',(-0.342020143325668,-0.939692620785909,0.));
#73601=DIRECTION('',(0.,0.,1.));
#73602=DIRECTION('center_axis',(0.,1.,0.));
#73603=DIRECTION('ref_axis',(-1.,0.,0.));
#73604=DIRECTION('',(-1.,0.,0.));
#73605=DIRECTION('',(-1.,0.,0.));
#73606=DIRECTION('',(0.,0.,1.));
#73607=DIRECTION('center_axis',(0.939692620785909,0.342020143325668,0.));
#73608=DIRECTION('ref_axis',(-0.342020143325668,0.939692620785909,0.));
#73609=DIRECTION('',(-0.342020143325668,0.939692620785909,0.));
#73610=DIRECTION('',(-0.342020143325668,0.939692620785909,0.));
#73611=DIRECTION('',(0.,0.,1.));
#73612=DIRECTION('center_axis',(0.,1.,0.));
#73613=DIRECTION('ref_axis',(-1.,0.,0.));
#73614=DIRECTION('',(-1.,0.,0.));
#73615=DIRECTION('',(-1.,0.,0.));
#73616=DIRECTION('',(0.,0.,1.));
#73617=DIRECTION('center_axis',(-0.939692620785919,0.342020143325641,0.));
#73618=DIRECTION('ref_axis',(-0.342020143325641,-0.939692620785918,0.));
#73619=DIRECTION('',(-0.342020143325641,-0.939692620785918,0.));
#73620=DIRECTION('',(-0.342020143325641,-0.939692620785918,0.));
#73621=DIRECTION('',(0.,0.,1.));
#73622=DIRECTION('center_axis',(0.,1.,0.));
#73623=DIRECTION('ref_axis',(-1.,0.,0.));
#73624=DIRECTION('',(-1.,0.,0.));
#73625=DIRECTION('',(-1.,0.,0.));
#73626=DIRECTION('',(0.,0.,1.));
#73627=DIRECTION('center_axis',(0.939692620785919,0.342020143325641,0.));
#73628=DIRECTION('ref_axis',(-0.342020143325641,0.939692620785918,0.));
#73629=DIRECTION('',(-0.342020143325641,0.939692620785918,0.));
#73630=DIRECTION('',(-0.342020143325641,0.939692620785918,0.));
#73631=DIRECTION('',(0.,0.,1.));
#73632=DIRECTION('center_axis',(0.,1.,0.));
#73633=DIRECTION('ref_axis',(-1.,0.,0.));
#73634=DIRECTION('',(-1.,0.,0.));
#73635=DIRECTION('',(-1.,0.,0.));
#73636=DIRECTION('',(0.,0.,1.));
#73637=DIRECTION('center_axis',(-0.939692620785909,0.342020143325668,0.));
#73638=DIRECTION('ref_axis',(-0.342020143325668,-0.939692620785909,0.));
#73639=DIRECTION('',(-0.342020143325668,-0.939692620785909,0.));
#73640=DIRECTION('',(-0.342020143325668,-0.939692620785909,0.));
#73641=DIRECTION('',(0.,0.,1.));
#73642=DIRECTION('center_axis',(0.,1.,0.));
#73643=DIRECTION('ref_axis',(-1.,0.,0.));
#73644=DIRECTION('',(-1.,0.,0.));
#73645=DIRECTION('',(-1.,0.,0.));
#73646=DIRECTION('',(0.,0.,1.));
#73647=DIRECTION('center_axis',(0.939692620785909,0.342020143325668,0.));
#73648=DIRECTION('ref_axis',(-0.342020143325668,0.939692620785909,0.));
#73649=DIRECTION('',(-0.342020143325668,0.939692620785909,0.));
#73650=DIRECTION('',(-0.342020143325668,0.939692620785909,0.));
#73651=DIRECTION('',(0.,0.,1.));
#73652=DIRECTION('center_axis',(0.,1.,0.));
#73653=DIRECTION('ref_axis',(-1.,0.,0.));
#73654=DIRECTION('',(-1.,0.,0.));
#73655=DIRECTION('',(-1.,0.,0.));
#73656=DIRECTION('',(0.,0.,1.));
#73657=DIRECTION('center_axis',(-0.939692620785919,0.342020143325641,0.));
#73658=DIRECTION('ref_axis',(-0.342020143325641,-0.939692620785918,0.));
#73659=DIRECTION('',(-0.342020143325641,-0.939692620785918,0.));
#73660=DIRECTION('',(-0.342020143325641,-0.939692620785918,0.));
#73661=DIRECTION('',(0.,0.,1.));
#73662=DIRECTION('center_axis',(0.,1.,0.));
#73663=DIRECTION('ref_axis',(-1.,0.,0.));
#73664=DIRECTION('',(-1.,0.,0.));
#73665=DIRECTION('',(-1.,0.,0.));
#73666=DIRECTION('',(0.,0.,1.));
#73667=DIRECTION('center_axis',(0.939692620785919,0.342020143325641,0.));
#73668=DIRECTION('ref_axis',(-0.342020143325641,0.939692620785918,0.));
#73669=DIRECTION('',(-0.342020143325641,0.939692620785918,0.));
#73670=DIRECTION('',(-0.342020143325641,0.939692620785918,0.));
#73671=DIRECTION('',(0.,0.,1.));
#73672=DIRECTION('center_axis',(0.,1.,0.));
#73673=DIRECTION('ref_axis',(-1.,0.,0.));
#73674=DIRECTION('',(-1.,0.,0.));
#73675=DIRECTION('',(-1.,0.,0.));
#73676=DIRECTION('',(0.,0.,1.));
#73677=DIRECTION('center_axis',(-0.939692620785909,0.342020143325668,0.));
#73678=DIRECTION('ref_axis',(-0.342020143325668,-0.939692620785909,0.));
#73679=DIRECTION('',(-0.342020143325668,-0.939692620785909,0.));
#73680=DIRECTION('',(-0.342020143325668,-0.939692620785909,0.));
#73681=DIRECTION('center_axis',(-1.,0.,0.));
#73682=DIRECTION('ref_axis',(0.,-1.,0.));
#73683=DIRECTION('',(0.,-1.,0.));
#73684=DIRECTION('',(0.,-1.,0.));
#73685=DIRECTION('center_axis',(0.,0.,1.));
#73686=DIRECTION('ref_axis',(1.,0.,0.));
#73687=DIRECTION('center_axis',(0.,0.,1.));
#73688=DIRECTION('ref_axis',(1.,0.,0.));
#98945=CARTESIAN_POINT('',(0.,0.,0.));
#98946=CARTESIAN_POINT('Origin',(214.,14.3,28.5));
#98947=CARTESIAN_POINT('',(211.2,14.45,28.5));
#98948=CARTESIAN_POINT('Origin',(214.,14.45,28.5));
#98949=CARTESIAN_POINT('',(211.5,14.15,28.5));
#98950=CARTESIAN_POINT('',(211.35,14.3,28.5));
#98951=CARTESIAN_POINT('Origin',(214.,14.15,28.5));
#98952=CARTESIAN_POINT('Origin',(214.,14.45,28.5));
#98953=CARTESIAN_POINT('',(211.5,11.5,28.5));
#98954=CARTESIAN_POINT('',(211.5,14.45,28.5));
#98955=CARTESIAN_POINT('Origin',(214.,11.5,28.5));
#98956=CARTESIAN_POINT('Origin',(218.,14.45,25.5));
#98957=CARTESIAN_POINT('',(218.,14.45,25.5));
#98958=CARTESIAN_POINT('',(207.955857948402,14.45,25.5));
#98959=CARTESIAN_POINT('',(218.,14.45,25.5));
#98960=CARTESIAN_POINT('',(207.955857948402,14.45,31.5));
#98961=CARTESIAN_POINT('',(207.955857948402,14.45,25.5));
#98962=CARTESIAN_POINT('',(218.,14.45,31.5));
#98963=CARTESIAN_POINT('',(218.,14.45,31.5));
#98964=CARTESIAN_POINT('',(218.,14.45,25.5));
#98965=CARTESIAN_POINT('Origin',(6.,14.3,28.5));
#98966=CARTESIAN_POINT('',(3.2,14.45,28.5));
#98967=CARTESIAN_POINT('Origin',(6.,14.45,28.5));
#98968=CARTESIAN_POINT('',(3.5,14.15,28.5));
#98969=CARTESIAN_POINT('',(3.35,14.3,28.5));
#98970=CARTESIAN_POINT('Origin',(6.,14.15,28.5));
#98971=CARTESIAN_POINT('Origin',(6.,14.45,28.5));
#98972=CARTESIAN_POINT('',(3.5,11.5,28.5));
#98973=CARTESIAN_POINT('',(3.5,14.45,28.5));
#98974=CARTESIAN_POINT('Origin',(6.,11.5,28.5));
#98975=CARTESIAN_POINT('Origin',(12.0441420515979,14.45,25.5));
#98976=CARTESIAN_POINT('',(12.0441420515979,14.45,25.5));
#98977=CARTESIAN_POINT('',(2.,14.45,25.5));
#98978=CARTESIAN_POINT('',(12.0441420515979,14.45,25.5));
#98979=CARTESIAN_POINT('',(2.,14.45,31.5));
#98980=CARTESIAN_POINT('',(2.,14.45,25.5));
#98981=CARTESIAN_POINT('',(12.0441420515979,14.45,31.5));
#98982=CARTESIAN_POINT('',(12.0441420515979,14.45,31.5));
#98983=CARTESIAN_POINT('',(12.0441420515979,14.45,25.5));
#98984=CARTESIAN_POINT('Origin',(6.,11.5,28.5));
#98985=CARTESIAN_POINT('',(4.55,11.5,28.5));
#98986=CARTESIAN_POINT('Origin',(6.,11.5,28.5));
#98987=CARTESIAN_POINT('Origin',(214.,11.5,28.5));
#98988=CARTESIAN_POINT('',(212.55,11.5,28.5));
#98989=CARTESIAN_POINT('Origin',(214.,11.5,28.5));
#98990=CARTESIAN_POINT('Origin',(6.,14.45,28.5));
#98991=CARTESIAN_POINT('',(4.55,9.5,28.5));
#98992=CARTESIAN_POINT('',(4.55,14.45,28.5));
#98993=CARTESIAN_POINT('Origin',(6.,9.5,28.5));
#98994=CARTESIAN_POINT('Origin',(214.,14.45,28.5));
#98995=CARTESIAN_POINT('',(212.55,9.5,28.5));
#98996=CARTESIAN_POINT('',(212.55,14.45,28.5));
#98997=CARTESIAN_POINT('Origin',(214.,9.5,28.5));
#98998=CARTESIAN_POINT('Origin',(56.,9.65,31.35));
#98999=CARTESIAN_POINT('',(218.,9.5,31.2));
#99000=CARTESIAN_POINT('',(218.,9.8,31.5));
#99001=CARTESIAN_POINT('',(218.,8.15,29.85));
#99002=CARTESIAN_POINT('',(2.,9.8,31.5));
#99003=CARTESIAN_POINT('',(56.,9.8,31.5));
#99004=CARTESIAN_POINT('',(2.,9.5,31.2));
#99005=CARTESIAN_POINT('',(2.,9.38750000000001,31.0875));
#99006=CARTESIAN_POINT('',(56.,9.5,31.2));
#99007=CARTESIAN_POINT('Origin',(218.,9.5,25.5));
#99008=CARTESIAN_POINT('',(218.,9.5,25.8));
#99009=CARTESIAN_POINT('',(218.,9.5,25.5));
#99010=CARTESIAN_POINT('',(218.,9.8,25.5));
#99011=CARTESIAN_POINT('',(218.,9.65,25.65));
#99012=CARTESIAN_POINT('',(218.,9.5,25.5));
#99013=CARTESIAN_POINT('',(218.,9.5,31.5));
#99014=CARTESIAN_POINT('Origin',(2.,9.5,25.5));
#99015=CARTESIAN_POINT('',(2.,9.5,25.8));
#99016=CARTESIAN_POINT('',(2.,9.5,25.5));
#99017=CARTESIAN_POINT('',(56.,9.5,25.8));
#99018=CARTESIAN_POINT('Origin',(56.,9.65,25.65));
#99019=CARTESIAN_POINT('',(2.,9.8,25.5));
#99020=CARTESIAN_POINT('',(2.,10.8875,24.4125));
#99021=CARTESIAN_POINT('',(56.,9.8,25.5));
#99022=CARTESIAN_POINT('Origin',(12.4354100534341,13.375,25.5));
#99023=CARTESIAN_POINT('',(12.4354100534341,13.375,25.5));
#99024=CARTESIAN_POINT('',(12.4354100534341,13.375,25.5));
#99025=CARTESIAN_POINT('',(12.4354100534341,13.375,31.5));
#99026=CARTESIAN_POINT('',(12.4354100534341,13.375,31.5));
#99027=CARTESIAN_POINT('',(12.4354100534341,13.375,25.5));
#99028=CARTESIAN_POINT('Origin',(12.7858454239988,13.375,25.5));
#99029=CARTESIAN_POINT('',(12.7858454239988,13.375,25.5));
#99030=CARTESIAN_POINT('',(12.7858454239988,13.375,25.5));
#99031=CARTESIAN_POINT('',(12.7858454239988,13.375,31.5));
#99032=CARTESIAN_POINT('',(12.7858454239988,13.375,31.5));
#99033=CARTESIAN_POINT('',(12.7858454239988,13.375,25.5));
#99034=CARTESIAN_POINT('Origin',(13.1771134258349,14.45,25.5));
#99035=CARTESIAN_POINT('',(13.1771134258349,14.45,25.5));
#99036=CARTESIAN_POINT('',(13.1771134258349,14.45,25.5));
#99037=CARTESIAN_POINT('',(13.1771134258349,14.45,31.5));
#99038=CARTESIAN_POINT('',(13.1771134258349,14.45,31.5));
#99039=CARTESIAN_POINT('',(13.1771134258349,14.45,25.5));
#99040=CARTESIAN_POINT('Origin',(13.6149383783928,14.45,25.5));
#99041=CARTESIAN_POINT('',(13.6149383783928,14.45,25.5));
#99042=CARTESIAN_POINT('',(13.6149383783928,14.45,25.5));
#99043=CARTESIAN_POINT('',(13.6149383783928,14.45,31.5));
#99044=CARTESIAN_POINT('',(13.6149383783928,14.45,31.5));
#99045=CARTESIAN_POINT('',(13.6149383783928,14.45,25.5));
#99046=CARTESIAN_POINT('Origin',(14.006206380229,13.375,25.5));
#99047=CARTESIAN_POINT('',(14.006206380229,13.375,25.5));
#99048=CARTESIAN_POINT('',(14.006206380229,13.375,25.5));
#99049=CARTESIAN_POINT('',(14.006206380229,13.375,31.5));
#99050=CARTESIAN_POINT('',(14.006206380229,13.375,31.5));
#99051=CARTESIAN_POINT('',(14.006206380229,13.375,25.5));
#99052=CARTESIAN_POINT('Origin',(14.3566417507937,13.375,25.5));
#99053=CARTESIAN_POINT('',(14.3566417507937,13.375,25.5));
#99054=CARTESIAN_POINT('',(14.3566417507937,13.375,25.5));
#99055=CARTESIAN_POINT('',(14.3566417507937,13.375,31.5));
#99056=CARTESIAN_POINT('',(14.3566417507937,13.375,31.5));
#99057=CARTESIAN_POINT('',(14.3566417507937,13.375,25.5));
#99058=CARTESIAN_POINT('Origin',(14.7479097526298,14.45,25.5));
#99059=CARTESIAN_POINT('',(14.7479097526298,14.45,25.5));
#99060=CARTESIAN_POINT('',(14.7479097526298,14.45,25.5));
#99061=CARTESIAN_POINT('',(14.7479097526298,14.45,31.5));
#99062=CARTESIAN_POINT('',(14.7479097526298,14.45,31.5));
#99063=CARTESIAN_POINT('',(14.7479097526298,14.45,25.5));
#99064=CARTESIAN_POINT('Origin',(15.1857347051877,14.45,25.5));
#99065=CARTESIAN_POINT('',(15.1857347051877,14.45,25.5));
#99066=CARTESIAN_POINT('',(15.1857347051877,14.45,25.5));
#99067=CARTESIAN_POINT('',(15.1857347051877,14.45,31.5));
#99068=CARTESIAN_POINT('',(15.1857347051877,14.45,31.5));
#99069=CARTESIAN_POINT('',(15.1857347051877,14.45,25.5));
#99070=CARTESIAN_POINT('Origin',(15.5770027070239,13.375,25.5));
#99071=CARTESIAN_POINT('',(15.5770027070239,13.375,25.5));
#99072=CARTESIAN_POINT('',(15.5770027070239,13.375,25.5));
#99073=CARTESIAN_POINT('',(15.5770027070239,13.375,31.5));
#99074=CARTESIAN_POINT('',(15.5770027070239,13.375,31.5));
#99075=CARTESIAN_POINT('',(15.5770027070239,13.375,25.5));
#99076=CARTESIAN_POINT('Origin',(15.9274380775886,13.375,25.5));
#99077=CARTESIAN_POINT('',(15.9274380775886,13.375,25.5));
#99078=CARTESIAN_POINT('',(15.9274380775886,13.375,25.5));
#99079=CARTESIAN_POINT('',(15.9274380775886,13.375,31.5));
#99080=CARTESIAN_POINT('',(15.9274380775886,13.375,31.5));
#99081=CARTESIAN_POINT('',(15.9274380775886,13.375,25.5));
#99082=CARTESIAN_POINT('Origin',(16.3187060794247,14.45,25.5));
#99083=CARTESIAN_POINT('',(16.3187060794247,14.45,25.5));
#99084=CARTESIAN_POINT('',(16.3187060794247,14.45,25.5));
#99085=CARTESIAN_POINT('',(16.3187060794247,14.45,31.5));
#99086=CARTESIAN_POINT('',(16.3187060794247,14.45,31.5));
#99087=CARTESIAN_POINT('',(16.3187060794247,14.45,25.5));
#99088=CARTESIAN_POINT('Origin',(16.7565310319826,14.45,25.5));
#99089=CARTESIAN_POINT('',(16.7565310319826,14.45,25.5));
#99090=CARTESIAN_POINT('',(16.7565310319826,14.45,25.5));
#99091=CARTESIAN_POINT('',(16.7565310319826,14.45,31.5));
#99092=CARTESIAN_POINT('',(16.7565310319826,14.45,31.5));
#99093=CARTESIAN_POINT('',(16.7565310319826,14.45,25.5));
#99094=CARTESIAN_POINT('Origin',(17.1477990338188,13.375,25.5));
#99095=CARTESIAN_POINT('',(17.1477990338188,13.375,25.5));
#99096=CARTESIAN_POINT('',(17.1477990338188,13.375,25.5));
#99097=CARTESIAN_POINT('',(17.1477990338188,13.375,31.5));
#99098=CARTESIAN_POINT('',(17.1477990338188,13.375,31.5));
#99099=CARTESIAN_POINT('',(17.1477990338188,13.375,25.5));
#99100=CARTESIAN_POINT('Origin',(17.4982344043835,13.375,25.5));
#99101=CARTESIAN_POINT('',(17.4982344043835,13.375,25.5));
#99102=CARTESIAN_POINT('',(17.4982344043835,13.375,25.5));
#99103=CARTESIAN_POINT('',(17.4982344043835,13.375,31.5));
#99104=CARTESIAN_POINT('',(17.4982344043835,13.375,31.5));
#99105=CARTESIAN_POINT('',(17.4982344043835,13.375,25.5));
#99106=CARTESIAN_POINT('Origin',(17.8895024062196,14.45,25.5));
#99107=CARTESIAN_POINT('',(17.8895024062196,14.45,25.5));
#99108=CARTESIAN_POINT('',(17.8895024062196,14.45,25.5));
#99109=CARTESIAN_POINT('',(17.8895024062196,14.45,31.5));
#99110=CARTESIAN_POINT('',(17.8895024062196,14.45,31.5));
#99111=CARTESIAN_POINT('',(17.8895024062196,14.45,25.5));
#99112=CARTESIAN_POINT('Origin',(18.3273273587775,14.45,25.5));
#99113=CARTESIAN_POINT('',(18.3273273587775,14.45,25.5));
#99114=CARTESIAN_POINT('',(18.3273273587775,14.45,25.5));
#99115=CARTESIAN_POINT('',(18.3273273587775,14.45,31.5));
#99116=CARTESIAN_POINT('',(18.3273273587775,14.45,31.5));
#99117=CARTESIAN_POINT('',(18.3273273587775,14.45,25.5));
#99118=CARTESIAN_POINT('Origin',(18.7185953606136,13.375,25.5));
#99119=CARTESIAN_POINT('',(18.7185953606136,13.375,25.5));
#99120=CARTESIAN_POINT('',(18.7185953606136,13.375,25.5));
#99121=CARTESIAN_POINT('',(18.7185953606136,13.375,31.5));
#99122=CARTESIAN_POINT('',(18.7185953606136,13.375,31.5));
#99123=CARTESIAN_POINT('',(18.7185953606136,13.375,25.5));
#99124=CARTESIAN_POINT('Origin',(19.0690307311783,13.375,25.5));
#99125=CARTESIAN_POINT('',(19.0690307311783,13.375,25.5));
#99126=CARTESIAN_POINT('',(19.0690307311783,13.375,25.5));
#99127=CARTESIAN_POINT('',(19.0690307311783,13.375,31.5));
#99128=CARTESIAN_POINT('',(19.0690307311783,13.375,31.5));
#99129=CARTESIAN_POINT('',(19.0690307311783,13.375,25.5));
#99130=CARTESIAN_POINT('Origin',(19.4602987330145,14.45,25.5));
#99131=CARTESIAN_POINT('',(19.4602987330145,14.45,25.5));
#99132=CARTESIAN_POINT('',(19.4602987330145,14.45,25.5));
#99133=CARTESIAN_POINT('',(19.4602987330145,14.45,31.5));
#99134=CARTESIAN_POINT('',(19.4602987330145,14.45,31.5));
#99135=CARTESIAN_POINT('',(19.4602987330145,14.45,25.5));
#99136=CARTESIAN_POINT('Origin',(19.8981236855724,14.45,25.5));
#99137=CARTESIAN_POINT('',(19.8981236855724,14.45,25.5));
#99138=CARTESIAN_POINT('',(19.8981236855724,14.45,25.5));
#99139=CARTESIAN_POINT('',(19.8981236855724,14.45,31.5));
#99140=CARTESIAN_POINT('',(19.8981236855724,14.45,31.5));
#99141=CARTESIAN_POINT('',(19.8981236855724,14.45,25.5));
#99142=CARTESIAN_POINT('Origin',(20.2893916874086,13.375,25.5));
#99143=CARTESIAN_POINT('',(20.2893916874086,13.375,25.5));
#99144=CARTESIAN_POINT('',(20.2893916874086,13.375,25.5));
#99145=CARTESIAN_POINT('',(20.2893916874086,13.375,31.5));
#99146=CARTESIAN_POINT('',(20.2893916874086,13.375,31.5));
#99147=CARTESIAN_POINT('',(20.2893916874086,13.375,25.5));
#99148=CARTESIAN_POINT('Origin',(20.6398270579732,13.375,25.5));
#99149=CARTESIAN_POINT('',(20.6398270579732,13.375,25.5));
#99150=CARTESIAN_POINT('',(20.6398270579732,13.375,25.5));
#99151=CARTESIAN_POINT('',(20.6398270579732,13.375,31.5));
#99152=CARTESIAN_POINT('',(20.6398270579732,13.375,31.5));
#99153=CARTESIAN_POINT('',(20.6398270579732,13.375,25.5));
#99154=CARTESIAN_POINT('Origin',(21.0310950598094,14.45,25.5));
#99155=CARTESIAN_POINT('',(21.0310950598094,14.45,25.5));
#99156=CARTESIAN_POINT('',(21.0310950598094,14.45,25.5));
#99157=CARTESIAN_POINT('',(21.0310950598094,14.45,31.5));
#99158=CARTESIAN_POINT('',(21.0310950598094,14.45,31.5));
#99159=CARTESIAN_POINT('',(21.0310950598094,14.45,25.5));
#99160=CARTESIAN_POINT('Origin',(21.4689200123673,14.45,25.5));
#99161=CARTESIAN_POINT('',(21.4689200123673,14.45,25.5));
#99162=CARTESIAN_POINT('',(21.4689200123673,14.45,25.5));
#99163=CARTESIAN_POINT('',(21.4689200123673,14.45,31.5));
#99164=CARTESIAN_POINT('',(21.4689200123673,14.45,31.5));
#99165=CARTESIAN_POINT('',(21.4689200123673,14.45,25.5));
#99166=CARTESIAN_POINT('Origin',(21.8601880142034,13.375,25.5));
#99167=CARTESIAN_POINT('',(21.8601880142034,13.375,25.5));
#99168=CARTESIAN_POINT('',(21.8601880142034,13.375,25.5));
#99169=CARTESIAN_POINT('',(21.8601880142034,13.375,31.5));
#99170=CARTESIAN_POINT('',(21.8601880142034,13.375,31.5));
#99171=CARTESIAN_POINT('',(21.8601880142034,13.375,25.5));
#99172=CARTESIAN_POINT('Origin',(22.2106233847681,13.375,25.5));
#99173=CARTESIAN_POINT('',(22.2106233847681,13.375,25.5));
#99174=CARTESIAN_POINT('',(22.2106233847681,13.375,25.5));
#99175=CARTESIAN_POINT('',(22.2106233847681,13.375,31.5));
#99176=CARTESIAN_POINT('',(22.2106233847681,13.375,31.5));
#99177=CARTESIAN_POINT('',(22.2106233847681,13.375,25.5));
#99178=CARTESIAN_POINT('Origin',(22.6018913866043,14.45,25.5));
#99179=CARTESIAN_POINT('',(22.6018913866043,14.45,25.5));
#99180=CARTESIAN_POINT('',(22.6018913866043,14.45,25.5));
#99181=CARTESIAN_POINT('',(22.6018913866043,14.45,31.5));
#99182=CARTESIAN_POINT('',(22.6018913866043,14.45,31.5));
#99183=CARTESIAN_POINT('',(22.6018913866043,14.45,25.5));
#99184=CARTESIAN_POINT('Origin',(23.0397163391622,14.45,25.5));
#99185=CARTESIAN_POINT('',(23.0397163391622,14.45,25.5));
#99186=CARTESIAN_POINT('',(23.0397163391622,14.45,25.5));
#99187=CARTESIAN_POINT('',(23.0397163391622,14.45,31.5));
#99188=CARTESIAN_POINT('',(23.0397163391622,14.45,31.5));
#99189=CARTESIAN_POINT('',(23.0397163391622,14.45,25.5));
#99190=CARTESIAN_POINT('Origin',(23.4309843409983,13.375,25.5));
#99191=CARTESIAN_POINT('',(23.4309843409983,13.375,25.5));
#99192=CARTESIAN_POINT('',(23.4309843409983,13.375,25.5));
#99193=CARTESIAN_POINT('',(23.4309843409983,13.375,31.5));
#99194=CARTESIAN_POINT('',(23.4309843409983,13.375,31.5));
#99195=CARTESIAN_POINT('',(23.4309843409983,13.375,25.5));
#99196=CARTESIAN_POINT('Origin',(23.781419711563,13.375,25.5));
#99197=CARTESIAN_POINT('',(23.781419711563,13.375,25.5));
#99198=CARTESIAN_POINT('',(23.781419711563,13.375,25.5));
#99199=CARTESIAN_POINT('',(23.781419711563,13.375,31.5));
#99200=CARTESIAN_POINT('',(23.781419711563,13.375,31.5));
#99201=CARTESIAN_POINT('',(23.781419711563,13.375,25.5));
#99202=CARTESIAN_POINT('Origin',(24.1726877133992,14.45,25.5));
#99203=CARTESIAN_POINT('',(24.1726877133992,14.45,25.5));
#99204=CARTESIAN_POINT('',(24.1726877133992,14.45,25.5));
#99205=CARTESIAN_POINT('',(24.1726877133992,14.45,31.5));
#99206=CARTESIAN_POINT('',(24.1726877133992,14.45,31.5));
#99207=CARTESIAN_POINT('',(24.1726877133992,14.45,25.5));
#99208=CARTESIAN_POINT('Origin',(24.6105126659571,14.45,25.5));
#99209=CARTESIAN_POINT('',(24.6105126659571,14.45,25.5));
#99210=CARTESIAN_POINT('',(24.6105126659571,14.45,25.5));
#99211=CARTESIAN_POINT('',(24.6105126659571,14.45,31.5));
#99212=CARTESIAN_POINT('',(24.6105126659571,14.45,31.5));
#99213=CARTESIAN_POINT('',(24.6105126659571,14.45,25.5));
#99214=CARTESIAN_POINT('Origin',(25.0017806677932,13.375,25.5));
#99215=CARTESIAN_POINT('',(25.0017806677932,13.375,25.5));
#99216=CARTESIAN_POINT('',(25.0017806677932,13.375,25.5));
#99217=CARTESIAN_POINT('',(25.0017806677932,13.375,31.5));
#99218=CARTESIAN_POINT('',(25.0017806677932,13.375,31.5));
#99219=CARTESIAN_POINT('',(25.0017806677932,13.375,25.5));
#99220=CARTESIAN_POINT('Origin',(25.3522160383579,13.375,25.5));
#99221=CARTESIAN_POINT('',(25.3522160383579,13.375,25.5));
#99222=CARTESIAN_POINT('',(25.3522160383579,13.375,25.5));
#99223=CARTESIAN_POINT('',(25.3522160383579,13.375,31.5));
#99224=CARTESIAN_POINT('',(25.3522160383579,13.375,31.5));
#99225=CARTESIAN_POINT('',(25.3522160383579,13.375,25.5));
#99226=CARTESIAN_POINT('Origin',(25.7434840401941,14.45,25.5));
#99227=CARTESIAN_POINT('',(25.7434840401941,14.45,25.5));
#99228=CARTESIAN_POINT('',(25.7434840401941,14.45,25.5));
#99229=CARTESIAN_POINT('',(25.7434840401941,14.45,31.5));
#99230=CARTESIAN_POINT('',(25.7434840401941,14.45,31.5));
#99231=CARTESIAN_POINT('',(25.7434840401941,14.45,25.5));
#99232=CARTESIAN_POINT('Origin',(26.181308992752,14.45,25.5));
#99233=CARTESIAN_POINT('',(26.181308992752,14.45,25.5));
#99234=CARTESIAN_POINT('',(26.181308992752,14.45,25.5));
#99235=CARTESIAN_POINT('',(26.181308992752,14.45,31.5));
#99236=CARTESIAN_POINT('',(26.181308992752,14.45,31.5));
#99237=CARTESIAN_POINT('',(26.181308992752,14.45,25.5));
#99238=CARTESIAN_POINT('Origin',(26.5725769945881,13.375,25.5));
#99239=CARTESIAN_POINT('',(26.5725769945881,13.375,25.5));
#99240=CARTESIAN_POINT('',(26.5725769945881,13.375,25.5));
#99241=CARTESIAN_POINT('',(26.5725769945881,13.375,31.5));
#99242=CARTESIAN_POINT('',(26.5725769945881,13.375,31.5));
#99243=CARTESIAN_POINT('',(26.5725769945881,13.375,25.5));
#99244=CARTESIAN_POINT('Origin',(26.9230123651528,13.375,25.5));
#99245=CARTESIAN_POINT('',(26.9230123651528,13.375,25.5));
#99246=CARTESIAN_POINT('',(26.9230123651528,13.375,25.5));
#99247=CARTESIAN_POINT('',(26.9230123651528,13.375,31.5));
#99248=CARTESIAN_POINT('',(26.9230123651528,13.375,31.5));
#99249=CARTESIAN_POINT('',(26.9230123651528,13.375,25.5));
#99250=CARTESIAN_POINT('Origin',(27.314280366989,14.45,25.5));
#99251=CARTESIAN_POINT('',(27.314280366989,14.45,25.5));
#99252=CARTESIAN_POINT('',(27.314280366989,14.45,25.5));
#99253=CARTESIAN_POINT('',(27.314280366989,14.45,31.5));
#99254=CARTESIAN_POINT('',(27.314280366989,14.45,31.5));
#99255=CARTESIAN_POINT('',(27.314280366989,14.45,25.5));
#99256=CARTESIAN_POINT('Origin',(27.7521053195469,14.45,25.5));
#99257=CARTESIAN_POINT('',(27.7521053195469,14.45,25.5));
#99258=CARTESIAN_POINT('',(27.7521053195469,14.45,25.5));
#99259=CARTESIAN_POINT('',(27.7521053195469,14.45,31.5));
#99260=CARTESIAN_POINT('',(27.7521053195469,14.45,31.5));
#99261=CARTESIAN_POINT('',(27.7521053195469,14.45,25.5));
#99262=CARTESIAN_POINT('Origin',(28.143373321383,13.375,25.5));
#99263=CARTESIAN_POINT('',(28.143373321383,13.375,25.5));
#99264=CARTESIAN_POINT('',(28.143373321383,13.375,25.5));
#99265=CARTESIAN_POINT('',(28.143373321383,13.375,31.5));
#99266=CARTESIAN_POINT('',(28.143373321383,13.375,31.5));
#99267=CARTESIAN_POINT('',(28.143373321383,13.375,25.5));
#99268=CARTESIAN_POINT('Origin',(28.4938086919477,13.375,25.5));
#99269=CARTESIAN_POINT('',(28.4938086919477,13.375,25.5));
#99270=CARTESIAN_POINT('',(28.4938086919477,13.375,25.5));
#99271=CARTESIAN_POINT('',(28.4938086919477,13.375,31.5));
#99272=CARTESIAN_POINT('',(28.4938086919477,13.375,31.5));
#99273=CARTESIAN_POINT('',(28.4938086919477,13.375,25.5));
#99274=CARTESIAN_POINT('Origin',(28.8850766937839,14.45,25.5));
#99275=CARTESIAN_POINT('',(28.8850766937839,14.45,25.5));
#99276=CARTESIAN_POINT('',(28.8850766937839,14.45,25.5));
#99277=CARTESIAN_POINT('',(28.8850766937839,14.45,31.5));
#99278=CARTESIAN_POINT('',(28.8850766937839,14.45,31.5));
#99279=CARTESIAN_POINT('',(28.8850766937839,14.45,25.5));
#99280=CARTESIAN_POINT('Origin',(29.3229016463418,14.45,25.5));
#99281=CARTESIAN_POINT('',(29.3229016463418,14.45,25.5));
#99282=CARTESIAN_POINT('',(29.3229016463418,14.45,25.5));
#99283=CARTESIAN_POINT('',(29.3229016463418,14.45,31.5));
#99284=CARTESIAN_POINT('',(29.3229016463418,14.45,31.5));
#99285=CARTESIAN_POINT('',(29.3229016463418,14.45,25.5));
#99286=CARTESIAN_POINT('Origin',(29.7141696481779,13.375,25.5));
#99287=CARTESIAN_POINT('',(29.7141696481779,13.375,25.5));
#99288=CARTESIAN_POINT('',(29.7141696481779,13.375,25.5));
#99289=CARTESIAN_POINT('',(29.7141696481779,13.375,31.5));
#99290=CARTESIAN_POINT('',(29.7141696481779,13.375,31.5));
#99291=CARTESIAN_POINT('',(29.7141696481779,13.375,25.5));
#99292=CARTESIAN_POINT('Origin',(30.0646050187426,13.375,25.5));
#99293=CARTESIAN_POINT('',(30.0646050187426,13.375,25.5));
#99294=CARTESIAN_POINT('',(30.0646050187426,13.375,25.5));
#99295=CARTESIAN_POINT('',(30.0646050187426,13.375,31.5));
#99296=CARTESIAN_POINT('',(30.0646050187426,13.375,31.5));
#99297=CARTESIAN_POINT('',(30.0646050187426,13.375,25.5));
#99298=CARTESIAN_POINT('Origin',(30.4558730205788,14.45,25.5));
#99299=CARTESIAN_POINT('',(30.4558730205788,14.45,25.5));
#99300=CARTESIAN_POINT('',(30.4558730205788,14.45,25.5));
#99301=CARTESIAN_POINT('',(30.4558730205788,14.45,31.5));
#99302=CARTESIAN_POINT('',(30.4558730205788,14.45,31.5));
#99303=CARTESIAN_POINT('',(30.4558730205788,14.45,25.5));
#99304=CARTESIAN_POINT('Origin',(30.8936979731367,14.45,25.5));
#99305=CARTESIAN_POINT('',(30.8936979731367,14.45,25.5));
#99306=CARTESIAN_POINT('',(30.8936979731367,14.45,25.5));
#99307=CARTESIAN_POINT('',(30.8936979731367,14.45,31.5));
#99308=CARTESIAN_POINT('',(30.8936979731367,14.45,31.5));
#99309=CARTESIAN_POINT('',(30.8936979731367,14.45,25.5));
#99310=CARTESIAN_POINT('Origin',(31.2849659749728,13.375,25.5));
#99311=CARTESIAN_POINT('',(31.2849659749728,13.375,25.5));
#99312=CARTESIAN_POINT('',(31.2849659749728,13.375,25.5));
#99313=CARTESIAN_POINT('',(31.2849659749728,13.375,31.5));
#99314=CARTESIAN_POINT('',(31.2849659749728,13.375,31.5));
#99315=CARTESIAN_POINT('',(31.2849659749728,13.375,25.5));
#99316=CARTESIAN_POINT('Origin',(31.6354013455375,13.375,25.5));
#99317=CARTESIAN_POINT('',(31.6354013455375,13.375,25.5));
#99318=CARTESIAN_POINT('',(31.6354013455375,13.375,25.5));
#99319=CARTESIAN_POINT('',(31.6354013455375,13.375,31.5));
#99320=CARTESIAN_POINT('',(31.6354013455375,13.375,31.5));
#99321=CARTESIAN_POINT('',(31.6354013455375,13.375,25.5));
#99322=CARTESIAN_POINT('Origin',(32.0266693473737,14.45,25.5));
#99323=CARTESIAN_POINT('',(32.0266693473737,14.45,25.5));
#99324=CARTESIAN_POINT('',(32.0266693473737,14.45,25.5));
#99325=CARTESIAN_POINT('',(32.0266693473737,14.45,31.5));
#99326=CARTESIAN_POINT('',(32.0266693473737,14.45,31.5));
#99327=CARTESIAN_POINT('',(32.0266693473737,14.45,25.5));
#99328=CARTESIAN_POINT('Origin',(32.4644942999316,14.45,25.5));
#99329=CARTESIAN_POINT('',(32.4644942999316,14.45,25.5));
#99330=CARTESIAN_POINT('',(32.4644942999316,14.45,25.5));
#99331=CARTESIAN_POINT('',(32.4644942999316,14.45,31.5));
#99332=CARTESIAN_POINT('',(32.4644942999316,14.45,31.5));
#99333=CARTESIAN_POINT('',(32.4644942999316,14.45,25.5));
#99334=CARTESIAN_POINT('Origin',(32.8557623017677,13.375,25.5));
#99335=CARTESIAN_POINT('',(32.8557623017677,13.375,25.5));
#99336=CARTESIAN_POINT('',(32.8557623017677,13.375,25.5));
#99337=CARTESIAN_POINT('',(32.8557623017677,13.375,31.5));
#99338=CARTESIAN_POINT('',(32.8557623017677,13.375,31.5));
#99339=CARTESIAN_POINT('',(32.8557623017677,13.375,25.5));
#99340=CARTESIAN_POINT('Origin',(33.2061976723324,13.375,25.5));
#99341=CARTESIAN_POINT('',(33.2061976723324,13.375,25.5));
#99342=CARTESIAN_POINT('',(33.2061976723324,13.375,25.5));
#99343=CARTESIAN_POINT('',(33.2061976723324,13.375,31.5));
#99344=CARTESIAN_POINT('',(33.2061976723324,13.375,31.5));
#99345=CARTESIAN_POINT('',(33.2061976723324,13.375,25.5));
#99346=CARTESIAN_POINT('Origin',(33.5974656741686,14.45,25.5));
#99347=CARTESIAN_POINT('',(33.5974656741686,14.45,25.5));
#99348=CARTESIAN_POINT('',(33.5974656741686,14.45,25.5));
#99349=CARTESIAN_POINT('',(33.5974656741686,14.45,31.5));
#99350=CARTESIAN_POINT('',(33.5974656741686,14.45,31.5));
#99351=CARTESIAN_POINT('',(33.5974656741686,14.45,25.5));
#99352=CARTESIAN_POINT('Origin',(34.0352906267265,14.45,25.5));
#99353=CARTESIAN_POINT('',(34.0352906267265,14.45,25.5));
#99354=CARTESIAN_POINT('',(34.0352906267265,14.45,25.5));
#99355=CARTESIAN_POINT('',(34.0352906267265,14.45,31.5));
#99356=CARTESIAN_POINT('',(34.0352906267265,14.45,31.5));
#99357=CARTESIAN_POINT('',(34.0352906267265,14.45,25.5));
#99358=CARTESIAN_POINT('Origin',(34.4265586285626,13.375,25.5));
#99359=CARTESIAN_POINT('',(34.4265586285626,13.375,25.5));
#99360=CARTESIAN_POINT('',(34.4265586285626,13.375,25.5));
#99361=CARTESIAN_POINT('',(34.4265586285626,13.375,31.5));
#99362=CARTESIAN_POINT('',(34.4265586285626,13.375,31.5));
#99363=CARTESIAN_POINT('',(34.4265586285626,13.375,25.5));
#99364=CARTESIAN_POINT('Origin',(34.7769939991273,13.375,25.5));
#99365=CARTESIAN_POINT('',(34.7769939991273,13.375,25.5));
#99366=CARTESIAN_POINT('',(34.7769939991273,13.375,25.5));
#99367=CARTESIAN_POINT('',(34.7769939991273,13.375,31.5));
#99368=CARTESIAN_POINT('',(34.7769939991273,13.375,31.5));
#99369=CARTESIAN_POINT('',(34.7769939991273,13.375,25.5));
#99370=CARTESIAN_POINT('Origin',(35.1682620009635,14.45,25.5));
#99371=CARTESIAN_POINT('',(35.1682620009635,14.45,25.5));
#99372=CARTESIAN_POINT('',(35.1682620009635,14.45,25.5));
#99373=CARTESIAN_POINT('',(35.1682620009635,14.45,31.5));
#99374=CARTESIAN_POINT('',(35.1682620009635,14.45,31.5));
#99375=CARTESIAN_POINT('',(35.1682620009635,14.45,25.5));
#99376=CARTESIAN_POINT('Origin',(35.6060869535213,14.45,25.5));
#99377=CARTESIAN_POINT('',(35.6060869535213,14.45,25.5));
#99378=CARTESIAN_POINT('',(35.6060869535213,14.45,25.5));
#99379=CARTESIAN_POINT('',(35.6060869535213,14.45,31.5));
#99380=CARTESIAN_POINT('',(35.6060869535213,14.45,31.5));
#99381=CARTESIAN_POINT('',(35.6060869535213,14.45,25.5));
#99382=CARTESIAN_POINT('Origin',(35.9973549553575,13.375,25.5));
#99383=CARTESIAN_POINT('',(35.9973549553575,13.375,25.5));
#99384=CARTESIAN_POINT('',(35.9973549553575,13.375,25.5));
#99385=CARTESIAN_POINT('',(35.9973549553575,13.375,31.5));
#99386=CARTESIAN_POINT('',(35.9973549553575,13.375,31.5));
#99387=CARTESIAN_POINT('',(35.9973549553575,13.375,25.5));
#99388=CARTESIAN_POINT('Origin',(36.3477903259222,13.375,25.5));
#99389=CARTESIAN_POINT('',(36.3477903259222,13.375,25.5));
#99390=CARTESIAN_POINT('',(36.3477903259222,13.375,25.5));
#99391=CARTESIAN_POINT('',(36.3477903259222,13.375,31.5));
#99392=CARTESIAN_POINT('',(36.3477903259222,13.375,31.5));
#99393=CARTESIAN_POINT('',(36.3477903259222,13.375,25.5));
#99394=CARTESIAN_POINT('Origin',(36.7390583277584,14.45,25.5));
#99395=CARTESIAN_POINT('',(36.7390583277584,14.45,25.5));
#99396=CARTESIAN_POINT('',(36.7390583277584,14.45,25.5));
#99397=CARTESIAN_POINT('',(36.7390583277584,14.45,31.5));
#99398=CARTESIAN_POINT('',(36.7390583277584,14.45,31.5));
#99399=CARTESIAN_POINT('',(36.7390583277584,14.45,25.5));
#99400=CARTESIAN_POINT('Origin',(37.1768832803162,14.45,25.5));
#99401=CARTESIAN_POINT('',(37.1768832803162,14.45,25.5));
#99402=CARTESIAN_POINT('',(37.1768832803162,14.45,25.5));
#99403=CARTESIAN_POINT('',(37.1768832803162,14.45,31.5));
#99404=CARTESIAN_POINT('',(37.1768832803162,14.45,31.5));
#99405=CARTESIAN_POINT('',(37.1768832803162,14.45,25.5));
#99406=CARTESIAN_POINT('Origin',(37.5681512821524,13.375,25.5));
#99407=CARTESIAN_POINT('',(37.5681512821524,13.375,25.5));
#99408=CARTESIAN_POINT('',(37.5681512821524,13.375,25.5));
#99409=CARTESIAN_POINT('',(37.5681512821524,13.375,31.5));
#99410=CARTESIAN_POINT('',(37.5681512821524,13.375,31.5));
#99411=CARTESIAN_POINT('',(37.5681512821524,13.375,25.5));
#99412=CARTESIAN_POINT('Origin',(37.9185866527171,13.375,25.5));
#99413=CARTESIAN_POINT('',(37.9185866527171,13.375,25.5));
#99414=CARTESIAN_POINT('',(37.9185866527171,13.375,25.5));
#99415=CARTESIAN_POINT('',(37.9185866527171,13.375,31.5));
#99416=CARTESIAN_POINT('',(37.9185866527171,13.375,31.5));
#99417=CARTESIAN_POINT('',(37.9185866527171,13.375,25.5));
#99418=CARTESIAN_POINT('Origin',(38.3098546545533,14.45,25.5));
#99419=CARTESIAN_POINT('',(38.3098546545533,14.45,25.5));
#99420=CARTESIAN_POINT('',(38.3098546545533,14.45,25.5));
#99421=CARTESIAN_POINT('',(38.3098546545533,14.45,31.5));
#99422=CARTESIAN_POINT('',(38.3098546545533,14.45,31.5));
#99423=CARTESIAN_POINT('',(38.3098546545533,14.45,25.5));
#99424=CARTESIAN_POINT('Origin',(38.7476796071111,14.45,25.5));
#99425=CARTESIAN_POINT('',(38.7476796071111,14.45,25.5));
#99426=CARTESIAN_POINT('',(38.7476796071111,14.45,25.5));
#99427=CARTESIAN_POINT('',(38.7476796071111,14.45,31.5));
#99428=CARTESIAN_POINT('',(38.7476796071111,14.45,31.5));
#99429=CARTESIAN_POINT('',(38.7476796071111,14.45,25.5));
#99430=CARTESIAN_POINT('Origin',(39.1389476089473,13.375,25.5));
#99431=CARTESIAN_POINT('',(39.1389476089473,13.375,25.5));
#99432=CARTESIAN_POINT('',(39.1389476089473,13.375,25.5));
#99433=CARTESIAN_POINT('',(39.1389476089473,13.375,31.5));
#99434=CARTESIAN_POINT('',(39.1389476089473,13.375,31.5));
#99435=CARTESIAN_POINT('',(39.1389476089473,13.375,25.5));
#99436=CARTESIAN_POINT('Origin',(39.489382979512,13.375,25.5));
#99437=CARTESIAN_POINT('',(39.489382979512,13.375,25.5));
#99438=CARTESIAN_POINT('',(39.489382979512,13.375,25.5));
#99439=CARTESIAN_POINT('',(39.489382979512,13.375,31.5));
#99440=CARTESIAN_POINT('',(39.489382979512,13.375,31.5));
#99441=CARTESIAN_POINT('',(39.489382979512,13.375,25.5));
#99442=CARTESIAN_POINT('Origin',(39.8806509813482,14.45,25.5));
#99443=CARTESIAN_POINT('',(39.8806509813482,14.45,25.5));
#99444=CARTESIAN_POINT('',(39.8806509813482,14.45,25.5));
#99445=CARTESIAN_POINT('',(39.8806509813482,14.45,31.5));
#99446=CARTESIAN_POINT('',(39.8806509813482,14.45,31.5));
#99447=CARTESIAN_POINT('',(39.8806509813482,14.45,25.5));
#99448=CARTESIAN_POINT('Origin',(40.318475933906,14.45,25.5));
#99449=CARTESIAN_POINT('',(40.318475933906,14.45,25.5));
#99450=CARTESIAN_POINT('',(40.318475933906,14.45,25.5));
#99451=CARTESIAN_POINT('',(40.318475933906,14.45,31.5));
#99452=CARTESIAN_POINT('',(40.318475933906,14.45,31.5));
#99453=CARTESIAN_POINT('',(40.318475933906,14.45,25.5));
#99454=CARTESIAN_POINT('Origin',(40.7097439357422,13.375,25.5));
#99455=CARTESIAN_POINT('',(40.7097439357422,13.375,25.5));
#99456=CARTESIAN_POINT('',(40.7097439357422,13.375,25.5));
#99457=CARTESIAN_POINT('',(40.7097439357422,13.375,31.5));
#99458=CARTESIAN_POINT('',(40.7097439357422,13.375,31.5));
#99459=CARTESIAN_POINT('',(40.7097439357422,13.375,25.5));
#99460=CARTESIAN_POINT('Origin',(41.0601793063069,13.375,25.5));
#99461=CARTESIAN_POINT('',(41.0601793063069,13.375,25.5));
#99462=CARTESIAN_POINT('',(41.0601793063069,13.375,25.5));
#99463=CARTESIAN_POINT('',(41.0601793063069,13.375,31.5));
#99464=CARTESIAN_POINT('',(41.0601793063069,13.375,31.5));
#99465=CARTESIAN_POINT('',(41.0601793063069,13.375,25.5));
#99466=CARTESIAN_POINT('Origin',(41.4514473081431,14.45,25.5));
#99467=CARTESIAN_POINT('',(41.4514473081431,14.45,25.5));
#99468=CARTESIAN_POINT('',(41.4514473081431,14.45,25.5));
#99469=CARTESIAN_POINT('',(41.4514473081431,14.45,31.5));
#99470=CARTESIAN_POINT('',(41.4514473081431,14.45,31.5));
#99471=CARTESIAN_POINT('',(41.4514473081431,14.45,25.5));
#99472=CARTESIAN_POINT('Origin',(41.8892722607009,14.45,25.5));
#99473=CARTESIAN_POINT('',(41.8892722607009,14.45,25.5));
#99474=CARTESIAN_POINT('',(41.8892722607009,14.45,25.5));
#99475=CARTESIAN_POINT('',(41.8892722607009,14.45,31.5));
#99476=CARTESIAN_POINT('',(41.8892722607009,14.45,31.5));
#99477=CARTESIAN_POINT('',(41.8892722607009,14.45,25.5));
#99478=CARTESIAN_POINT('Origin',(42.2805402625371,13.375,25.5));
#99479=CARTESIAN_POINT('',(42.2805402625371,13.375,25.5));
#99480=CARTESIAN_POINT('',(42.2805402625371,13.375,25.5));
#99481=CARTESIAN_POINT('',(42.2805402625371,13.375,31.5));
#99482=CARTESIAN_POINT('',(42.2805402625371,13.375,31.5));
#99483=CARTESIAN_POINT('',(42.2805402625371,13.375,25.5));
#99484=CARTESIAN_POINT('Origin',(42.6309756331018,13.375,25.5));
#99485=CARTESIAN_POINT('',(42.6309756331018,13.375,25.5));
#99486=CARTESIAN_POINT('',(42.6309756331018,13.375,25.5));
#99487=CARTESIAN_POINT('',(42.6309756331018,13.375,31.5));
#99488=CARTESIAN_POINT('',(42.6309756331018,13.375,31.5));
#99489=CARTESIAN_POINT('',(42.6309756331018,13.375,25.5));
#99490=CARTESIAN_POINT('Origin',(43.022243634938,14.45,25.5));
#99491=CARTESIAN_POINT('',(43.022243634938,14.45,25.5));
#99492=CARTESIAN_POINT('',(43.022243634938,14.45,25.5));
#99493=CARTESIAN_POINT('',(43.022243634938,14.45,31.5));
#99494=CARTESIAN_POINT('',(43.022243634938,14.45,31.5));
#99495=CARTESIAN_POINT('',(43.022243634938,14.45,25.5));
#99496=CARTESIAN_POINT('Origin',(43.4600685874958,14.45,25.5));
#99497=CARTESIAN_POINT('',(43.4600685874958,14.45,25.5));
#99498=CARTESIAN_POINT('',(43.4600685874958,14.45,25.5));
#99499=CARTESIAN_POINT('',(43.4600685874958,14.45,31.5));
#99500=CARTESIAN_POINT('',(43.4600685874958,14.45,31.5));
#99501=CARTESIAN_POINT('',(43.4600685874958,14.45,25.5));
#99502=CARTESIAN_POINT('Origin',(43.851336589332,13.375,25.5));
#99503=CARTESIAN_POINT('',(43.851336589332,13.375,25.5));
#99504=CARTESIAN_POINT('',(43.851336589332,13.375,25.5));
#99505=CARTESIAN_POINT('',(43.851336589332,13.375,31.5));
#99506=CARTESIAN_POINT('',(43.851336589332,13.375,31.5));
#99507=CARTESIAN_POINT('',(43.851336589332,13.375,25.5));
#99508=CARTESIAN_POINT('Origin',(44.2017719598967,13.375,25.5));
#99509=CARTESIAN_POINT('',(44.2017719598967,13.375,25.5));
#99510=CARTESIAN_POINT('',(44.2017719598967,13.375,25.5));
#99511=CARTESIAN_POINT('',(44.2017719598967,13.375,31.5));
#99512=CARTESIAN_POINT('',(44.2017719598967,13.375,31.5));
#99513=CARTESIAN_POINT('',(44.2017719598967,13.375,25.5));
#99514=CARTESIAN_POINT('Origin',(44.5930399617329,14.45,25.5));
#99515=CARTESIAN_POINT('',(44.5930399617329,14.45,25.5));
#99516=CARTESIAN_POINT('',(44.5930399617329,14.45,25.5));
#99517=CARTESIAN_POINT('',(44.5930399617329,14.45,31.5));
#99518=CARTESIAN_POINT('',(44.5930399617329,14.45,31.5));
#99519=CARTESIAN_POINT('',(44.5930399617329,14.45,25.5));
#99520=CARTESIAN_POINT('Origin',(45.0308649142907,14.45,25.5));
#99521=CARTESIAN_POINT('',(45.0308649142907,14.45,25.5));
#99522=CARTESIAN_POINT('',(45.0308649142907,14.45,25.5));
#99523=CARTESIAN_POINT('',(45.0308649142907,14.45,31.5));
#99524=CARTESIAN_POINT('',(45.0308649142907,14.45,31.5));
#99525=CARTESIAN_POINT('',(45.0308649142907,14.45,25.5));
#99526=CARTESIAN_POINT('Origin',(45.4221329161269,13.375,25.5));
#99527=CARTESIAN_POINT('',(45.4221329161269,13.375,25.5));
#99528=CARTESIAN_POINT('',(45.4221329161269,13.375,25.5));
#99529=CARTESIAN_POINT('',(45.4221329161269,13.375,31.5));
#99530=CARTESIAN_POINT('',(45.4221329161269,13.375,31.5));
#99531=CARTESIAN_POINT('',(45.4221329161269,13.375,25.5));
#99532=CARTESIAN_POINT('Origin',(45.7725682866916,13.375,25.5));
#99533=CARTESIAN_POINT('',(45.7725682866916,13.375,25.5));
#99534=CARTESIAN_POINT('',(45.7725682866916,13.375,25.5));
#99535=CARTESIAN_POINT('',(45.7725682866916,13.375,31.5));
#99536=CARTESIAN_POINT('',(45.7725682866916,13.375,31.5));
#99537=CARTESIAN_POINT('',(45.7725682866916,13.375,25.5));
#99538=CARTESIAN_POINT('Origin',(46.1638362885278,14.45,25.5));
#99539=CARTESIAN_POINT('',(46.1638362885278,14.45,25.5));
#99540=CARTESIAN_POINT('',(46.1638362885278,14.45,25.5));
#99541=CARTESIAN_POINT('',(46.1638362885278,14.45,31.5));
#99542=CARTESIAN_POINT('',(46.1638362885278,14.45,31.5));
#99543=CARTESIAN_POINT('',(46.1638362885278,14.45,25.5));
#99544=CARTESIAN_POINT('Origin',(46.6016612410856,14.45,25.5));
#99545=CARTESIAN_POINT('',(46.6016612410856,14.45,25.5));
#99546=CARTESIAN_POINT('',(46.6016612410856,14.45,25.5));
#99547=CARTESIAN_POINT('',(46.6016612410856,14.45,31.5));
#99548=CARTESIAN_POINT('',(46.6016612410856,14.45,31.5));
#99549=CARTESIAN_POINT('',(46.6016612410856,14.45,25.5));
#99550=CARTESIAN_POINT('Origin',(46.9929292429218,13.375,25.5));
#99551=CARTESIAN_POINT('',(46.9929292429218,13.375,25.5));
#99552=CARTESIAN_POINT('',(46.9929292429218,13.375,25.5));
#99553=CARTESIAN_POINT('',(46.9929292429218,13.375,31.5));
#99554=CARTESIAN_POINT('',(46.9929292429218,13.375,31.5));
#99555=CARTESIAN_POINT('',(46.9929292429218,13.375,25.5));
#99556=CARTESIAN_POINT('Origin',(47.3433646134865,13.375,25.5));
#99557=CARTESIAN_POINT('',(47.3433646134865,13.375,25.5));
#99558=CARTESIAN_POINT('',(47.3433646134865,13.375,25.5));
#99559=CARTESIAN_POINT('',(47.3433646134865,13.375,31.5));
#99560=CARTESIAN_POINT('',(47.3433646134865,13.375,31.5));
#99561=CARTESIAN_POINT('',(47.3433646134865,13.375,25.5));
#99562=CARTESIAN_POINT('Origin',(47.7346326153227,14.45,25.5));
#99563=CARTESIAN_POINT('',(47.7346326153227,14.45,25.5));
#99564=CARTESIAN_POINT('',(47.7346326153227,14.45,25.5));
#99565=CARTESIAN_POINT('',(47.7346326153227,14.45,31.5));
#99566=CARTESIAN_POINT('',(47.7346326153227,14.45,31.5));
#99567=CARTESIAN_POINT('',(47.7346326153227,14.45,25.5));
#99568=CARTESIAN_POINT('Origin',(48.1724575678805,14.45,25.5));
#99569=CARTESIAN_POINT('',(48.1724575678805,14.45,25.5));
#99570=CARTESIAN_POINT('',(48.1724575678805,14.45,25.5));
#99571=CARTESIAN_POINT('',(48.1724575678805,14.45,31.5));
#99572=CARTESIAN_POINT('',(48.1724575678805,14.45,31.5));
#99573=CARTESIAN_POINT('',(48.1724575678805,14.45,25.5));
#99574=CARTESIAN_POINT('Origin',(48.5637255697167,13.375,25.5));
#99575=CARTESIAN_POINT('',(48.5637255697167,13.375,25.5));
#99576=CARTESIAN_POINT('',(48.5637255697167,13.375,25.5));
#99577=CARTESIAN_POINT('',(48.5637255697167,13.375,31.5));
#99578=CARTESIAN_POINT('',(48.5637255697167,13.375,31.5));
#99579=CARTESIAN_POINT('',(48.5637255697167,13.375,25.5));
#99580=CARTESIAN_POINT('Origin',(48.9141609402814,13.375,25.5));
#99581=CARTESIAN_POINT('',(48.9141609402814,13.375,25.5));
#99582=CARTESIAN_POINT('',(48.9141609402814,13.375,25.5));
#99583=CARTESIAN_POINT('',(48.9141609402814,13.375,31.5));
#99584=CARTESIAN_POINT('',(48.9141609402814,13.375,31.5));
#99585=CARTESIAN_POINT('',(48.9141609402814,13.375,25.5));
#99586=CARTESIAN_POINT('Origin',(49.3054289421176,14.45,25.5));
#99587=CARTESIAN_POINT('',(49.3054289421176,14.45,25.5));
#99588=CARTESIAN_POINT('',(49.3054289421176,14.45,25.5));
#99589=CARTESIAN_POINT('',(49.3054289421176,14.45,31.5));
#99590=CARTESIAN_POINT('',(49.3054289421176,14.45,31.5));
#99591=CARTESIAN_POINT('',(49.3054289421176,14.45,25.5));
#99592=CARTESIAN_POINT('Origin',(49.7432538946754,14.45,25.5));
#99593=CARTESIAN_POINT('',(49.7432538946754,14.45,25.5));
#99594=CARTESIAN_POINT('',(49.7432538946754,14.45,25.5));
#99595=CARTESIAN_POINT('',(49.7432538946754,14.45,31.5));
#99596=CARTESIAN_POINT('',(49.7432538946754,14.45,31.5));
#99597=CARTESIAN_POINT('',(49.7432538946754,14.45,25.5));
#99598=CARTESIAN_POINT('Origin',(50.1345218965116,13.375,25.5));
#99599=CARTESIAN_POINT('',(50.1345218965116,13.375,25.5));
#99600=CARTESIAN_POINT('',(50.1345218965116,13.375,25.5));
#99601=CARTESIAN_POINT('',(50.1345218965116,13.375,31.5));
#99602=CARTESIAN_POINT('',(50.1345218965116,13.375,31.5));
#99603=CARTESIAN_POINT('',(50.1345218965116,13.375,25.5));
#99604=CARTESIAN_POINT('Origin',(50.4849572670763,13.375,25.5));
#99605=CARTESIAN_POINT('',(50.4849572670763,13.375,25.5));
#99606=CARTESIAN_POINT('',(50.4849572670763,13.375,25.5));
#99607=CARTESIAN_POINT('',(50.4849572670763,13.375,31.5));
#99608=CARTESIAN_POINT('',(50.4849572670763,13.375,31.5));
#99609=CARTESIAN_POINT('',(50.4849572670763,13.375,25.5));
#99610=CARTESIAN_POINT('Origin',(50.8762252689124,14.45,25.5));
#99611=CARTESIAN_POINT('',(50.8762252689124,14.45,25.5));
#99612=CARTESIAN_POINT('',(50.8762252689124,14.45,25.5));
#99613=CARTESIAN_POINT('',(50.8762252689124,14.45,31.5));
#99614=CARTESIAN_POINT('',(50.8762252689124,14.45,31.5));
#99615=CARTESIAN_POINT('',(50.8762252689124,14.45,25.5));
#99616=CARTESIAN_POINT('Origin',(51.3140502214703,14.45,25.5));
#99617=CARTESIAN_POINT('',(51.3140502214703,14.45,25.5));
#99618=CARTESIAN_POINT('',(51.3140502214703,14.45,25.5));
#99619=CARTESIAN_POINT('',(51.3140502214703,14.45,31.5));
#99620=CARTESIAN_POINT('',(51.3140502214703,14.45,31.5));
#99621=CARTESIAN_POINT('',(51.3140502214703,14.45,25.5));
#99622=CARTESIAN_POINT('Origin',(51.7053182233065,13.375,25.5));
#99623=CARTESIAN_POINT('',(51.7053182233065,13.375,25.5));
#99624=CARTESIAN_POINT('',(51.7053182233065,13.375,25.5));
#99625=CARTESIAN_POINT('',(51.7053182233065,13.375,31.5));
#99626=CARTESIAN_POINT('',(51.7053182233065,13.375,31.5));
#99627=CARTESIAN_POINT('',(51.7053182233065,13.375,25.5));
#99628=CARTESIAN_POINT('Origin',(52.0557535938712,13.375,25.5));
#99629=CARTESIAN_POINT('',(52.0557535938712,13.375,25.5));
#99630=CARTESIAN_POINT('',(52.0557535938712,13.375,25.5));
#99631=CARTESIAN_POINT('',(52.0557535938712,13.375,31.5));
#99632=CARTESIAN_POINT('',(52.0557535938712,13.375,31.5));
#99633=CARTESIAN_POINT('',(52.0557535938712,13.375,25.5));
#99634=CARTESIAN_POINT('Origin',(52.4470215957073,14.45,25.5));
#99635=CARTESIAN_POINT('',(52.4470215957073,14.45,25.5));
#99636=CARTESIAN_POINT('',(52.4470215957073,14.45,25.5));
#99637=CARTESIAN_POINT('',(52.4470215957073,14.45,31.5));
#99638=CARTESIAN_POINT('',(52.4470215957073,14.45,31.5));
#99639=CARTESIAN_POINT('',(52.4470215957073,14.45,25.5));
#99640=CARTESIAN_POINT('Origin',(52.8848465482652,14.45,25.5));
#99641=CARTESIAN_POINT('',(52.8848465482652,14.45,25.5));
#99642=CARTESIAN_POINT('',(52.8848465482652,14.45,25.5));
#99643=CARTESIAN_POINT('',(52.8848465482652,14.45,31.5));
#99644=CARTESIAN_POINT('',(52.8848465482652,14.45,31.5));
#99645=CARTESIAN_POINT('',(52.8848465482652,14.45,25.5));
#99646=CARTESIAN_POINT('Origin',(53.2761145501014,13.375,25.5));
#99647=CARTESIAN_POINT('',(53.2761145501014,13.375,25.5));
#99648=CARTESIAN_POINT('',(53.2761145501014,13.375,25.5));
#99649=CARTESIAN_POINT('',(53.2761145501014,13.375,31.5));
#99650=CARTESIAN_POINT('',(53.2761145501014,13.375,31.5));
#99651=CARTESIAN_POINT('',(53.2761145501014,13.375,25.5));
#99652=CARTESIAN_POINT('Origin',(53.6265499206661,13.375,25.5));
#99653=CARTESIAN_POINT('',(53.6265499206661,13.375,25.5));
#99654=CARTESIAN_POINT('',(53.6265499206661,13.375,25.5));
#99655=CARTESIAN_POINT('',(53.6265499206661,13.375,31.5));
#99656=CARTESIAN_POINT('',(53.6265499206661,13.375,31.5));
#99657=CARTESIAN_POINT('',(53.6265499206661,13.375,25.5));
#99658=CARTESIAN_POINT('Origin',(54.0178179225022,14.45,25.5));
#99659=CARTESIAN_POINT('',(54.0178179225022,14.45,25.5));
#99660=CARTESIAN_POINT('',(54.0178179225022,14.45,25.5));
#99661=CARTESIAN_POINT('',(54.0178179225022,14.45,31.5));
#99662=CARTESIAN_POINT('',(54.0178179225022,14.45,31.5));
#99663=CARTESIAN_POINT('',(54.0178179225022,14.45,25.5));
#99664=CARTESIAN_POINT('Origin',(54.4556428750601,14.45,25.5));
#99665=CARTESIAN_POINT('',(54.4556428750601,14.45,25.5));
#99666=CARTESIAN_POINT('',(54.4556428750601,14.45,25.5));
#99667=CARTESIAN_POINT('',(54.4556428750601,14.45,31.5));
#99668=CARTESIAN_POINT('',(54.4556428750601,14.45,31.5));
#99669=CARTESIAN_POINT('',(54.4556428750601,14.45,25.5));
#99670=CARTESIAN_POINT('Origin',(54.8469108768963,13.375,25.5));
#99671=CARTESIAN_POINT('',(54.8469108768963,13.375,25.5));
#99672=CARTESIAN_POINT('',(54.8469108768963,13.375,25.5));
#99673=CARTESIAN_POINT('',(54.8469108768963,13.375,31.5));
#99674=CARTESIAN_POINT('',(54.8469108768963,13.375,31.5));
#99675=CARTESIAN_POINT('',(54.8469108768963,13.375,25.5));
#99676=CARTESIAN_POINT('Origin',(55.197346247461,13.375,25.5));
#99677=CARTESIAN_POINT('',(55.197346247461,13.375,25.5));
#99678=CARTESIAN_POINT('',(55.197346247461,13.375,25.5));
#99679=CARTESIAN_POINT('',(55.197346247461,13.375,31.5));
#99680=CARTESIAN_POINT('',(55.197346247461,13.375,31.5));
#99681=CARTESIAN_POINT('',(55.197346247461,13.375,25.5));
#99682=CARTESIAN_POINT('Origin',(55.5886142492971,14.45,25.5));
#99683=CARTESIAN_POINT('',(55.5886142492971,14.45,25.5));
#99684=CARTESIAN_POINT('',(55.5886142492971,14.45,25.5));
#99685=CARTESIAN_POINT('',(55.5886142492971,14.45,31.5));
#99686=CARTESIAN_POINT('',(55.5886142492971,14.45,31.5));
#99687=CARTESIAN_POINT('',(55.5886142492971,14.45,25.5));
#99688=CARTESIAN_POINT('Origin',(56.026439201855,14.45,25.5));
#99689=CARTESIAN_POINT('',(56.026439201855,14.45,25.5));
#99690=CARTESIAN_POINT('',(56.026439201855,14.45,25.5));
#99691=CARTESIAN_POINT('',(56.026439201855,14.45,31.5));
#99692=CARTESIAN_POINT('',(56.026439201855,14.45,31.5));
#99693=CARTESIAN_POINT('',(56.026439201855,14.45,25.5));
#99694=CARTESIAN_POINT('Origin',(56.4177072036912,13.375,25.5));
#99695=CARTESIAN_POINT('',(56.4177072036912,13.375,25.5));
#99696=CARTESIAN_POINT('',(56.4177072036912,13.375,25.5));
#99697=CARTESIAN_POINT('',(56.4177072036912,13.375,31.5));
#99698=CARTESIAN_POINT('',(56.4177072036912,13.375,31.5));
#99699=CARTESIAN_POINT('',(56.4177072036912,13.375,25.5));
#99700=CARTESIAN_POINT('Origin',(56.7681425742559,13.375,25.5));
#99701=CARTESIAN_POINT('',(56.7681425742559,13.375,25.5));
#99702=CARTESIAN_POINT('',(56.7681425742559,13.375,25.5));
#99703=CARTESIAN_POINT('',(56.7681425742559,13.375,31.5));
#99704=CARTESIAN_POINT('',(56.7681425742559,13.375,31.5));
#99705=CARTESIAN_POINT('',(56.7681425742559,13.375,25.5));
#99706=CARTESIAN_POINT('Origin',(57.159410576092,14.45,25.5));
#99707=CARTESIAN_POINT('',(57.159410576092,14.45,25.5));
#99708=CARTESIAN_POINT('',(57.159410576092,14.45,25.5));
#99709=CARTESIAN_POINT('',(57.159410576092,14.45,31.5));
#99710=CARTESIAN_POINT('',(57.159410576092,14.45,31.5));
#99711=CARTESIAN_POINT('',(57.159410576092,14.45,25.5));
#99712=CARTESIAN_POINT('Origin',(57.5972355286499,14.45,25.5));
#99713=CARTESIAN_POINT('',(57.5972355286499,14.45,25.5));
#99714=CARTESIAN_POINT('',(57.5972355286499,14.45,25.5));
#99715=CARTESIAN_POINT('',(57.5972355286499,14.45,31.5));
#99716=CARTESIAN_POINT('',(57.5972355286499,14.45,31.5));
#99717=CARTESIAN_POINT('',(57.5972355286499,14.45,25.5));
#99718=CARTESIAN_POINT('Origin',(57.9885035304861,13.375,25.5));
#99719=CARTESIAN_POINT('',(57.9885035304861,13.375,25.5));
#99720=CARTESIAN_POINT('',(57.9885035304861,13.375,25.5));
#99721=CARTESIAN_POINT('',(57.9885035304861,13.375,31.5));
#99722=CARTESIAN_POINT('',(57.9885035304861,13.375,31.5));
#99723=CARTESIAN_POINT('',(57.9885035304861,13.375,25.5));
#99724=CARTESIAN_POINT('Origin',(58.3389389010508,13.375,25.5));
#99725=CARTESIAN_POINT('',(58.3389389010508,13.375,25.5));
#99726=CARTESIAN_POINT('',(58.3389389010508,13.375,25.5));
#99727=CARTESIAN_POINT('',(58.3389389010508,13.375,31.5));
#99728=CARTESIAN_POINT('',(58.3389389010508,13.375,31.5));
#99729=CARTESIAN_POINT('',(58.3389389010508,13.375,25.5));
#99730=CARTESIAN_POINT('Origin',(58.7302069028869,14.45,25.5));
#99731=CARTESIAN_POINT('',(58.7302069028869,14.45,25.5));
#99732=CARTESIAN_POINT('',(58.7302069028869,14.45,25.5));
#99733=CARTESIAN_POINT('',(58.7302069028869,14.45,31.5));
#99734=CARTESIAN_POINT('',(58.7302069028869,14.45,31.5));
#99735=CARTESIAN_POINT('',(58.7302069028869,14.45,25.5));
#99736=CARTESIAN_POINT('Origin',(59.1680318554448,14.45,25.5));
#99737=CARTESIAN_POINT('',(59.1680318554448,14.45,25.5));
#99738=CARTESIAN_POINT('',(59.1680318554448,14.45,25.5));
#99739=CARTESIAN_POINT('',(59.1680318554448,14.45,31.5));
#99740=CARTESIAN_POINT('',(59.1680318554448,14.45,31.5));
#99741=CARTESIAN_POINT('',(59.1680318554448,14.45,25.5));
#99742=CARTESIAN_POINT('Origin',(59.559299857281,13.375,25.5));
#99743=CARTESIAN_POINT('',(59.559299857281,13.375,25.5));
#99744=CARTESIAN_POINT('',(59.559299857281,13.375,25.5));
#99745=CARTESIAN_POINT('',(59.559299857281,13.375,31.5));
#99746=CARTESIAN_POINT('',(59.559299857281,13.375,31.5));
#99747=CARTESIAN_POINT('',(59.559299857281,13.375,25.5));
#99748=CARTESIAN_POINT('Origin',(59.9097352278457,13.375,25.5));
#99749=CARTESIAN_POINT('',(59.9097352278457,13.375,25.5));
#99750=CARTESIAN_POINT('',(59.9097352278457,13.375,25.5));
#99751=CARTESIAN_POINT('',(59.9097352278457,13.375,31.5));
#99752=CARTESIAN_POINT('',(59.9097352278457,13.375,31.5));
#99753=CARTESIAN_POINT('',(59.9097352278457,13.375,25.5));
#99754=CARTESIAN_POINT('Origin',(60.3010032296818,14.45,25.5));
#99755=CARTESIAN_POINT('',(60.3010032296818,14.45,25.5));
#99756=CARTESIAN_POINT('',(60.3010032296818,14.45,25.5));
#99757=CARTESIAN_POINT('',(60.3010032296818,14.45,31.5));
#99758=CARTESIAN_POINT('',(60.3010032296818,14.45,31.5));
#99759=CARTESIAN_POINT('',(60.3010032296818,14.45,25.5));
#99760=CARTESIAN_POINT('Origin',(60.7388281822397,14.45,25.5));
#99761=CARTESIAN_POINT('',(60.7388281822397,14.45,25.5));
#99762=CARTESIAN_POINT('',(60.7388281822397,14.45,25.5));
#99763=CARTESIAN_POINT('',(60.7388281822397,14.45,31.5));
#99764=CARTESIAN_POINT('',(60.7388281822397,14.45,31.5));
#99765=CARTESIAN_POINT('',(60.7388281822397,14.45,25.5));
#99766=CARTESIAN_POINT('Origin',(61.1300961840759,13.375,25.5));
#99767=CARTESIAN_POINT('',(61.1300961840759,13.375,25.5));
#99768=CARTESIAN_POINT('',(61.1300961840759,13.375,25.5));
#99769=CARTESIAN_POINT('',(61.1300961840759,13.375,31.5));
#99770=CARTESIAN_POINT('',(61.1300961840759,13.375,31.5));
#99771=CARTESIAN_POINT('',(61.1300961840759,13.375,25.5));
#99772=CARTESIAN_POINT('Origin',(61.4805315546406,13.375,25.5));
#99773=CARTESIAN_POINT('',(61.4805315546406,13.375,25.5));
#99774=CARTESIAN_POINT('',(61.4805315546406,13.375,25.5));
#99775=CARTESIAN_POINT('',(61.4805315546406,13.375,31.5));
#99776=CARTESIAN_POINT('',(61.4805315546406,13.375,31.5));
#99777=CARTESIAN_POINT('',(61.4805315546406,13.375,25.5));
#99778=CARTESIAN_POINT('Origin',(61.8717995564767,14.45,25.5));
#99779=CARTESIAN_POINT('',(61.8717995564767,14.45,25.5));
#99780=CARTESIAN_POINT('',(61.8717995564767,14.45,25.5));
#99781=CARTESIAN_POINT('',(61.8717995564767,14.45,31.5));
#99782=CARTESIAN_POINT('',(61.8717995564767,14.45,31.5));
#99783=CARTESIAN_POINT('',(61.8717995564767,14.45,25.5));
#99784=CARTESIAN_POINT('Origin',(62.3096245090346,14.45,25.5));
#99785=CARTESIAN_POINT('',(62.3096245090346,14.45,25.5));
#99786=CARTESIAN_POINT('',(62.3096245090346,14.45,25.5));
#99787=CARTESIAN_POINT('',(62.3096245090346,14.45,31.5));
#99788=CARTESIAN_POINT('',(62.3096245090346,14.45,31.5));
#99789=CARTESIAN_POINT('',(62.3096245090346,14.45,25.5));
#99790=CARTESIAN_POINT('Origin',(62.7008925108708,13.375,25.5));
#99791=CARTESIAN_POINT('',(62.7008925108708,13.375,25.5));
#99792=CARTESIAN_POINT('',(62.7008925108708,13.375,25.5));
#99793=CARTESIAN_POINT('',(62.7008925108708,13.375,31.5));
#99794=CARTESIAN_POINT('',(62.7008925108708,13.375,31.5));
#99795=CARTESIAN_POINT('',(62.7008925108708,13.375,25.5));
#99796=CARTESIAN_POINT('Origin',(63.0513278814355,13.375,25.5));
#99797=CARTESIAN_POINT('',(63.0513278814355,13.375,25.5));
#99798=CARTESIAN_POINT('',(63.0513278814355,13.375,25.5));
#99799=CARTESIAN_POINT('',(63.0513278814355,13.375,31.5));
#99800=CARTESIAN_POINT('',(63.0513278814355,13.375,31.5));
#99801=CARTESIAN_POINT('',(63.0513278814355,13.375,25.5));
#99802=CARTESIAN_POINT('Origin',(63.4425958832716,14.45,25.5));
#99803=CARTESIAN_POINT('',(63.4425958832716,14.45,25.5));
#99804=CARTESIAN_POINT('',(63.4425958832716,14.45,25.5));
#99805=CARTESIAN_POINT('',(63.4425958832716,14.45,31.5));
#99806=CARTESIAN_POINT('',(63.4425958832716,14.45,31.5));
#99807=CARTESIAN_POINT('',(63.4425958832716,14.45,25.5));
#99808=CARTESIAN_POINT('Origin',(63.8804208358295,14.45,25.5));
#99809=CARTESIAN_POINT('',(63.8804208358295,14.45,25.5));
#99810=CARTESIAN_POINT('',(63.8804208358295,14.45,25.5));
#99811=CARTESIAN_POINT('',(63.8804208358295,14.45,31.5));
#99812=CARTESIAN_POINT('',(63.8804208358295,14.45,31.5));
#99813=CARTESIAN_POINT('',(63.8804208358295,14.45,25.5));
#99814=CARTESIAN_POINT('Origin',(64.2716888376656,13.375,25.5));
#99815=CARTESIAN_POINT('',(64.2716888376656,13.375,25.5));
#99816=CARTESIAN_POINT('',(64.2716888376656,13.375,25.5));
#99817=CARTESIAN_POINT('',(64.2716888376656,13.375,31.5));
#99818=CARTESIAN_POINT('',(64.2716888376656,13.375,31.5));
#99819=CARTESIAN_POINT('',(64.2716888376656,13.375,25.5));
#99820=CARTESIAN_POINT('Origin',(64.6221242082303,13.375,25.5));
#99821=CARTESIAN_POINT('',(64.6221242082303,13.375,25.5));
#99822=CARTESIAN_POINT('',(64.6221242082303,13.375,25.5));
#99823=CARTESIAN_POINT('',(64.6221242082303,13.375,31.5));
#99824=CARTESIAN_POINT('',(64.6221242082303,13.375,31.5));
#99825=CARTESIAN_POINT('',(64.6221242082303,13.375,25.5));
#99826=CARTESIAN_POINT('Origin',(65.0133922100665,14.45,25.5));
#99827=CARTESIAN_POINT('',(65.0133922100665,14.45,25.5));
#99828=CARTESIAN_POINT('',(65.0133922100665,14.45,25.5));
#99829=CARTESIAN_POINT('',(65.0133922100665,14.45,31.5));
#99830=CARTESIAN_POINT('',(65.0133922100665,14.45,31.5));
#99831=CARTESIAN_POINT('',(65.0133922100665,14.45,25.5));
#99832=CARTESIAN_POINT('Origin',(65.4512171626244,14.45,25.5));
#99833=CARTESIAN_POINT('',(65.4512171626244,14.45,25.5));
#99834=CARTESIAN_POINT('',(65.4512171626244,14.45,25.5));
#99835=CARTESIAN_POINT('',(65.4512171626244,14.45,31.5));
#99836=CARTESIAN_POINT('',(65.4512171626244,14.45,31.5));
#99837=CARTESIAN_POINT('',(65.4512171626244,14.45,25.5));
#99838=CARTESIAN_POINT('Origin',(65.8424851644606,13.375,25.5));
#99839=CARTESIAN_POINT('',(65.8424851644606,13.375,25.5));
#99840=CARTESIAN_POINT('',(65.8424851644606,13.375,25.5));
#99841=CARTESIAN_POINT('',(65.8424851644606,13.375,31.5));
#99842=CARTESIAN_POINT('',(65.8424851644606,13.375,31.5));
#99843=CARTESIAN_POINT('',(65.8424851644606,13.375,25.5));
#99844=CARTESIAN_POINT('Origin',(66.1929205350253,13.375,25.5));
#99845=CARTESIAN_POINT('',(66.1929205350253,13.375,25.5));
#99846=CARTESIAN_POINT('',(66.1929205350253,13.375,25.5));
#99847=CARTESIAN_POINT('',(66.1929205350253,13.375,31.5));
#99848=CARTESIAN_POINT('',(66.1929205350253,13.375,31.5));
#99849=CARTESIAN_POINT('',(66.1929205350253,13.375,25.5));
#99850=CARTESIAN_POINT('Origin',(66.5841885368614,14.45,25.5));
#99851=CARTESIAN_POINT('',(66.5841885368614,14.45,25.5));
#99852=CARTESIAN_POINT('',(66.5841885368614,14.45,25.5));
#99853=CARTESIAN_POINT('',(66.5841885368614,14.45,31.5));
#99854=CARTESIAN_POINT('',(66.5841885368614,14.45,31.5));
#99855=CARTESIAN_POINT('',(66.5841885368614,14.45,25.5));
#99856=CARTESIAN_POINT('Origin',(67.0220134894193,14.45,25.5));
#99857=CARTESIAN_POINT('',(67.0220134894193,14.45,25.5));
#99858=CARTESIAN_POINT('',(67.0220134894193,14.45,25.5));
#99859=CARTESIAN_POINT('',(67.0220134894193,14.45,31.5));
#99860=CARTESIAN_POINT('',(67.0220134894193,14.45,31.5));
#99861=CARTESIAN_POINT('',(67.0220134894193,14.45,25.5));
#99862=CARTESIAN_POINT('Origin',(67.4132814912554,13.375,25.5));
#99863=CARTESIAN_POINT('',(67.4132814912554,13.375,25.5));
#99864=CARTESIAN_POINT('',(67.4132814912554,13.375,25.5));
#99865=CARTESIAN_POINT('',(67.4132814912554,13.375,31.5));
#99866=CARTESIAN_POINT('',(67.4132814912554,13.375,31.5));
#99867=CARTESIAN_POINT('',(67.4132814912554,13.375,25.5));
#99868=CARTESIAN_POINT('Origin',(67.7637168618201,13.375,25.5));
#99869=CARTESIAN_POINT('',(67.7637168618201,13.375,25.5));
#99870=CARTESIAN_POINT('',(67.7637168618201,13.375,25.5));
#99871=CARTESIAN_POINT('',(67.7637168618201,13.375,31.5));
#99872=CARTESIAN_POINT('',(67.7637168618201,13.375,31.5));
#99873=CARTESIAN_POINT('',(67.7637168618201,13.375,25.5));
#99874=CARTESIAN_POINT('Origin',(68.1549848636563,14.45,25.5));
#99875=CARTESIAN_POINT('',(68.1549848636563,14.45,25.5));
#99876=CARTESIAN_POINT('',(68.1549848636563,14.45,25.5));
#99877=CARTESIAN_POINT('',(68.1549848636563,14.45,31.5));
#99878=CARTESIAN_POINT('',(68.1549848636563,14.45,31.5));
#99879=CARTESIAN_POINT('',(68.1549848636563,14.45,25.5));
#99880=CARTESIAN_POINT('Origin',(68.5928098162142,14.45,25.5));
#99881=CARTESIAN_POINT('',(68.5928098162142,14.45,25.5));
#99882=CARTESIAN_POINT('',(68.5928098162142,14.45,25.5));
#99883=CARTESIAN_POINT('',(68.5928098162142,14.45,31.5));
#99884=CARTESIAN_POINT('',(68.5928098162142,14.45,31.5));
#99885=CARTESIAN_POINT('',(68.5928098162142,14.45,25.5));
#99886=CARTESIAN_POINT('Origin',(68.9840778180503,13.375,25.5));
#99887=CARTESIAN_POINT('',(68.9840778180503,13.375,25.5));
#99888=CARTESIAN_POINT('',(68.9840778180503,13.375,25.5));
#99889=CARTESIAN_POINT('',(68.9840778180503,13.375,31.5));
#99890=CARTESIAN_POINT('',(68.9840778180503,13.375,31.5));
#99891=CARTESIAN_POINT('',(68.9840778180503,13.375,25.5));
#99892=CARTESIAN_POINT('Origin',(69.334513188615,13.375,25.5));
#99893=CARTESIAN_POINT('',(69.334513188615,13.375,25.5));
#99894=CARTESIAN_POINT('',(69.334513188615,13.375,25.5));
#99895=CARTESIAN_POINT('',(69.334513188615,13.375,31.5));
#99896=CARTESIAN_POINT('',(69.334513188615,13.375,31.5));
#99897=CARTESIAN_POINT('',(69.334513188615,13.375,25.5));
#99898=CARTESIAN_POINT('Origin',(69.7257811904512,14.45,25.5));
#99899=CARTESIAN_POINT('',(69.7257811904512,14.45,25.5));
#99900=CARTESIAN_POINT('',(69.7257811904512,14.45,25.5));
#99901=CARTESIAN_POINT('',(69.7257811904512,14.45,31.5));
#99902=CARTESIAN_POINT('',(69.7257811904512,14.45,31.5));
#99903=CARTESIAN_POINT('',(69.7257811904512,14.45,25.5));
#99904=CARTESIAN_POINT('Origin',(70.1636061430091,14.45,25.5));
#99905=CARTESIAN_POINT('',(70.1636061430091,14.45,25.5));
#99906=CARTESIAN_POINT('',(70.1636061430091,14.45,25.5));
#99907=CARTESIAN_POINT('',(70.1636061430091,14.45,31.5));
#99908=CARTESIAN_POINT('',(70.1636061430091,14.45,31.5));
#99909=CARTESIAN_POINT('',(70.1636061430091,14.45,25.5));
#99910=CARTESIAN_POINT('Origin',(70.5548741448452,13.375,25.5));
#99911=CARTESIAN_POINT('',(70.5548741448452,13.375,25.5));
#99912=CARTESIAN_POINT('',(70.5548741448452,13.375,25.5));
#99913=CARTESIAN_POINT('',(70.5548741448452,13.375,31.5));
#99914=CARTESIAN_POINT('',(70.5548741448452,13.375,31.5));
#99915=CARTESIAN_POINT('',(70.5548741448452,13.375,25.5));
#99916=CARTESIAN_POINT('Origin',(70.9053095154099,13.375,25.5));
#99917=CARTESIAN_POINT('',(70.9053095154099,13.375,25.5));
#99918=CARTESIAN_POINT('',(70.9053095154099,13.375,25.5));
#99919=CARTESIAN_POINT('',(70.9053095154099,13.375,31.5));
#99920=CARTESIAN_POINT('',(70.9053095154099,13.375,31.5));
#99921=CARTESIAN_POINT('',(70.9053095154099,13.375,25.5));
#99922=CARTESIAN_POINT('Origin',(71.2965775172461,14.45,25.5));
#99923=CARTESIAN_POINT('',(71.2965775172461,14.45,25.5));
#99924=CARTESIAN_POINT('',(71.2965775172461,14.45,25.5));
#99925=CARTESIAN_POINT('',(71.2965775172461,14.45,31.5));
#99926=CARTESIAN_POINT('',(71.2965775172461,14.45,31.5));
#99927=CARTESIAN_POINT('',(71.2965775172461,14.45,25.5));
#99928=CARTESIAN_POINT('Origin',(71.734402469804,14.45,25.5));
#99929=CARTESIAN_POINT('',(71.734402469804,14.45,25.5));
#99930=CARTESIAN_POINT('',(71.734402469804,14.45,25.5));
#99931=CARTESIAN_POINT('',(71.734402469804,14.45,31.5));
#99932=CARTESIAN_POINT('',(71.734402469804,14.45,31.5));
#99933=CARTESIAN_POINT('',(71.734402469804,14.45,25.5));
#99934=CARTESIAN_POINT('Origin',(72.1256704716401,13.375,25.5));
#99935=CARTESIAN_POINT('',(72.1256704716401,13.375,25.5));
#99936=CARTESIAN_POINT('',(72.1256704716401,13.375,25.5));
#99937=CARTESIAN_POINT('',(72.1256704716401,13.375,31.5));
#99938=CARTESIAN_POINT('',(72.1256704716401,13.375,31.5));
#99939=CARTESIAN_POINT('',(72.1256704716401,13.375,25.5));
#99940=CARTESIAN_POINT('Origin',(72.4761058422048,13.375,25.5));
#99941=CARTESIAN_POINT('',(72.4761058422048,13.375,25.5));
#99942=CARTESIAN_POINT('',(72.4761058422048,13.375,25.5));
#99943=CARTESIAN_POINT('',(72.4761058422048,13.375,31.5));
#99944=CARTESIAN_POINT('',(72.4761058422048,13.375,31.5));
#99945=CARTESIAN_POINT('',(72.4761058422048,13.375,25.5));
#99946=CARTESIAN_POINT('Origin',(72.867373844041,14.45,25.5));
#99947=CARTESIAN_POINT('',(72.867373844041,14.45,25.5));
#99948=CARTESIAN_POINT('',(72.867373844041,14.45,25.5));
#99949=CARTESIAN_POINT('',(72.867373844041,14.45,31.5));
#99950=CARTESIAN_POINT('',(72.867373844041,14.45,31.5));
#99951=CARTESIAN_POINT('',(72.867373844041,14.45,25.5));
#99952=CARTESIAN_POINT('Origin',(73.3051987965989,14.45,25.5));
#99953=CARTESIAN_POINT('',(73.3051987965989,14.45,25.5));
#99954=CARTESIAN_POINT('',(73.3051987965989,14.45,25.5));
#99955=CARTESIAN_POINT('',(73.3051987965989,14.45,31.5));
#99956=CARTESIAN_POINT('',(73.3051987965989,14.45,31.5));
#99957=CARTESIAN_POINT('',(73.3051987965989,14.45,25.5));
#99958=CARTESIAN_POINT('Origin',(73.696466798435,13.375,25.5));
#99959=CARTESIAN_POINT('',(73.696466798435,13.375,25.5));
#99960=CARTESIAN_POINT('',(73.696466798435,13.375,25.5));
#99961=CARTESIAN_POINT('',(73.696466798435,13.375,31.5));
#99962=CARTESIAN_POINT('',(73.696466798435,13.375,31.5));
#99963=CARTESIAN_POINT('',(73.696466798435,13.375,25.5));
#99964=CARTESIAN_POINT('Origin',(74.0469021689997,13.375,25.5));
#99965=CARTESIAN_POINT('',(74.0469021689997,13.375,25.5));
#99966=CARTESIAN_POINT('',(74.0469021689997,13.375,25.5));
#99967=CARTESIAN_POINT('',(74.0469021689997,13.375,31.5));
#99968=CARTESIAN_POINT('',(74.0469021689997,13.375,31.5));
#99969=CARTESIAN_POINT('',(74.0469021689997,13.375,25.5));
#99970=CARTESIAN_POINT('Origin',(74.4381701708359,14.45,25.5));
#99971=CARTESIAN_POINT('',(74.4381701708359,14.45,25.5));
#99972=CARTESIAN_POINT('',(74.4381701708359,14.45,25.5));
#99973=CARTESIAN_POINT('',(74.4381701708359,14.45,31.5));
#99974=CARTESIAN_POINT('',(74.4381701708359,14.45,31.5));
#99975=CARTESIAN_POINT('',(74.4381701708359,14.45,25.5));
#99976=CARTESIAN_POINT('Origin',(74.8759951233938,14.45,25.5));
#99977=CARTESIAN_POINT('',(74.8759951233938,14.45,25.5));
#99978=CARTESIAN_POINT('',(74.8759951233938,14.45,25.5));
#99979=CARTESIAN_POINT('',(74.8759951233938,14.45,31.5));
#99980=CARTESIAN_POINT('',(74.8759951233938,14.45,31.5));
#99981=CARTESIAN_POINT('',(74.8759951233938,14.45,25.5));
#99982=CARTESIAN_POINT('Origin',(75.2672631252299,13.375,25.5));
#99983=CARTESIAN_POINT('',(75.2672631252299,13.375,25.5));
#99984=CARTESIAN_POINT('',(75.2672631252299,13.375,25.5));
#99985=CARTESIAN_POINT('',(75.2672631252299,13.375,31.5));
#99986=CARTESIAN_POINT('',(75.2672631252299,13.375,31.5));
#99987=CARTESIAN_POINT('',(75.2672631252299,13.375,25.5));
#99988=CARTESIAN_POINT('Origin',(75.6176984957946,13.375,25.5));
#99989=CARTESIAN_POINT('',(75.6176984957946,13.375,25.5));
#99990=CARTESIAN_POINT('',(75.6176984957946,13.375,25.5));
#99991=CARTESIAN_POINT('',(75.6176984957946,13.375,31.5));
#99992=CARTESIAN_POINT('',(75.6176984957946,13.375,31.5));
#99993=CARTESIAN_POINT('',(75.6176984957946,13.375,25.5));
#99994=CARTESIAN_POINT('Origin',(76.0089664976308,14.45,25.5));
#99995=CARTESIAN_POINT('',(76.0089664976308,14.45,25.5));
#99996=CARTESIAN_POINT('',(76.0089664976308,14.45,25.5));
#99997=CARTESIAN_POINT('',(76.0089664976308,14.45,31.5));
#99998=CARTESIAN_POINT('',(76.0089664976308,14.45,31.5));
#99999=CARTESIAN_POINT('',(76.0089664976308,14.45,25.5));
#100000=CARTESIAN_POINT('Origin',(76.4467914501887,14.45,25.5));
#100001=CARTESIAN_POINT('',(76.4467914501887,14.45,25.5));
#100002=CARTESIAN_POINT('',(76.4467914501887,14.45,25.5));
#100003=CARTESIAN_POINT('',(76.4467914501887,14.45,31.5));
#100004=CARTESIAN_POINT('',(76.4467914501887,14.45,31.5));
#100005=CARTESIAN_POINT('',(76.4467914501887,14.45,25.5));
#100006=CARTESIAN_POINT('Origin',(76.8380594520248,13.375,25.5));
#100007=CARTESIAN_POINT('',(76.8380594520248,13.375,25.5));
#100008=CARTESIAN_POINT('',(76.8380594520248,13.375,25.5));
#100009=CARTESIAN_POINT('',(76.8380594520248,13.375,31.5));
#100010=CARTESIAN_POINT('',(76.8380594520248,13.375,31.5));
#100011=CARTESIAN_POINT('',(76.8380594520248,13.375,25.5));
#100012=CARTESIAN_POINT('Origin',(77.1884948225895,13.375,25.5));
#100013=CARTESIAN_POINT('',(77.1884948225895,13.375,25.5));
#100014=CARTESIAN_POINT('',(77.1884948225895,13.375,25.5));
#100015=CARTESIAN_POINT('',(77.1884948225895,13.375,31.5));
#100016=CARTESIAN_POINT('',(77.1884948225895,13.375,31.5));
#100017=CARTESIAN_POINT('',(77.1884948225895,13.375,25.5));
#100018=CARTESIAN_POINT('Origin',(77.5797628244257,14.45,25.5));
#100019=CARTESIAN_POINT('',(77.5797628244257,14.45,25.5));
#100020=CARTESIAN_POINT('',(77.5797628244257,14.45,25.5));
#100021=CARTESIAN_POINT('',(77.5797628244257,14.45,31.5));
#100022=CARTESIAN_POINT('',(77.5797628244257,14.45,31.5));
#100023=CARTESIAN_POINT('',(77.5797628244257,14.45,25.5));
#100024=CARTESIAN_POINT('Origin',(78.0175877769835,14.45,25.5));
#100025=CARTESIAN_POINT('',(78.0175877769835,14.45,25.5));
#100026=CARTESIAN_POINT('',(78.0175877769835,14.45,25.5));
#100027=CARTESIAN_POINT('',(78.0175877769835,14.45,31.5));
#100028=CARTESIAN_POINT('',(78.0175877769835,14.45,31.5));
#100029=CARTESIAN_POINT('',(78.0175877769835,14.45,25.5));
#100030=CARTESIAN_POINT('Origin',(78.4088557788197,13.375,25.5));
#100031=CARTESIAN_POINT('',(78.4088557788197,13.375,25.5));
#100032=CARTESIAN_POINT('',(78.4088557788197,13.375,25.5));
#100033=CARTESIAN_POINT('',(78.4088557788197,13.375,31.5));
#100034=CARTESIAN_POINT('',(78.4088557788197,13.375,31.5));
#100035=CARTESIAN_POINT('',(78.4088557788197,13.375,25.5));
#100036=CARTESIAN_POINT('Origin',(78.7592911493844,13.375,25.5));
#100037=CARTESIAN_POINT('',(78.7592911493844,13.375,25.5));
#100038=CARTESIAN_POINT('',(78.7592911493844,13.375,25.5));
#100039=CARTESIAN_POINT('',(78.7592911493844,13.375,31.5));
#100040=CARTESIAN_POINT('',(78.7592911493844,13.375,31.5));
#100041=CARTESIAN_POINT('',(78.7592911493844,13.375,25.5));
#100042=CARTESIAN_POINT('Origin',(79.1505591512206,14.45,25.5));
#100043=CARTESIAN_POINT('',(79.1505591512206,14.45,25.5));
#100044=CARTESIAN_POINT('',(79.1505591512206,14.45,25.5));
#100045=CARTESIAN_POINT('',(79.1505591512206,14.45,31.5));
#100046=CARTESIAN_POINT('',(79.1505591512206,14.45,31.5));
#100047=CARTESIAN_POINT('',(79.1505591512206,14.45,25.5));
#100048=CARTESIAN_POINT('Origin',(79.5883841037785,14.45,25.5));
#100049=CARTESIAN_POINT('',(79.5883841037785,14.45,25.5));
#100050=CARTESIAN_POINT('',(79.5883841037785,14.45,25.5));
#100051=CARTESIAN_POINT('',(79.5883841037785,14.45,31.5));
#100052=CARTESIAN_POINT('',(79.5883841037785,14.45,31.5));
#100053=CARTESIAN_POINT('',(79.5883841037785,14.45,25.5));
#100054=CARTESIAN_POINT('Origin',(79.9796521056146,13.375,25.5));
#100055=CARTESIAN_POINT('',(79.9796521056146,13.375,25.5));
#100056=CARTESIAN_POINT('',(79.9796521056146,13.375,25.5));
#100057=CARTESIAN_POINT('',(79.9796521056146,13.375,31.5));
#100058=CARTESIAN_POINT('',(79.9796521056146,13.375,31.5));
#100059=CARTESIAN_POINT('',(79.9796521056146,13.375,25.5));
#100060=CARTESIAN_POINT('Origin',(80.3300874761793,13.375,25.5));
#100061=CARTESIAN_POINT('',(80.3300874761793,13.375,25.5));
#100062=CARTESIAN_POINT('',(80.3300874761793,13.375,25.5));
#100063=CARTESIAN_POINT('',(80.3300874761793,13.375,31.5));
#100064=CARTESIAN_POINT('',(80.3300874761793,13.375,31.5));
#100065=CARTESIAN_POINT('',(80.3300874761793,13.375,25.5));
#100066=CARTESIAN_POINT('Origin',(80.7213554780155,14.45,25.5));
#100067=CARTESIAN_POINT('',(80.7213554780155,14.45,25.5));
#100068=CARTESIAN_POINT('',(80.7213554780155,14.45,25.5));
#100069=CARTESIAN_POINT('',(80.7213554780155,14.45,31.5));
#100070=CARTESIAN_POINT('',(80.7213554780155,14.45,31.5));
#100071=CARTESIAN_POINT('',(80.7213554780155,14.45,25.5));
#100072=CARTESIAN_POINT('Origin',(81.1591804305733,14.45,25.5));
#100073=CARTESIAN_POINT('',(81.1591804305733,14.45,25.5));
#100074=CARTESIAN_POINT('',(81.1591804305733,14.45,25.5));
#100075=CARTESIAN_POINT('',(81.1591804305733,14.45,31.5));
#100076=CARTESIAN_POINT('',(81.1591804305733,14.45,31.5));
#100077=CARTESIAN_POINT('',(81.1591804305733,14.45,25.5));
#100078=CARTESIAN_POINT('Origin',(81.5504484324095,13.375,25.5));
#100079=CARTESIAN_POINT('',(81.5504484324095,13.375,25.5));
#100080=CARTESIAN_POINT('',(81.5504484324095,13.375,25.5));
#100081=CARTESIAN_POINT('',(81.5504484324095,13.375,31.5));
#100082=CARTESIAN_POINT('',(81.5504484324095,13.375,31.5));
#100083=CARTESIAN_POINT('',(81.5504484324095,13.375,25.5));
#100084=CARTESIAN_POINT('Origin',(81.9008838029742,13.375,25.5));
#100085=CARTESIAN_POINT('',(81.9008838029742,13.375,25.5));
#100086=CARTESIAN_POINT('',(81.9008838029742,13.375,25.5));
#100087=CARTESIAN_POINT('',(81.9008838029742,13.375,31.5));
#100088=CARTESIAN_POINT('',(81.9008838029742,13.375,31.5));
#100089=CARTESIAN_POINT('',(81.9008838029742,13.375,25.5));
#100090=CARTESIAN_POINT('Origin',(82.2921518048104,14.45,25.5));
#100091=CARTESIAN_POINT('',(82.2921518048104,14.45,25.5));
#100092=CARTESIAN_POINT('',(82.2921518048104,14.45,25.5));
#100093=CARTESIAN_POINT('',(82.2921518048104,14.45,31.5));
#100094=CARTESIAN_POINT('',(82.2921518048104,14.45,31.5));
#100095=CARTESIAN_POINT('',(82.2921518048104,14.45,25.5));
#100096=CARTESIAN_POINT('Origin',(82.7299767573682,14.45,25.5));
#100097=CARTESIAN_POINT('',(82.7299767573682,14.45,25.5));
#100098=CARTESIAN_POINT('',(82.7299767573682,14.45,25.5));
#100099=CARTESIAN_POINT('',(82.7299767573682,14.45,31.5));
#100100=CARTESIAN_POINT('',(82.7299767573682,14.45,31.5));
#100101=CARTESIAN_POINT('',(82.7299767573682,14.45,25.5));
#100102=CARTESIAN_POINT('Origin',(83.1212447592044,13.375,25.5));
#100103=CARTESIAN_POINT('',(83.1212447592044,13.375,25.5));
#100104=CARTESIAN_POINT('',(83.1212447592044,13.375,25.5));
#100105=CARTESIAN_POINT('',(83.1212447592044,13.375,31.5));
#100106=CARTESIAN_POINT('',(83.1212447592044,13.375,31.5));
#100107=CARTESIAN_POINT('',(83.1212447592044,13.375,25.5));
#100108=CARTESIAN_POINT('Origin',(83.4716801297691,13.375,25.5));
#100109=CARTESIAN_POINT('',(83.4716801297691,13.375,25.5));
#100110=CARTESIAN_POINT('',(83.4716801297691,13.375,25.5));
#100111=CARTESIAN_POINT('',(83.4716801297691,13.375,31.5));
#100112=CARTESIAN_POINT('',(83.4716801297691,13.375,31.5));
#100113=CARTESIAN_POINT('',(83.4716801297691,13.375,25.5));
#100114=CARTESIAN_POINT('Origin',(83.8629481316053,14.45,25.5));
#100115=CARTESIAN_POINT('',(83.8629481316053,14.45,25.5));
#100116=CARTESIAN_POINT('',(83.8629481316053,14.45,25.5));
#100117=CARTESIAN_POINT('',(83.8629481316053,14.45,31.5));
#100118=CARTESIAN_POINT('',(83.8629481316053,14.45,31.5));
#100119=CARTESIAN_POINT('',(83.8629481316053,14.45,25.5));
#100120=CARTESIAN_POINT('Origin',(84.3007730841631,14.45,25.5));
#100121=CARTESIAN_POINT('',(84.3007730841631,14.45,25.5));
#100122=CARTESIAN_POINT('',(84.3007730841631,14.45,25.5));
#100123=CARTESIAN_POINT('',(84.3007730841631,14.45,31.5));
#100124=CARTESIAN_POINT('',(84.3007730841631,14.45,31.5));
#100125=CARTESIAN_POINT('',(84.3007730841631,14.45,25.5));
#100126=CARTESIAN_POINT('Origin',(84.6920410859993,13.375,25.5));
#100127=CARTESIAN_POINT('',(84.6920410859993,13.375,25.5));
#100128=CARTESIAN_POINT('',(84.6920410859993,13.375,25.5));
#100129=CARTESIAN_POINT('',(84.6920410859993,13.375,31.5));
#100130=CARTESIAN_POINT('',(84.6920410859993,13.375,31.5));
#100131=CARTESIAN_POINT('',(84.6920410859993,13.375,25.5));
#100132=CARTESIAN_POINT('Origin',(85.042476456564,13.375,25.5));
#100133=CARTESIAN_POINT('',(85.042476456564,13.375,25.5));
#100134=CARTESIAN_POINT('',(85.042476456564,13.375,25.5));
#100135=CARTESIAN_POINT('',(85.042476456564,13.375,31.5));
#100136=CARTESIAN_POINT('',(85.042476456564,13.375,31.5));
#100137=CARTESIAN_POINT('',(85.042476456564,13.375,25.5));
#100138=CARTESIAN_POINT('Origin',(85.4337444584002,14.45,25.5));
#100139=CARTESIAN_POINT('',(85.4337444584002,14.45,25.5));
#100140=CARTESIAN_POINT('',(85.4337444584002,14.45,25.5));
#100141=CARTESIAN_POINT('',(85.4337444584002,14.45,31.5));
#100142=CARTESIAN_POINT('',(85.4337444584002,14.45,31.5));
#100143=CARTESIAN_POINT('',(85.4337444584002,14.45,25.5));
#100144=CARTESIAN_POINT('Origin',(85.871569410958,14.45,25.5));
#100145=CARTESIAN_POINT('',(85.871569410958,14.45,25.5));
#100146=CARTESIAN_POINT('',(85.871569410958,14.45,25.5));
#100147=CARTESIAN_POINT('',(85.871569410958,14.45,31.5));
#100148=CARTESIAN_POINT('',(85.871569410958,14.45,31.5));
#100149=CARTESIAN_POINT('',(85.871569410958,14.45,25.5));
#100150=CARTESIAN_POINT('Origin',(86.2628374127942,13.375,25.5));
#100151=CARTESIAN_POINT('',(86.2628374127942,13.375,25.5));
#100152=CARTESIAN_POINT('',(86.2628374127942,13.375,25.5));
#100153=CARTESIAN_POINT('',(86.2628374127942,13.375,31.5));
#100154=CARTESIAN_POINT('',(86.2628374127942,13.375,31.5));
#100155=CARTESIAN_POINT('',(86.2628374127942,13.375,25.5));
#100156=CARTESIAN_POINT('Origin',(86.6132727833589,13.375,25.5));
#100157=CARTESIAN_POINT('',(86.6132727833589,13.375,25.5));
#100158=CARTESIAN_POINT('',(86.6132727833589,13.375,25.5));
#100159=CARTESIAN_POINT('',(86.6132727833589,13.375,31.5));
#100160=CARTESIAN_POINT('',(86.6132727833589,13.375,31.5));
#100161=CARTESIAN_POINT('',(86.6132727833589,13.375,25.5));
#100162=CARTESIAN_POINT('Origin',(87.0045407851951,14.45,25.5));
#100163=CARTESIAN_POINT('',(87.0045407851951,14.45,25.5));
#100164=CARTESIAN_POINT('',(87.0045407851951,14.45,25.5));
#100165=CARTESIAN_POINT('',(87.0045407851951,14.45,31.5));
#100166=CARTESIAN_POINT('',(87.0045407851951,14.45,31.5));
#100167=CARTESIAN_POINT('',(87.0045407851951,14.45,25.5));
#100168=CARTESIAN_POINT('Origin',(87.4423657377529,14.45,25.5));
#100169=CARTESIAN_POINT('',(87.4423657377529,14.45,25.5));
#100170=CARTESIAN_POINT('',(87.4423657377529,14.45,25.5));
#100171=CARTESIAN_POINT('',(87.4423657377529,14.45,31.5));
#100172=CARTESIAN_POINT('',(87.4423657377529,14.45,31.5));
#100173=CARTESIAN_POINT('',(87.4423657377529,14.45,25.5));
#100174=CARTESIAN_POINT('Origin',(87.8336337395891,13.375,25.5));
#100175=CARTESIAN_POINT('',(87.8336337395891,13.375,25.5));
#100176=CARTESIAN_POINT('',(87.8336337395891,13.375,25.5));
#100177=CARTESIAN_POINT('',(87.8336337395891,13.375,31.5));
#100178=CARTESIAN_POINT('',(87.8336337395891,13.375,31.5));
#100179=CARTESIAN_POINT('',(87.8336337395891,13.375,25.5));
#100180=CARTESIAN_POINT('Origin',(88.1840691101538,13.375,25.5));
#100181=CARTESIAN_POINT('',(88.1840691101538,13.375,25.5));
#100182=CARTESIAN_POINT('',(88.1840691101538,13.375,25.5));
#100183=CARTESIAN_POINT('',(88.1840691101538,13.375,31.5));
#100184=CARTESIAN_POINT('',(88.1840691101538,13.375,31.5));
#100185=CARTESIAN_POINT('',(88.1840691101538,13.375,25.5));
#100186=CARTESIAN_POINT('Origin',(88.57533711199,14.45,25.5));
#100187=CARTESIAN_POINT('',(88.57533711199,14.45,25.5));
#100188=CARTESIAN_POINT('',(88.57533711199,14.45,25.5));
#100189=CARTESIAN_POINT('',(88.57533711199,14.45,31.5));
#100190=CARTESIAN_POINT('',(88.57533711199,14.45,31.5));
#100191=CARTESIAN_POINT('',(88.57533711199,14.45,25.5));
#100192=CARTESIAN_POINT('Origin',(89.0131620645478,14.45,25.5));
#100193=CARTESIAN_POINT('',(89.0131620645478,14.45,25.5));
#100194=CARTESIAN_POINT('',(89.0131620645478,14.45,25.5));
#100195=CARTESIAN_POINT('',(89.0131620645478,14.45,31.5));
#100196=CARTESIAN_POINT('',(89.0131620645478,14.45,31.5));
#100197=CARTESIAN_POINT('',(89.0131620645478,14.45,25.5));
#100198=CARTESIAN_POINT('Origin',(89.404430066384,13.375,25.5));
#100199=CARTESIAN_POINT('',(89.404430066384,13.375,25.5));
#100200=CARTESIAN_POINT('',(89.404430066384,13.375,25.5));
#100201=CARTESIAN_POINT('',(89.404430066384,13.375,31.5));
#100202=CARTESIAN_POINT('',(89.404430066384,13.375,31.5));
#100203=CARTESIAN_POINT('',(89.404430066384,13.375,25.5));
#100204=CARTESIAN_POINT('Origin',(89.7548654369487,13.375,25.5));
#100205=CARTESIAN_POINT('',(89.7548654369487,13.375,25.5));
#100206=CARTESIAN_POINT('',(89.7548654369487,13.375,25.5));
#100207=CARTESIAN_POINT('',(89.7548654369487,13.375,31.5));
#100208=CARTESIAN_POINT('',(89.7548654369487,13.375,31.5));
#100209=CARTESIAN_POINT('',(89.7548654369487,13.375,25.5));
#100210=CARTESIAN_POINT('Origin',(90.1461334387849,14.45,25.5));
#100211=CARTESIAN_POINT('',(90.1461334387849,14.45,25.5));
#100212=CARTESIAN_POINT('',(90.1461334387849,14.45,25.5));
#100213=CARTESIAN_POINT('',(90.1461334387849,14.45,31.5));
#100214=CARTESIAN_POINT('',(90.1461334387849,14.45,31.5));
#100215=CARTESIAN_POINT('',(90.1461334387849,14.45,25.5));
#100216=CARTESIAN_POINT('Origin',(90.5839583913427,14.45,25.5));
#100217=CARTESIAN_POINT('',(90.5839583913427,14.45,25.5));
#100218=CARTESIAN_POINT('',(90.5839583913427,14.45,25.5));
#100219=CARTESIAN_POINT('',(90.5839583913427,14.45,31.5));
#100220=CARTESIAN_POINT('',(90.5839583913427,14.45,31.5));
#100221=CARTESIAN_POINT('',(90.5839583913427,14.45,25.5));
#100222=CARTESIAN_POINT('Origin',(90.9752263931789,13.375,25.5));
#100223=CARTESIAN_POINT('',(90.9752263931789,13.375,25.5));
#100224=CARTESIAN_POINT('',(90.9752263931789,13.375,25.5));
#100225=CARTESIAN_POINT('',(90.9752263931789,13.375,31.5));
#100226=CARTESIAN_POINT('',(90.9752263931789,13.375,31.5));
#100227=CARTESIAN_POINT('',(90.9752263931789,13.375,25.5));
#100228=CARTESIAN_POINT('Origin',(91.3256617637436,13.375,25.5));
#100229=CARTESIAN_POINT('',(91.3256617637436,13.375,25.5));
#100230=CARTESIAN_POINT('',(91.3256617637436,13.375,25.5));
#100231=CARTESIAN_POINT('',(91.3256617637436,13.375,31.5));
#100232=CARTESIAN_POINT('',(91.3256617637436,13.375,31.5));
#100233=CARTESIAN_POINT('',(91.3256617637436,13.375,25.5));
#100234=CARTESIAN_POINT('Origin',(91.7169297655798,14.45,25.5));
#100235=CARTESIAN_POINT('',(91.7169297655798,14.45,25.5));
#100236=CARTESIAN_POINT('',(91.7169297655798,14.45,25.5));
#100237=CARTESIAN_POINT('',(91.7169297655798,14.45,31.5));
#100238=CARTESIAN_POINT('',(91.7169297655798,14.45,31.5));
#100239=CARTESIAN_POINT('',(91.7169297655798,14.45,25.5));
#100240=CARTESIAN_POINT('Origin',(92.1547547181376,14.45,25.5));
#100241=CARTESIAN_POINT('',(92.1547547181376,14.45,25.5));
#100242=CARTESIAN_POINT('',(92.1547547181376,14.45,25.5));
#100243=CARTESIAN_POINT('',(92.1547547181376,14.45,31.5));
#100244=CARTESIAN_POINT('',(92.1547547181376,14.45,31.5));
#100245=CARTESIAN_POINT('',(92.1547547181376,14.45,25.5));
#100246=CARTESIAN_POINT('Origin',(92.5460227199738,13.375,25.5));
#100247=CARTESIAN_POINT('',(92.5460227199738,13.375,25.5));
#100248=CARTESIAN_POINT('',(92.5460227199738,13.375,25.5));
#100249=CARTESIAN_POINT('',(92.5460227199738,13.375,31.5));
#100250=CARTESIAN_POINT('',(92.5460227199738,13.375,31.5));
#100251=CARTESIAN_POINT('',(92.5460227199738,13.375,25.5));
#100252=CARTESIAN_POINT('Origin',(92.8964580905385,13.375,25.5));
#100253=CARTESIAN_POINT('',(92.8964580905385,13.375,25.5));
#100254=CARTESIAN_POINT('',(92.8964580905385,13.375,25.5));
#100255=CARTESIAN_POINT('',(92.8964580905385,13.375,31.5));
#100256=CARTESIAN_POINT('',(92.8964580905385,13.375,31.5));
#100257=CARTESIAN_POINT('',(92.8964580905385,13.375,25.5));
#100258=CARTESIAN_POINT('Origin',(93.2877260923746,14.45,25.5));
#100259=CARTESIAN_POINT('',(93.2877260923746,14.45,25.5));
#100260=CARTESIAN_POINT('',(93.2877260923746,14.45,25.5));
#100261=CARTESIAN_POINT('',(93.2877260923746,14.45,31.5));
#100262=CARTESIAN_POINT('',(93.2877260923746,14.45,31.5));
#100263=CARTESIAN_POINT('',(93.2877260923746,14.45,25.5));
#100264=CARTESIAN_POINT('Origin',(93.7255510449325,14.45,25.5));
#100265=CARTESIAN_POINT('',(93.7255510449325,14.45,25.5));
#100266=CARTESIAN_POINT('',(93.7255510449325,14.45,25.5));
#100267=CARTESIAN_POINT('',(93.7255510449325,14.45,31.5));
#100268=CARTESIAN_POINT('',(93.7255510449325,14.45,31.5));
#100269=CARTESIAN_POINT('',(93.7255510449325,14.45,25.5));
#100270=CARTESIAN_POINT('Origin',(94.1168190467687,13.375,25.5));
#100271=CARTESIAN_POINT('',(94.1168190467687,13.375,25.5));
#100272=CARTESIAN_POINT('',(94.1168190467687,13.375,25.5));
#100273=CARTESIAN_POINT('',(94.1168190467687,13.375,31.5));
#100274=CARTESIAN_POINT('',(94.1168190467687,13.375,31.5));
#100275=CARTESIAN_POINT('',(94.1168190467687,13.375,25.5));
#100276=CARTESIAN_POINT('Origin',(94.4672544173334,13.375,25.5));
#100277=CARTESIAN_POINT('',(94.4672544173334,13.375,25.5));
#100278=CARTESIAN_POINT('',(94.4672544173334,13.375,25.5));
#100279=CARTESIAN_POINT('',(94.4672544173334,13.375,31.5));
#100280=CARTESIAN_POINT('',(94.4672544173334,13.375,31.5));
#100281=CARTESIAN_POINT('',(94.4672544173334,13.375,25.5));
#100282=CARTESIAN_POINT('Origin',(94.8585224191696,14.45,25.5));
#100283=CARTESIAN_POINT('',(94.8585224191696,14.45,25.5));
#100284=CARTESIAN_POINT('',(94.8585224191696,14.45,25.5));
#100285=CARTESIAN_POINT('',(94.8585224191696,14.45,31.5));
#100286=CARTESIAN_POINT('',(94.8585224191696,14.45,31.5));
#100287=CARTESIAN_POINT('',(94.8585224191696,14.45,25.5));
#100288=CARTESIAN_POINT('Origin',(95.2963473717274,14.45,25.5));
#100289=CARTESIAN_POINT('',(95.2963473717274,14.45,25.5));
#100290=CARTESIAN_POINT('',(95.2963473717274,14.45,25.5));
#100291=CARTESIAN_POINT('',(95.2963473717274,14.45,31.5));
#100292=CARTESIAN_POINT('',(95.2963473717274,14.45,31.5));
#100293=CARTESIAN_POINT('',(95.2963473717274,14.45,25.5));
#100294=CARTESIAN_POINT('Origin',(95.6876153735636,13.375,25.5));
#100295=CARTESIAN_POINT('',(95.6876153735636,13.375,25.5));
#100296=CARTESIAN_POINT('',(95.6876153735636,13.375,25.5));
#100297=CARTESIAN_POINT('',(95.6876153735636,13.375,31.5));
#100298=CARTESIAN_POINT('',(95.6876153735636,13.375,31.5));
#100299=CARTESIAN_POINT('',(95.6876153735636,13.375,25.5));
#100300=CARTESIAN_POINT('Origin',(96.0380507441283,13.375,25.5));
#100301=CARTESIAN_POINT('',(96.0380507441283,13.375,25.5));
#100302=CARTESIAN_POINT('',(96.0380507441283,13.375,25.5));
#100303=CARTESIAN_POINT('',(96.0380507441283,13.375,31.5));
#100304=CARTESIAN_POINT('',(96.0380507441283,13.375,31.5));
#100305=CARTESIAN_POINT('',(96.0380507441283,13.375,25.5));
#100306=CARTESIAN_POINT('Origin',(96.4293187459645,14.45,25.5));
#100307=CARTESIAN_POINT('',(96.4293187459645,14.45,25.5));
#100308=CARTESIAN_POINT('',(96.4293187459645,14.45,25.5));
#100309=CARTESIAN_POINT('',(96.4293187459645,14.45,31.5));
#100310=CARTESIAN_POINT('',(96.4293187459645,14.45,31.5));
#100311=CARTESIAN_POINT('',(96.4293187459645,14.45,25.5));
#100312=CARTESIAN_POINT('Origin',(96.8671436985223,14.45,25.5));
#100313=CARTESIAN_POINT('',(96.8671436985223,14.45,25.5));
#100314=CARTESIAN_POINT('',(96.8671436985223,14.45,25.5));
#100315=CARTESIAN_POINT('',(96.8671436985223,14.45,31.5));
#100316=CARTESIAN_POINT('',(96.8671436985223,14.45,31.5));
#100317=CARTESIAN_POINT('',(96.8671436985223,14.45,25.5));
#100318=CARTESIAN_POINT('Origin',(97.2584117003585,13.375,25.5));
#100319=CARTESIAN_POINT('',(97.2584117003585,13.375,25.5));
#100320=CARTESIAN_POINT('',(97.2584117003585,13.375,25.5));
#100321=CARTESIAN_POINT('',(97.2584117003585,13.375,31.5));
#100322=CARTESIAN_POINT('',(97.2584117003585,13.375,31.5));
#100323=CARTESIAN_POINT('',(97.2584117003585,13.375,25.5));
#100324=CARTESIAN_POINT('Origin',(97.6088470709232,13.375,25.5));
#100325=CARTESIAN_POINT('',(97.6088470709232,13.375,25.5));
#100326=CARTESIAN_POINT('',(97.6088470709232,13.375,25.5));
#100327=CARTESIAN_POINT('',(97.6088470709232,13.375,31.5));
#100328=CARTESIAN_POINT('',(97.6088470709232,13.375,31.5));
#100329=CARTESIAN_POINT('',(97.6088470709232,13.375,25.5));
#100330=CARTESIAN_POINT('Origin',(98.0001150727593,14.45,25.5));
#100331=CARTESIAN_POINT('',(98.0001150727593,14.45,25.5));
#100332=CARTESIAN_POINT('',(98.0001150727593,14.45,25.5));
#100333=CARTESIAN_POINT('',(98.0001150727593,14.45,31.5));
#100334=CARTESIAN_POINT('',(98.0001150727593,14.45,31.5));
#100335=CARTESIAN_POINT('',(98.0001150727593,14.45,25.5));
#100336=CARTESIAN_POINT('Origin',(98.4379400253172,14.45,25.5));
#100337=CARTESIAN_POINT('',(98.4379400253172,14.45,25.5));
#100338=CARTESIAN_POINT('',(98.4379400253172,14.45,25.5));
#100339=CARTESIAN_POINT('',(98.4379400253172,14.45,31.5));
#100340=CARTESIAN_POINT('',(98.4379400253172,14.45,31.5));
#100341=CARTESIAN_POINT('',(98.4379400253172,14.45,25.5));
#100342=CARTESIAN_POINT('Origin',(98.8292080271534,13.375,25.5));
#100343=CARTESIAN_POINT('',(98.8292080271534,13.375,25.5));
#100344=CARTESIAN_POINT('',(98.8292080271534,13.375,25.5));
#100345=CARTESIAN_POINT('',(98.8292080271534,13.375,31.5));
#100346=CARTESIAN_POINT('',(98.8292080271534,13.375,31.5));
#100347=CARTESIAN_POINT('',(98.8292080271534,13.375,25.5));
#100348=CARTESIAN_POINT('Origin',(99.1796433977181,13.375,25.5));
#100349=CARTESIAN_POINT('',(99.1796433977181,13.375,25.5));
#100350=CARTESIAN_POINT('',(99.1796433977181,13.375,25.5));
#100351=CARTESIAN_POINT('',(99.1796433977181,13.375,31.5));
#100352=CARTESIAN_POINT('',(99.1796433977181,13.375,31.5));
#100353=CARTESIAN_POINT('',(99.1796433977181,13.375,25.5));
#100354=CARTESIAN_POINT('Origin',(99.5709113995542,14.45,25.5));
#100355=CARTESIAN_POINT('',(99.5709113995542,14.45,25.5));
#100356=CARTESIAN_POINT('',(99.5709113995542,14.45,25.5));
#100357=CARTESIAN_POINT('',(99.5709113995542,14.45,31.5));
#100358=CARTESIAN_POINT('',(99.5709113995542,14.45,31.5));
#100359=CARTESIAN_POINT('',(99.5709113995542,14.45,25.5));
#100360=CARTESIAN_POINT('Origin',(100.008736352112,14.45,25.5));
#100361=CARTESIAN_POINT('',(100.008736352112,14.45,25.5));
#100362=CARTESIAN_POINT('',(100.008736352112,14.45,25.5));
#100363=CARTESIAN_POINT('',(100.008736352112,14.45,31.5));
#100364=CARTESIAN_POINT('',(100.008736352112,14.45,31.5));
#100365=CARTESIAN_POINT('',(100.008736352112,14.45,25.5));
#100366=CARTESIAN_POINT('Origin',(100.400004353948,13.375,25.5));
#100367=CARTESIAN_POINT('',(100.400004353948,13.375,25.5));
#100368=CARTESIAN_POINT('',(100.400004353948,13.375,25.5));
#100369=CARTESIAN_POINT('',(100.400004353948,13.375,31.5));
#100370=CARTESIAN_POINT('',(100.400004353948,13.375,31.5));
#100371=CARTESIAN_POINT('',(100.400004353948,13.375,25.5));
#100372=CARTESIAN_POINT('Origin',(100.750439724513,13.375,25.5));
#100373=CARTESIAN_POINT('',(100.750439724513,13.375,25.5));
#100374=CARTESIAN_POINT('',(100.750439724513,13.375,25.5));
#100375=CARTESIAN_POINT('',(100.750439724513,13.375,31.5));
#100376=CARTESIAN_POINT('',(100.750439724513,13.375,31.5));
#100377=CARTESIAN_POINT('',(100.750439724513,13.375,25.5));
#100378=CARTESIAN_POINT('Origin',(101.141707726349,14.45,25.5));
#100379=CARTESIAN_POINT('',(101.141707726349,14.45,25.5));
#100380=CARTESIAN_POINT('',(101.141707726349,14.45,25.5));
#100381=CARTESIAN_POINT('',(101.141707726349,14.45,31.5));
#100382=CARTESIAN_POINT('',(101.141707726349,14.45,31.5));
#100383=CARTESIAN_POINT('',(101.141707726349,14.45,25.5));
#100384=CARTESIAN_POINT('Origin',(101.579532678907,14.45,25.5));
#100385=CARTESIAN_POINT('',(101.579532678907,14.45,25.5));
#100386=CARTESIAN_POINT('',(101.579532678907,14.45,25.5));
#100387=CARTESIAN_POINT('',(101.579532678907,14.45,31.5));
#100388=CARTESIAN_POINT('',(101.579532678907,14.45,31.5));
#100389=CARTESIAN_POINT('',(101.579532678907,14.45,25.5));
#100390=CARTESIAN_POINT('Origin',(101.970800680743,13.375,25.5));
#100391=CARTESIAN_POINT('',(101.970800680743,13.375,25.5));
#100392=CARTESIAN_POINT('',(101.970800680743,13.375,25.5));
#100393=CARTESIAN_POINT('',(101.970800680743,13.375,31.5));
#100394=CARTESIAN_POINT('',(101.970800680743,13.375,31.5));
#100395=CARTESIAN_POINT('',(101.970800680743,13.375,25.5));
#100396=CARTESIAN_POINT('Origin',(102.321236051308,13.375,25.5));
#100397=CARTESIAN_POINT('',(102.321236051308,13.375,25.5));
#100398=CARTESIAN_POINT('',(102.321236051308,13.375,25.5));
#100399=CARTESIAN_POINT('',(102.321236051308,13.375,31.5));
#100400=CARTESIAN_POINT('',(102.321236051308,13.375,31.5));
#100401=CARTESIAN_POINT('',(102.321236051308,13.375,25.5));
#100402=CARTESIAN_POINT('Origin',(102.712504053144,14.45,25.5));
#100403=CARTESIAN_POINT('',(102.712504053144,14.45,25.5));
#100404=CARTESIAN_POINT('',(102.712504053144,14.45,25.5));
#100405=CARTESIAN_POINT('',(102.712504053144,14.45,31.5));
#100406=CARTESIAN_POINT('',(102.712504053144,14.45,31.5));
#100407=CARTESIAN_POINT('',(102.712504053144,14.45,25.5));
#100408=CARTESIAN_POINT('Origin',(103.150329005702,14.45,25.5));
#100409=CARTESIAN_POINT('',(103.150329005702,14.45,25.5));
#100410=CARTESIAN_POINT('',(103.150329005702,14.45,25.5));
#100411=CARTESIAN_POINT('',(103.150329005702,14.45,31.5));
#100412=CARTESIAN_POINT('',(103.150329005702,14.45,31.5));
#100413=CARTESIAN_POINT('',(103.150329005702,14.45,25.5));
#100414=CARTESIAN_POINT('Origin',(103.541597007538,13.375,25.5));
#100415=CARTESIAN_POINT('',(103.541597007538,13.375,25.5));
#100416=CARTESIAN_POINT('',(103.541597007538,13.375,25.5));
#100417=CARTESIAN_POINT('',(103.541597007538,13.375,31.5));
#100418=CARTESIAN_POINT('',(103.541597007538,13.375,31.5));
#100419=CARTESIAN_POINT('',(103.541597007538,13.375,25.5));
#100420=CARTESIAN_POINT('Origin',(103.892032378103,13.375,25.5));
#100421=CARTESIAN_POINT('',(103.892032378103,13.375,25.5));
#100422=CARTESIAN_POINT('',(103.892032378103,13.375,25.5));
#100423=CARTESIAN_POINT('',(103.892032378103,13.375,31.5));
#100424=CARTESIAN_POINT('',(103.892032378103,13.375,31.5));
#100425=CARTESIAN_POINT('',(103.892032378103,13.375,25.5));
#100426=CARTESIAN_POINT('Origin',(104.283300379939,14.45,25.5));
#100427=CARTESIAN_POINT('',(104.283300379939,14.45,25.5));
#100428=CARTESIAN_POINT('',(104.283300379939,14.45,25.5));
#100429=CARTESIAN_POINT('',(104.283300379939,14.45,31.5));
#100430=CARTESIAN_POINT('',(104.283300379939,14.45,31.5));
#100431=CARTESIAN_POINT('',(104.283300379939,14.45,25.5));
#100432=CARTESIAN_POINT('Origin',(104.721125332497,14.45,25.5));
#100433=CARTESIAN_POINT('',(104.721125332497,14.45,25.5));
#100434=CARTESIAN_POINT('',(104.721125332497,14.45,25.5));
#100435=CARTESIAN_POINT('',(104.721125332497,14.45,31.5));
#100436=CARTESIAN_POINT('',(104.721125332497,14.45,31.5));
#100437=CARTESIAN_POINT('',(104.721125332497,14.45,25.5));
#100438=CARTESIAN_POINT('Origin',(105.112393334333,13.375,25.5));
#100439=CARTESIAN_POINT('',(105.112393334333,13.375,25.5));
#100440=CARTESIAN_POINT('',(105.112393334333,13.375,25.5));
#100441=CARTESIAN_POINT('',(105.112393334333,13.375,31.5));
#100442=CARTESIAN_POINT('',(105.112393334333,13.375,31.5));
#100443=CARTESIAN_POINT('',(105.112393334333,13.375,25.5));
#100444=CARTESIAN_POINT('Origin',(105.462828704898,13.375,25.5));
#100445=CARTESIAN_POINT('',(105.462828704898,13.375,25.5));
#100446=CARTESIAN_POINT('',(105.462828704898,13.375,25.5));
#100447=CARTESIAN_POINT('',(105.462828704898,13.375,31.5));
#100448=CARTESIAN_POINT('',(105.462828704898,13.375,31.5));
#100449=CARTESIAN_POINT('',(105.462828704898,13.375,25.5));
#100450=CARTESIAN_POINT('Origin',(105.854096706734,14.45,25.5));
#100451=CARTESIAN_POINT('',(105.854096706734,14.45,25.5));
#100452=CARTESIAN_POINT('',(105.854096706734,14.45,25.5));
#100453=CARTESIAN_POINT('',(105.854096706734,14.45,31.5));
#100454=CARTESIAN_POINT('',(105.854096706734,14.45,31.5));
#100455=CARTESIAN_POINT('',(105.854096706734,14.45,25.5));
#100456=CARTESIAN_POINT('Origin',(106.291921659292,14.45,25.5));
#100457=CARTESIAN_POINT('',(106.291921659292,14.45,25.5));
#100458=CARTESIAN_POINT('',(106.291921659292,14.45,25.5));
#100459=CARTESIAN_POINT('',(106.291921659292,14.45,31.5));
#100460=CARTESIAN_POINT('',(106.291921659292,14.45,31.5));
#100461=CARTESIAN_POINT('',(106.291921659292,14.45,25.5));
#100462=CARTESIAN_POINT('Origin',(106.683189661128,13.375,25.5));
#100463=CARTESIAN_POINT('',(106.683189661128,13.375,25.5));
#100464=CARTESIAN_POINT('',(106.683189661128,13.375,25.5));
#100465=CARTESIAN_POINT('',(106.683189661128,13.375,31.5));
#100466=CARTESIAN_POINT('',(106.683189661128,13.375,31.5));
#100467=CARTESIAN_POINT('',(106.683189661128,13.375,25.5));
#100468=CARTESIAN_POINT('Origin',(107.033625031693,13.375,25.5));
#100469=CARTESIAN_POINT('',(107.033625031693,13.375,25.5));
#100470=CARTESIAN_POINT('',(107.033625031693,13.375,25.5));
#100471=CARTESIAN_POINT('',(107.033625031693,13.375,31.5));
#100472=CARTESIAN_POINT('',(107.033625031693,13.375,31.5));
#100473=CARTESIAN_POINT('',(107.033625031693,13.375,25.5));
#100474=CARTESIAN_POINT('Origin',(107.424893033529,14.45,25.5));
#100475=CARTESIAN_POINT('',(107.424893033529,14.45,25.5));
#100476=CARTESIAN_POINT('',(107.424893033529,14.45,25.5));
#100477=CARTESIAN_POINT('',(107.424893033529,14.45,31.5));
#100478=CARTESIAN_POINT('',(107.424893033529,14.45,31.5));
#100479=CARTESIAN_POINT('',(107.424893033529,14.45,25.5));
#100480=CARTESIAN_POINT('Origin',(107.862717986087,14.45,25.5));
#100481=CARTESIAN_POINT('',(107.862717986087,14.45,25.5));
#100482=CARTESIAN_POINT('',(107.862717986087,14.45,25.5));
#100483=CARTESIAN_POINT('',(107.862717986087,14.45,31.5));
#100484=CARTESIAN_POINT('',(107.862717986087,14.45,31.5));
#100485=CARTESIAN_POINT('',(107.862717986087,14.45,25.5));
#100486=CARTESIAN_POINT('Origin',(108.253985987923,13.375,25.5));
#100487=CARTESIAN_POINT('',(108.253985987923,13.375,25.5));
#100488=CARTESIAN_POINT('',(108.253985987923,13.375,25.5));
#100489=CARTESIAN_POINT('',(108.253985987923,13.375,31.5));
#100490=CARTESIAN_POINT('',(108.253985987923,13.375,31.5));
#100491=CARTESIAN_POINT('',(108.253985987923,13.375,25.5));
#100492=CARTESIAN_POINT('Origin',(108.604421358487,13.375,25.5));
#100493=CARTESIAN_POINT('',(108.604421358487,13.375,25.5));
#100494=CARTESIAN_POINT('',(108.604421358487,13.375,25.5));
#100495=CARTESIAN_POINT('',(108.604421358487,13.375,31.5));
#100496=CARTESIAN_POINT('',(108.604421358487,13.375,31.5));
#100497=CARTESIAN_POINT('',(108.604421358487,13.375,25.5));
#100498=CARTESIAN_POINT('Origin',(108.995689360324,14.45,25.5));
#100499=CARTESIAN_POINT('',(108.995689360324,14.45,25.5));
#100500=CARTESIAN_POINT('',(108.995689360324,14.45,25.5));
#100501=CARTESIAN_POINT('',(108.995689360324,14.45,31.5));
#100502=CARTESIAN_POINT('',(108.995689360324,14.45,31.5));
#100503=CARTESIAN_POINT('',(108.995689360324,14.45,25.5));
#100504=CARTESIAN_POINT('Origin',(109.433514312881,14.45,25.5));
#100505=CARTESIAN_POINT('',(109.433514312881,14.45,25.5));
#100506=CARTESIAN_POINT('',(109.433514312881,14.45,25.5));
#100507=CARTESIAN_POINT('',(109.433514312881,14.45,31.5));
#100508=CARTESIAN_POINT('',(109.433514312881,14.45,31.5));
#100509=CARTESIAN_POINT('',(109.433514312881,14.45,25.5));
#100510=CARTESIAN_POINT('Origin',(109.824782314718,13.375,25.5));
#100511=CARTESIAN_POINT('',(109.824782314718,13.375,25.5));
#100512=CARTESIAN_POINT('',(109.824782314718,13.375,25.5));
#100513=CARTESIAN_POINT('',(109.824782314718,13.375,31.5));
#100514=CARTESIAN_POINT('',(109.824782314718,13.375,31.5));
#100515=CARTESIAN_POINT('',(109.824782314718,13.375,25.5));
#100516=CARTESIAN_POINT('Origin',(110.175217685282,13.375,25.5));
#100517=CARTESIAN_POINT('',(110.175217685282,13.375,25.5));
#100518=CARTESIAN_POINT('',(110.175217685282,13.375,25.5));
#100519=CARTESIAN_POINT('',(110.175217685282,13.375,31.5));
#100520=CARTESIAN_POINT('',(110.175217685282,13.375,31.5));
#100521=CARTESIAN_POINT('',(110.175217685282,13.375,25.5));
#100522=CARTESIAN_POINT('Origin',(110.566485687119,14.45,25.5));
#100523=CARTESIAN_POINT('',(110.566485687119,14.45,25.5));
#100524=CARTESIAN_POINT('',(110.566485687119,14.45,25.5));
#100525=CARTESIAN_POINT('',(110.566485687119,14.45,31.5));
#100526=CARTESIAN_POINT('',(110.566485687119,14.45,31.5));
#100527=CARTESIAN_POINT('',(110.566485687119,14.45,25.5));
#100528=CARTESIAN_POINT('Origin',(111.004310639676,14.45,25.5));
#100529=CARTESIAN_POINT('',(111.004310639676,14.45,25.5));
#100530=CARTESIAN_POINT('',(111.004310639676,14.45,25.5));
#100531=CARTESIAN_POINT('',(111.004310639676,14.45,31.5));
#100532=CARTESIAN_POINT('',(111.004310639676,14.45,31.5));
#100533=CARTESIAN_POINT('',(111.004310639676,14.45,25.5));
#100534=CARTESIAN_POINT('Origin',(111.395578641513,13.375,25.5));
#100535=CARTESIAN_POINT('',(111.395578641513,13.375,25.5));
#100536=CARTESIAN_POINT('',(111.395578641513,13.375,25.5));
#100537=CARTESIAN_POINT('',(111.395578641513,13.375,31.5));
#100538=CARTESIAN_POINT('',(111.395578641513,13.375,31.5));
#100539=CARTESIAN_POINT('',(111.395578641513,13.375,25.5));
#100540=CARTESIAN_POINT('Origin',(111.746014012077,13.375,25.5));
#100541=CARTESIAN_POINT('',(111.746014012077,13.375,25.5));
#100542=CARTESIAN_POINT('',(111.746014012077,13.375,25.5));
#100543=CARTESIAN_POINT('',(111.746014012077,13.375,31.5));
#100544=CARTESIAN_POINT('',(111.746014012077,13.375,31.5));
#100545=CARTESIAN_POINT('',(111.746014012077,13.375,25.5));
#100546=CARTESIAN_POINT('Origin',(112.137282013913,14.45,25.5));
#100547=CARTESIAN_POINT('',(112.137282013913,14.45,25.5));
#100548=CARTESIAN_POINT('',(112.137282013913,14.45,25.5));
#100549=CARTESIAN_POINT('',(112.137282013913,14.45,31.5));
#100550=CARTESIAN_POINT('',(112.137282013913,14.45,31.5));
#100551=CARTESIAN_POINT('',(112.137282013913,14.45,25.5));
#100552=CARTESIAN_POINT('Origin',(112.575106966471,14.45,25.5));
#100553=CARTESIAN_POINT('',(112.575106966471,14.45,25.5));
#100554=CARTESIAN_POINT('',(112.575106966471,14.45,25.5));
#100555=CARTESIAN_POINT('',(112.575106966471,14.45,31.5));
#100556=CARTESIAN_POINT('',(112.575106966471,14.45,31.5));
#100557=CARTESIAN_POINT('',(112.575106966471,14.45,25.5));
#100558=CARTESIAN_POINT('Origin',(112.966374968307,13.375,25.5));
#100559=CARTESIAN_POINT('',(112.966374968307,13.375,25.5));
#100560=CARTESIAN_POINT('',(112.966374968307,13.375,25.5));
#100561=CARTESIAN_POINT('',(112.966374968307,13.375,31.5));
#100562=CARTESIAN_POINT('',(112.966374968307,13.375,31.5));
#100563=CARTESIAN_POINT('',(112.966374968307,13.375,25.5));
#100564=CARTESIAN_POINT('Origin',(113.316810338872,13.375,25.5));
#100565=CARTESIAN_POINT('',(113.316810338872,13.375,25.5));
#100566=CARTESIAN_POINT('',(113.316810338872,13.375,25.5));
#100567=CARTESIAN_POINT('',(113.316810338872,13.375,31.5));
#100568=CARTESIAN_POINT('',(113.316810338872,13.375,31.5));
#100569=CARTESIAN_POINT('',(113.316810338872,13.375,25.5));
#100570=CARTESIAN_POINT('Origin',(113.708078340708,14.45,25.5));
#100571=CARTESIAN_POINT('',(113.708078340708,14.45,25.5));
#100572=CARTESIAN_POINT('',(113.708078340708,14.45,25.5));
#100573=CARTESIAN_POINT('',(113.708078340708,14.45,31.5));
#100574=CARTESIAN_POINT('',(113.708078340708,14.45,31.5));
#100575=CARTESIAN_POINT('',(113.708078340708,14.45,25.5));
#100576=CARTESIAN_POINT('Origin',(114.145903293266,14.45,25.5));
#100577=CARTESIAN_POINT('',(114.145903293266,14.45,25.5));
#100578=CARTESIAN_POINT('',(114.145903293266,14.45,25.5));
#100579=CARTESIAN_POINT('',(114.145903293266,14.45,31.5));
#100580=CARTESIAN_POINT('',(114.145903293266,14.45,31.5));
#100581=CARTESIAN_POINT('',(114.145903293266,14.45,25.5));
#100582=CARTESIAN_POINT('Origin',(114.537171295102,13.375,25.5));
#100583=CARTESIAN_POINT('',(114.537171295102,13.375,25.5));
#100584=CARTESIAN_POINT('',(114.537171295102,13.375,25.5));
#100585=CARTESIAN_POINT('',(114.537171295102,13.375,31.5));
#100586=CARTESIAN_POINT('',(114.537171295102,13.375,31.5));
#100587=CARTESIAN_POINT('',(114.537171295102,13.375,25.5));
#100588=CARTESIAN_POINT('Origin',(114.887606665667,13.375,25.5));
#100589=CARTESIAN_POINT('',(114.887606665667,13.375,25.5));
#100590=CARTESIAN_POINT('',(114.887606665667,13.375,25.5));
#100591=CARTESIAN_POINT('',(114.887606665667,13.375,31.5));
#100592=CARTESIAN_POINT('',(114.887606665667,13.375,31.5));
#100593=CARTESIAN_POINT('',(114.887606665667,13.375,25.5));
#100594=CARTESIAN_POINT('Origin',(115.278874667503,14.45,25.5));
#100595=CARTESIAN_POINT('',(115.278874667503,14.45,25.5));
#100596=CARTESIAN_POINT('',(115.278874667503,14.45,25.5));
#100597=CARTESIAN_POINT('',(115.278874667503,14.45,31.5));
#100598=CARTESIAN_POINT('',(115.278874667503,14.45,31.5));
#100599=CARTESIAN_POINT('',(115.278874667503,14.45,25.5));
#100600=CARTESIAN_POINT('Origin',(115.716699620061,14.45,25.5));
#100601=CARTESIAN_POINT('',(115.716699620061,14.45,25.5));
#100602=CARTESIAN_POINT('',(115.716699620061,14.45,25.5));
#100603=CARTESIAN_POINT('',(115.716699620061,14.45,31.5));
#100604=CARTESIAN_POINT('',(115.716699620061,14.45,31.5));
#100605=CARTESIAN_POINT('',(115.716699620061,14.45,25.5));
#100606=CARTESIAN_POINT('Origin',(116.107967621897,13.375,25.5));
#100607=CARTESIAN_POINT('',(116.107967621897,13.375,25.5));
#100608=CARTESIAN_POINT('',(116.107967621897,13.375,25.5));
#100609=CARTESIAN_POINT('',(116.107967621897,13.375,31.5));
#100610=CARTESIAN_POINT('',(116.107967621897,13.375,31.5));
#100611=CARTESIAN_POINT('',(116.107967621897,13.375,25.5));
#100612=CARTESIAN_POINT('Origin',(116.458402992462,13.375,25.5));
#100613=CARTESIAN_POINT('',(116.458402992462,13.375,25.5));
#100614=CARTESIAN_POINT('',(116.458402992462,13.375,25.5));
#100615=CARTESIAN_POINT('',(116.458402992462,13.375,31.5));
#100616=CARTESIAN_POINT('',(116.458402992462,13.375,31.5));
#100617=CARTESIAN_POINT('',(116.458402992462,13.375,25.5));
#100618=CARTESIAN_POINT('Origin',(116.849670994298,14.45,25.5));
#100619=CARTESIAN_POINT('',(116.849670994298,14.45,25.5));
#100620=CARTESIAN_POINT('',(116.849670994298,14.45,25.5));
#100621=CARTESIAN_POINT('',(116.849670994298,14.45,31.5));
#100622=CARTESIAN_POINT('',(116.849670994298,14.45,31.5));
#100623=CARTESIAN_POINT('',(116.849670994298,14.45,25.5));
#100624=CARTESIAN_POINT('Origin',(117.287495946856,14.45,25.5));
#100625=CARTESIAN_POINT('',(117.287495946856,14.45,25.5));
#100626=CARTESIAN_POINT('',(117.287495946856,14.45,25.5));
#100627=CARTESIAN_POINT('',(117.287495946856,14.45,31.5));
#100628=CARTESIAN_POINT('',(117.287495946856,14.45,31.5));
#100629=CARTESIAN_POINT('',(117.287495946856,14.45,25.5));
#100630=CARTESIAN_POINT('Origin',(117.678763948692,13.375,25.5));
#100631=CARTESIAN_POINT('',(117.678763948692,13.375,25.5));
#100632=CARTESIAN_POINT('',(117.678763948692,13.375,25.5));
#100633=CARTESIAN_POINT('',(117.678763948692,13.375,31.5));
#100634=CARTESIAN_POINT('',(117.678763948692,13.375,31.5));
#100635=CARTESIAN_POINT('',(117.678763948692,13.375,25.5));
#100636=CARTESIAN_POINT('Origin',(118.029199319257,13.375,25.5));
#100637=CARTESIAN_POINT('',(118.029199319257,13.375,25.5));
#100638=CARTESIAN_POINT('',(118.029199319257,13.375,25.5));
#100639=CARTESIAN_POINT('',(118.029199319257,13.375,31.5));
#100640=CARTESIAN_POINT('',(118.029199319257,13.375,31.5));
#100641=CARTESIAN_POINT('',(118.029199319257,13.375,25.5));
#100642=CARTESIAN_POINT('Origin',(118.420467321093,14.45,25.5));
#100643=CARTESIAN_POINT('',(118.420467321093,14.45,25.5));
#100644=CARTESIAN_POINT('',(118.420467321093,14.45,25.5));
#100645=CARTESIAN_POINT('',(118.420467321093,14.45,31.5));
#100646=CARTESIAN_POINT('',(118.420467321093,14.45,31.5));
#100647=CARTESIAN_POINT('',(118.420467321093,14.45,25.5));
#100648=CARTESIAN_POINT('Origin',(118.858292273651,14.45,25.5));
#100649=CARTESIAN_POINT('',(118.858292273651,14.45,25.5));
#100650=CARTESIAN_POINT('',(118.858292273651,14.45,25.5));
#100651=CARTESIAN_POINT('',(118.858292273651,14.45,31.5));
#100652=CARTESIAN_POINT('',(118.858292273651,14.45,31.5));
#100653=CARTESIAN_POINT('',(118.858292273651,14.45,25.5));
#100654=CARTESIAN_POINT('Origin',(119.249560275487,13.375,25.5));
#100655=CARTESIAN_POINT('',(119.249560275487,13.375,25.5));
#100656=CARTESIAN_POINT('',(119.249560275487,13.375,25.5));
#100657=CARTESIAN_POINT('',(119.249560275487,13.375,31.5));
#100658=CARTESIAN_POINT('',(119.249560275487,13.375,31.5));
#100659=CARTESIAN_POINT('',(119.249560275487,13.375,25.5));
#100660=CARTESIAN_POINT('Origin',(119.599995646052,13.375,25.5));
#100661=CARTESIAN_POINT('',(119.599995646052,13.375,25.5));
#100662=CARTESIAN_POINT('',(119.599995646052,13.375,25.5));
#100663=CARTESIAN_POINT('',(119.599995646052,13.375,31.5));
#100664=CARTESIAN_POINT('',(119.599995646052,13.375,31.5));
#100665=CARTESIAN_POINT('',(119.599995646052,13.375,25.5));
#100666=CARTESIAN_POINT('Origin',(119.991263647888,14.45,25.5));
#100667=CARTESIAN_POINT('',(119.991263647888,14.45,25.5));
#100668=CARTESIAN_POINT('',(119.991263647888,14.45,25.5));
#100669=CARTESIAN_POINT('',(119.991263647888,14.45,31.5));
#100670=CARTESIAN_POINT('',(119.991263647888,14.45,31.5));
#100671=CARTESIAN_POINT('',(119.991263647888,14.45,25.5));
#100672=CARTESIAN_POINT('Origin',(120.429088600446,14.45,25.5));
#100673=CARTESIAN_POINT('',(120.429088600446,14.45,25.5));
#100674=CARTESIAN_POINT('',(120.429088600446,14.45,25.5));
#100675=CARTESIAN_POINT('',(120.429088600446,14.45,31.5));
#100676=CARTESIAN_POINT('',(120.429088600446,14.45,31.5));
#100677=CARTESIAN_POINT('',(120.429088600446,14.45,25.5));
#100678=CARTESIAN_POINT('Origin',(120.820356602282,13.375,25.5));
#100679=CARTESIAN_POINT('',(120.820356602282,13.375,25.5));
#100680=CARTESIAN_POINT('',(120.820356602282,13.375,25.5));
#100681=CARTESIAN_POINT('',(120.820356602282,13.375,31.5));
#100682=CARTESIAN_POINT('',(120.820356602282,13.375,31.5));
#100683=CARTESIAN_POINT('',(120.820356602282,13.375,25.5));
#100684=CARTESIAN_POINT('Origin',(121.170791972847,13.375,25.5));
#100685=CARTESIAN_POINT('',(121.170791972847,13.375,25.5));
#100686=CARTESIAN_POINT('',(121.170791972847,13.375,25.5));
#100687=CARTESIAN_POINT('',(121.170791972847,13.375,31.5));
#100688=CARTESIAN_POINT('',(121.170791972847,13.375,31.5));
#100689=CARTESIAN_POINT('',(121.170791972847,13.375,25.5));
#100690=CARTESIAN_POINT('Origin',(121.562059974683,14.45,25.5));
#100691=CARTESIAN_POINT('',(121.562059974683,14.45,25.5));
#100692=CARTESIAN_POINT('',(121.562059974683,14.45,25.5));
#100693=CARTESIAN_POINT('',(121.562059974683,14.45,31.5));
#100694=CARTESIAN_POINT('',(121.562059974683,14.45,31.5));
#100695=CARTESIAN_POINT('',(121.562059974683,14.45,25.5));
#100696=CARTESIAN_POINT('Origin',(121.999884927241,14.45,25.5));
#100697=CARTESIAN_POINT('',(121.999884927241,14.45,25.5));
#100698=CARTESIAN_POINT('',(121.999884927241,14.45,25.5));
#100699=CARTESIAN_POINT('',(121.999884927241,14.45,31.5));
#100700=CARTESIAN_POINT('',(121.999884927241,14.45,31.5));
#100701=CARTESIAN_POINT('',(121.999884927241,14.45,25.5));
#100702=CARTESIAN_POINT('Origin',(122.391152929077,13.375,25.5));
#100703=CARTESIAN_POINT('',(122.391152929077,13.375,25.5));
#100704=CARTESIAN_POINT('',(122.391152929077,13.375,25.5));
#100705=CARTESIAN_POINT('',(122.391152929077,13.375,31.5));
#100706=CARTESIAN_POINT('',(122.391152929077,13.375,31.5));
#100707=CARTESIAN_POINT('',(122.391152929077,13.375,25.5));
#100708=CARTESIAN_POINT('Origin',(122.741588299642,13.375,25.5));
#100709=CARTESIAN_POINT('',(122.741588299642,13.375,25.5));
#100710=CARTESIAN_POINT('',(122.741588299642,13.375,25.5));
#100711=CARTESIAN_POINT('',(122.741588299642,13.375,31.5));
#100712=CARTESIAN_POINT('',(122.741588299642,13.375,31.5));
#100713=CARTESIAN_POINT('',(122.741588299642,13.375,25.5));
#100714=CARTESIAN_POINT('Origin',(123.132856301478,14.45,25.5));
#100715=CARTESIAN_POINT('',(123.132856301478,14.45,25.5));
#100716=CARTESIAN_POINT('',(123.132856301478,14.45,25.5));
#100717=CARTESIAN_POINT('',(123.132856301478,14.45,31.5));
#100718=CARTESIAN_POINT('',(123.132856301478,14.45,31.5));
#100719=CARTESIAN_POINT('',(123.132856301478,14.45,25.5));
#100720=CARTESIAN_POINT('Origin',(123.570681254036,14.45,25.5));
#100721=CARTESIAN_POINT('',(123.570681254036,14.45,25.5));
#100722=CARTESIAN_POINT('',(123.570681254036,14.45,25.5));
#100723=CARTESIAN_POINT('',(123.570681254036,14.45,31.5));
#100724=CARTESIAN_POINT('',(123.570681254036,14.45,31.5));
#100725=CARTESIAN_POINT('',(123.570681254036,14.45,25.5));
#100726=CARTESIAN_POINT('Origin',(123.961949255872,13.375,25.5));
#100727=CARTESIAN_POINT('',(123.961949255872,13.375,25.5));
#100728=CARTESIAN_POINT('',(123.961949255872,13.375,25.5));
#100729=CARTESIAN_POINT('',(123.961949255872,13.375,31.5));
#100730=CARTESIAN_POINT('',(123.961949255872,13.375,31.5));
#100731=CARTESIAN_POINT('',(123.961949255872,13.375,25.5));
#100732=CARTESIAN_POINT('Origin',(124.312384626436,13.375,25.5));
#100733=CARTESIAN_POINT('',(124.312384626436,13.375,25.5));
#100734=CARTESIAN_POINT('',(124.312384626436,13.375,25.5));
#100735=CARTESIAN_POINT('',(124.312384626436,13.375,31.5));
#100736=CARTESIAN_POINT('',(124.312384626436,13.375,31.5));
#100737=CARTESIAN_POINT('',(124.312384626436,13.375,25.5));
#100738=CARTESIAN_POINT('Origin',(124.703652628273,14.45,25.5));
#100739=CARTESIAN_POINT('',(124.703652628273,14.45,25.5));
#100740=CARTESIAN_POINT('',(124.703652628273,14.45,25.5));
#100741=CARTESIAN_POINT('',(124.703652628273,14.45,31.5));
#100742=CARTESIAN_POINT('',(124.703652628273,14.45,31.5));
#100743=CARTESIAN_POINT('',(124.703652628273,14.45,25.5));
#100744=CARTESIAN_POINT('Origin',(125.14147758083,14.45,25.5));
#100745=CARTESIAN_POINT('',(125.14147758083,14.45,25.5));
#100746=CARTESIAN_POINT('',(125.14147758083,14.45,25.5));
#100747=CARTESIAN_POINT('',(125.14147758083,14.45,31.5));
#100748=CARTESIAN_POINT('',(125.14147758083,14.45,31.5));
#100749=CARTESIAN_POINT('',(125.14147758083,14.45,25.5));
#100750=CARTESIAN_POINT('Origin',(125.532745582667,13.375,25.5));
#100751=CARTESIAN_POINT('',(125.532745582667,13.375,25.5));
#100752=CARTESIAN_POINT('',(125.532745582667,13.375,25.5));
#100753=CARTESIAN_POINT('',(125.532745582667,13.375,31.5));
#100754=CARTESIAN_POINT('',(125.532745582667,13.375,31.5));
#100755=CARTESIAN_POINT('',(125.532745582667,13.375,25.5));
#100756=CARTESIAN_POINT('Origin',(125.883180953231,13.375,25.5));
#100757=CARTESIAN_POINT('',(125.883180953231,13.375,25.5));
#100758=CARTESIAN_POINT('',(125.883180953231,13.375,25.5));
#100759=CARTESIAN_POINT('',(125.883180953231,13.375,31.5));
#100760=CARTESIAN_POINT('',(125.883180953231,13.375,31.5));
#100761=CARTESIAN_POINT('',(125.883180953231,13.375,25.5));
#100762=CARTESIAN_POINT('Origin',(126.274448955067,14.45,25.5));
#100763=CARTESIAN_POINT('',(126.274448955067,14.45,25.5));
#100764=CARTESIAN_POINT('',(126.274448955067,14.45,25.5));
#100765=CARTESIAN_POINT('',(126.274448955067,14.45,31.5));
#100766=CARTESIAN_POINT('',(126.274448955067,14.45,31.5));
#100767=CARTESIAN_POINT('',(126.274448955067,14.45,25.5));
#100768=CARTESIAN_POINT('Origin',(126.712273907625,14.45,25.5));
#100769=CARTESIAN_POINT('',(126.712273907625,14.45,25.5));
#100770=CARTESIAN_POINT('',(126.712273907625,14.45,25.5));
#100771=CARTESIAN_POINT('',(126.712273907625,14.45,31.5));
#100772=CARTESIAN_POINT('',(126.712273907625,14.45,31.5));
#100773=CARTESIAN_POINT('',(126.712273907625,14.45,25.5));
#100774=CARTESIAN_POINT('Origin',(127.103541909462,13.375,25.5));
#100775=CARTESIAN_POINT('',(127.103541909462,13.375,25.5));
#100776=CARTESIAN_POINT('',(127.103541909462,13.375,25.5));
#100777=CARTESIAN_POINT('',(127.103541909462,13.375,31.5));
#100778=CARTESIAN_POINT('',(127.103541909462,13.375,31.5));
#100779=CARTESIAN_POINT('',(127.103541909462,13.375,25.5));
#100780=CARTESIAN_POINT('Origin',(127.453977280026,13.375,25.5));
#100781=CARTESIAN_POINT('',(127.453977280026,13.375,25.5));
#100782=CARTESIAN_POINT('',(127.453977280026,13.375,25.5));
#100783=CARTESIAN_POINT('',(127.453977280026,13.375,31.5));
#100784=CARTESIAN_POINT('',(127.453977280026,13.375,31.5));
#100785=CARTESIAN_POINT('',(127.453977280026,13.375,25.5));
#100786=CARTESIAN_POINT('Origin',(127.845245281862,14.45,25.5));
#100787=CARTESIAN_POINT('',(127.845245281862,14.45,25.5));
#100788=CARTESIAN_POINT('',(127.845245281862,14.45,25.5));
#100789=CARTESIAN_POINT('',(127.845245281862,14.45,31.5));
#100790=CARTESIAN_POINT('',(127.845245281862,14.45,31.5));
#100791=CARTESIAN_POINT('',(127.845245281862,14.45,25.5));
#100792=CARTESIAN_POINT('Origin',(128.28307023442,14.45,25.5));
#100793=CARTESIAN_POINT('',(128.28307023442,14.45,25.5));
#100794=CARTESIAN_POINT('',(128.28307023442,14.45,25.5));
#100795=CARTESIAN_POINT('',(128.28307023442,14.45,31.5));
#100796=CARTESIAN_POINT('',(128.28307023442,14.45,31.5));
#100797=CARTESIAN_POINT('',(128.28307023442,14.45,25.5));
#100798=CARTESIAN_POINT('Origin',(128.674338236256,13.375,25.5));
#100799=CARTESIAN_POINT('',(128.674338236256,13.375,25.5));
#100800=CARTESIAN_POINT('',(128.674338236256,13.375,25.5));
#100801=CARTESIAN_POINT('',(128.674338236256,13.375,31.5));
#100802=CARTESIAN_POINT('',(128.674338236256,13.375,31.5));
#100803=CARTESIAN_POINT('',(128.674338236256,13.375,25.5));
#100804=CARTESIAN_POINT('Origin',(129.024773606821,13.375,25.5));
#100805=CARTESIAN_POINT('',(129.024773606821,13.375,25.5));
#100806=CARTESIAN_POINT('',(129.024773606821,13.375,25.5));
#100807=CARTESIAN_POINT('',(129.024773606821,13.375,31.5));
#100808=CARTESIAN_POINT('',(129.024773606821,13.375,31.5));
#100809=CARTESIAN_POINT('',(129.024773606821,13.375,25.5));
#100810=CARTESIAN_POINT('Origin',(129.416041608657,14.45,25.5));
#100811=CARTESIAN_POINT('',(129.416041608657,14.45,25.5));
#100812=CARTESIAN_POINT('',(129.416041608657,14.45,25.5));
#100813=CARTESIAN_POINT('',(129.416041608657,14.45,31.5));
#100814=CARTESIAN_POINT('',(129.416041608657,14.45,31.5));
#100815=CARTESIAN_POINT('',(129.416041608657,14.45,25.5));
#100816=CARTESIAN_POINT('Origin',(129.853866561215,14.45,25.5));
#100817=CARTESIAN_POINT('',(129.853866561215,14.45,25.5));
#100818=CARTESIAN_POINT('',(129.853866561215,14.45,25.5));
#100819=CARTESIAN_POINT('',(129.853866561215,14.45,31.5));
#100820=CARTESIAN_POINT('',(129.853866561215,14.45,31.5));
#100821=CARTESIAN_POINT('',(129.853866561215,14.45,25.5));
#100822=CARTESIAN_POINT('Origin',(130.245134563051,13.375,25.5));
#100823=CARTESIAN_POINT('',(130.245134563051,13.375,25.5));
#100824=CARTESIAN_POINT('',(130.245134563051,13.375,25.5));
#100825=CARTESIAN_POINT('',(130.245134563051,13.375,31.5));
#100826=CARTESIAN_POINT('',(130.245134563051,13.375,31.5));
#100827=CARTESIAN_POINT('',(130.245134563051,13.375,25.5));
#100828=CARTESIAN_POINT('Origin',(130.595569933616,13.375,25.5));
#100829=CARTESIAN_POINT('',(130.595569933616,13.375,25.5));
#100830=CARTESIAN_POINT('',(130.595569933616,13.375,25.5));
#100831=CARTESIAN_POINT('',(130.595569933616,13.375,31.5));
#100832=CARTESIAN_POINT('',(130.595569933616,13.375,31.5));
#100833=CARTESIAN_POINT('',(130.595569933616,13.375,25.5));
#100834=CARTESIAN_POINT('Origin',(130.986837935452,14.45,25.5));
#100835=CARTESIAN_POINT('',(130.986837935452,14.45,25.5));
#100836=CARTESIAN_POINT('',(130.986837935452,14.45,25.5));
#100837=CARTESIAN_POINT('',(130.986837935452,14.45,31.5));
#100838=CARTESIAN_POINT('',(130.986837935452,14.45,31.5));
#100839=CARTESIAN_POINT('',(130.986837935452,14.45,25.5));
#100840=CARTESIAN_POINT('Origin',(131.42466288801,14.45,25.5));
#100841=CARTESIAN_POINT('',(131.42466288801,14.45,25.5));
#100842=CARTESIAN_POINT('',(131.42466288801,14.45,25.5));
#100843=CARTESIAN_POINT('',(131.42466288801,14.45,31.5));
#100844=CARTESIAN_POINT('',(131.42466288801,14.45,31.5));
#100845=CARTESIAN_POINT('',(131.42466288801,14.45,25.5));
#100846=CARTESIAN_POINT('Origin',(131.815930889846,13.375,25.5));
#100847=CARTESIAN_POINT('',(131.815930889846,13.375,25.5));
#100848=CARTESIAN_POINT('',(131.815930889846,13.375,25.5));
#100849=CARTESIAN_POINT('',(131.815930889846,13.375,31.5));
#100850=CARTESIAN_POINT('',(131.815930889846,13.375,31.5));
#100851=CARTESIAN_POINT('',(131.815930889846,13.375,25.5));
#100852=CARTESIAN_POINT('Origin',(132.166366260411,13.375,25.5));
#100853=CARTESIAN_POINT('',(132.166366260411,13.375,25.5));
#100854=CARTESIAN_POINT('',(132.166366260411,13.375,25.5));
#100855=CARTESIAN_POINT('',(132.166366260411,13.375,31.5));
#100856=CARTESIAN_POINT('',(132.166366260411,13.375,31.5));
#100857=CARTESIAN_POINT('',(132.166366260411,13.375,25.5));
#100858=CARTESIAN_POINT('Origin',(132.557634262247,14.45,25.5));
#100859=CARTESIAN_POINT('',(132.557634262247,14.45,25.5));
#100860=CARTESIAN_POINT('',(132.557634262247,14.45,25.5));
#100861=CARTESIAN_POINT('',(132.557634262247,14.45,31.5));
#100862=CARTESIAN_POINT('',(132.557634262247,14.45,31.5));
#100863=CARTESIAN_POINT('',(132.557634262247,14.45,25.5));
#100864=CARTESIAN_POINT('Origin',(132.995459214805,14.45,25.5));
#100865=CARTESIAN_POINT('',(132.995459214805,14.45,25.5));
#100866=CARTESIAN_POINT('',(132.995459214805,14.45,25.5));
#100867=CARTESIAN_POINT('',(132.995459214805,14.45,31.5));
#100868=CARTESIAN_POINT('',(132.995459214805,14.45,31.5));
#100869=CARTESIAN_POINT('',(132.995459214805,14.45,25.5));
#100870=CARTESIAN_POINT('Origin',(133.386727216641,13.375,25.5));
#100871=CARTESIAN_POINT('',(133.386727216641,13.375,25.5));
#100872=CARTESIAN_POINT('',(133.386727216641,13.375,25.5));
#100873=CARTESIAN_POINT('',(133.386727216641,13.375,31.5));
#100874=CARTESIAN_POINT('',(133.386727216641,13.375,31.5));
#100875=CARTESIAN_POINT('',(133.386727216641,13.375,25.5));
#100876=CARTESIAN_POINT('Origin',(133.737162587206,13.375,25.5));
#100877=CARTESIAN_POINT('',(133.737162587206,13.375,25.5));
#100878=CARTESIAN_POINT('',(133.737162587206,13.375,25.5));
#100879=CARTESIAN_POINT('',(133.737162587206,13.375,31.5));
#100880=CARTESIAN_POINT('',(133.737162587206,13.375,31.5));
#100881=CARTESIAN_POINT('',(133.737162587206,13.375,25.5));
#100882=CARTESIAN_POINT('Origin',(134.128430589042,14.45,25.5));
#100883=CARTESIAN_POINT('',(134.128430589042,14.45,25.5));
#100884=CARTESIAN_POINT('',(134.128430589042,14.45,25.5));
#100885=CARTESIAN_POINT('',(134.128430589042,14.45,31.5));
#100886=CARTESIAN_POINT('',(134.128430589042,14.45,31.5));
#100887=CARTESIAN_POINT('',(134.128430589042,14.45,25.5));
#100888=CARTESIAN_POINT('Origin',(134.5662555416,14.45,25.5));
#100889=CARTESIAN_POINT('',(134.5662555416,14.45,25.5));
#100890=CARTESIAN_POINT('',(134.5662555416,14.45,25.5));
#100891=CARTESIAN_POINT('',(134.5662555416,14.45,31.5));
#100892=CARTESIAN_POINT('',(134.5662555416,14.45,31.5));
#100893=CARTESIAN_POINT('',(134.5662555416,14.45,25.5));
#100894=CARTESIAN_POINT('Origin',(134.957523543436,13.375,25.5));
#100895=CARTESIAN_POINT('',(134.957523543436,13.375,25.5));
#100896=CARTESIAN_POINT('',(134.957523543436,13.375,25.5));
#100897=CARTESIAN_POINT('',(134.957523543436,13.375,31.5));
#100898=CARTESIAN_POINT('',(134.957523543436,13.375,31.5));
#100899=CARTESIAN_POINT('',(134.957523543436,13.375,25.5));
#100900=CARTESIAN_POINT('Origin',(135.307958914001,13.375,25.5));
#100901=CARTESIAN_POINT('',(135.307958914001,13.375,25.5));
#100902=CARTESIAN_POINT('',(135.307958914001,13.375,25.5));
#100903=CARTESIAN_POINT('',(135.307958914001,13.375,31.5));
#100904=CARTESIAN_POINT('',(135.307958914001,13.375,31.5));
#100905=CARTESIAN_POINT('',(135.307958914001,13.375,25.5));
#100906=CARTESIAN_POINT('Origin',(135.699226915837,14.45,25.5));
#100907=CARTESIAN_POINT('',(135.699226915837,14.45,25.5));
#100908=CARTESIAN_POINT('',(135.699226915837,14.45,25.5));
#100909=CARTESIAN_POINT('',(135.699226915837,14.45,31.5));
#100910=CARTESIAN_POINT('',(135.699226915837,14.45,31.5));
#100911=CARTESIAN_POINT('',(135.699226915837,14.45,25.5));
#100912=CARTESIAN_POINT('Origin',(136.137051868395,14.45,25.5));
#100913=CARTESIAN_POINT('',(136.137051868395,14.45,25.5));
#100914=CARTESIAN_POINT('',(136.137051868395,14.45,25.5));
#100915=CARTESIAN_POINT('',(136.137051868395,14.45,31.5));
#100916=CARTESIAN_POINT('',(136.137051868395,14.45,31.5));
#100917=CARTESIAN_POINT('',(136.137051868395,14.45,25.5));
#100918=CARTESIAN_POINT('Origin',(136.528319870231,13.375,25.5));
#100919=CARTESIAN_POINT('',(136.528319870231,13.375,25.5));
#100920=CARTESIAN_POINT('',(136.528319870231,13.375,25.5));
#100921=CARTESIAN_POINT('',(136.528319870231,13.375,31.5));
#100922=CARTESIAN_POINT('',(136.528319870231,13.375,31.5));
#100923=CARTESIAN_POINT('',(136.528319870231,13.375,25.5));
#100924=CARTESIAN_POINT('Origin',(136.878755240796,13.375,25.5));
#100925=CARTESIAN_POINT('',(136.878755240796,13.375,25.5));
#100926=CARTESIAN_POINT('',(136.878755240796,13.375,25.5));
#100927=CARTESIAN_POINT('',(136.878755240796,13.375,31.5));
#100928=CARTESIAN_POINT('',(136.878755240796,13.375,31.5));
#100929=CARTESIAN_POINT('',(136.878755240796,13.375,25.5));
#100930=CARTESIAN_POINT('Origin',(137.270023242632,14.45,25.5));
#100931=CARTESIAN_POINT('',(137.270023242632,14.45,25.5));
#100932=CARTESIAN_POINT('',(137.270023242632,14.45,25.5));
#100933=CARTESIAN_POINT('',(137.270023242632,14.45,31.5));
#100934=CARTESIAN_POINT('',(137.270023242632,14.45,31.5));
#100935=CARTESIAN_POINT('',(137.270023242632,14.45,25.5));
#100936=CARTESIAN_POINT('Origin',(137.70784819519,14.45,25.5));
#100937=CARTESIAN_POINT('',(137.70784819519,14.45,25.5));
#100938=CARTESIAN_POINT('',(137.70784819519,14.45,25.5));
#100939=CARTESIAN_POINT('',(137.70784819519,14.45,31.5));
#100940=CARTESIAN_POINT('',(137.70784819519,14.45,31.5));
#100941=CARTESIAN_POINT('',(137.70784819519,14.45,25.5));
#100942=CARTESIAN_POINT('Origin',(138.099116197026,13.375,25.5));
#100943=CARTESIAN_POINT('',(138.099116197026,13.375,25.5));
#100944=CARTESIAN_POINT('',(138.099116197026,13.375,25.5));
#100945=CARTESIAN_POINT('',(138.099116197026,13.375,31.5));
#100946=CARTESIAN_POINT('',(138.099116197026,13.375,31.5));
#100947=CARTESIAN_POINT('',(138.099116197026,13.375,25.5));
#100948=CARTESIAN_POINT('Origin',(138.44955156759,13.375,25.5));
#100949=CARTESIAN_POINT('',(138.44955156759,13.375,25.5));
#100950=CARTESIAN_POINT('',(138.44955156759,13.375,25.5));
#100951=CARTESIAN_POINT('',(138.44955156759,13.375,31.5));
#100952=CARTESIAN_POINT('',(138.44955156759,13.375,31.5));
#100953=CARTESIAN_POINT('',(138.44955156759,13.375,25.5));
#100954=CARTESIAN_POINT('Origin',(138.840819569427,14.45,25.5));
#100955=CARTESIAN_POINT('',(138.840819569427,14.45,25.5));
#100956=CARTESIAN_POINT('',(138.840819569427,14.45,25.5));
#100957=CARTESIAN_POINT('',(138.840819569427,14.45,31.5));
#100958=CARTESIAN_POINT('',(138.840819569427,14.45,31.5));
#100959=CARTESIAN_POINT('',(138.840819569427,14.45,25.5));
#100960=CARTESIAN_POINT('Origin',(139.278644521985,14.45,25.5));
#100961=CARTESIAN_POINT('',(139.278644521985,14.45,25.5));
#100962=CARTESIAN_POINT('',(139.278644521985,14.45,25.5));
#100963=CARTESIAN_POINT('',(139.278644521985,14.45,31.5));
#100964=CARTESIAN_POINT('',(139.278644521985,14.45,31.5));
#100965=CARTESIAN_POINT('',(139.278644521985,14.45,25.5));
#100966=CARTESIAN_POINT('Origin',(139.669912523821,13.375,25.5));
#100967=CARTESIAN_POINT('',(139.669912523821,13.375,25.5));
#100968=CARTESIAN_POINT('',(139.669912523821,13.375,25.5));
#100969=CARTESIAN_POINT('',(139.669912523821,13.375,31.5));
#100970=CARTESIAN_POINT('',(139.669912523821,13.375,31.5));
#100971=CARTESIAN_POINT('',(139.669912523821,13.375,25.5));
#100972=CARTESIAN_POINT('Origin',(140.020347894385,13.375,25.5));
#100973=CARTESIAN_POINT('',(140.020347894385,13.375,25.5));
#100974=CARTESIAN_POINT('',(140.020347894385,13.375,25.5));
#100975=CARTESIAN_POINT('',(140.020347894385,13.375,31.5));
#100976=CARTESIAN_POINT('',(140.020347894385,13.375,31.5));
#100977=CARTESIAN_POINT('',(140.020347894385,13.375,25.5));
#100978=CARTESIAN_POINT('Origin',(140.411615896222,14.45,25.5));
#100979=CARTESIAN_POINT('',(140.411615896222,14.45,25.5));
#100980=CARTESIAN_POINT('',(140.411615896222,14.45,25.5));
#100981=CARTESIAN_POINT('',(140.411615896222,14.45,31.5));
#100982=CARTESIAN_POINT('',(140.411615896222,14.45,31.5));
#100983=CARTESIAN_POINT('',(140.411615896222,14.45,25.5));
#100984=CARTESIAN_POINT('Origin',(140.849440848779,14.45,25.5));
#100985=CARTESIAN_POINT('',(140.849440848779,14.45,25.5));
#100986=CARTESIAN_POINT('',(140.849440848779,14.45,25.5));
#100987=CARTESIAN_POINT('',(140.849440848779,14.45,31.5));
#100988=CARTESIAN_POINT('',(140.849440848779,14.45,31.5));
#100989=CARTESIAN_POINT('',(140.849440848779,14.45,25.5));
#100990=CARTESIAN_POINT('Origin',(141.240708850616,13.375,25.5));
#100991=CARTESIAN_POINT('',(141.240708850616,13.375,25.5));
#100992=CARTESIAN_POINT('',(141.240708850616,13.375,25.5));
#100993=CARTESIAN_POINT('',(141.240708850616,13.375,31.5));
#100994=CARTESIAN_POINT('',(141.240708850616,13.375,31.5));
#100995=CARTESIAN_POINT('',(141.240708850616,13.375,25.5));
#100996=CARTESIAN_POINT('Origin',(141.59114422118,13.375,25.5));
#100997=CARTESIAN_POINT('',(141.59114422118,13.375,25.5));
#100998=CARTESIAN_POINT('',(141.59114422118,13.375,25.5));
#100999=CARTESIAN_POINT('',(141.59114422118,13.375,31.5));
#101000=CARTESIAN_POINT('',(141.59114422118,13.375,31.5));
#101001=CARTESIAN_POINT('',(141.59114422118,13.375,25.5));
#101002=CARTESIAN_POINT('Origin',(141.982412223016,14.45,25.5));
#101003=CARTESIAN_POINT('',(141.982412223016,14.45,25.5));
#101004=CARTESIAN_POINT('',(141.982412223016,14.45,25.5));
#101005=CARTESIAN_POINT('',(141.982412223016,14.45,31.5));
#101006=CARTESIAN_POINT('',(141.982412223016,14.45,31.5));
#101007=CARTESIAN_POINT('',(141.982412223016,14.45,25.5));
#101008=CARTESIAN_POINT('Origin',(142.420237175574,14.45,25.5));
#101009=CARTESIAN_POINT('',(142.420237175574,14.45,25.5));
#101010=CARTESIAN_POINT('',(142.420237175574,14.45,25.5));
#101011=CARTESIAN_POINT('',(142.420237175574,14.45,31.5));
#101012=CARTESIAN_POINT('',(142.420237175574,14.45,31.5));
#101013=CARTESIAN_POINT('',(142.420237175574,14.45,25.5));
#101014=CARTESIAN_POINT('Origin',(142.81150517741,13.375,25.5));
#101015=CARTESIAN_POINT('',(142.81150517741,13.375,25.5));
#101016=CARTESIAN_POINT('',(142.81150517741,13.375,25.5));
#101017=CARTESIAN_POINT('',(142.81150517741,13.375,31.5));
#101018=CARTESIAN_POINT('',(142.81150517741,13.375,31.5));
#101019=CARTESIAN_POINT('',(142.81150517741,13.375,25.5));
#101020=CARTESIAN_POINT('Origin',(143.161940547975,13.375,25.5));
#101021=CARTESIAN_POINT('',(143.161940547975,13.375,25.5));
#101022=CARTESIAN_POINT('',(143.161940547975,13.375,25.5));
#101023=CARTESIAN_POINT('',(143.161940547975,13.375,31.5));
#101024=CARTESIAN_POINT('',(143.161940547975,13.375,31.5));
#101025=CARTESIAN_POINT('',(143.161940547975,13.375,25.5));
#101026=CARTESIAN_POINT('Origin',(143.553208549811,14.45,25.5));
#101027=CARTESIAN_POINT('',(143.553208549811,14.45,25.5));
#101028=CARTESIAN_POINT('',(143.553208549811,14.45,25.5));
#101029=CARTESIAN_POINT('',(143.553208549811,14.45,31.5));
#101030=CARTESIAN_POINT('',(143.553208549811,14.45,31.5));
#101031=CARTESIAN_POINT('',(143.553208549811,14.45,25.5));
#101032=CARTESIAN_POINT('Origin',(143.991033502369,14.45,25.5));
#101033=CARTESIAN_POINT('',(143.991033502369,14.45,25.5));
#101034=CARTESIAN_POINT('',(143.991033502369,14.45,25.5));
#101035=CARTESIAN_POINT('',(143.991033502369,14.45,31.5));
#101036=CARTESIAN_POINT('',(143.991033502369,14.45,31.5));
#101037=CARTESIAN_POINT('',(143.991033502369,14.45,25.5));
#101038=CARTESIAN_POINT('Origin',(144.382301504205,13.375,25.5));
#101039=CARTESIAN_POINT('',(144.382301504205,13.375,25.5));
#101040=CARTESIAN_POINT('',(144.382301504205,13.375,25.5));
#101041=CARTESIAN_POINT('',(144.382301504205,13.375,31.5));
#101042=CARTESIAN_POINT('',(144.382301504205,13.375,31.5));
#101043=CARTESIAN_POINT('',(144.382301504205,13.375,25.5));
#101044=CARTESIAN_POINT('Origin',(144.73273687477,13.375,25.5));
#101045=CARTESIAN_POINT('',(144.73273687477,13.375,25.5));
#101046=CARTESIAN_POINT('',(144.73273687477,13.375,25.5));
#101047=CARTESIAN_POINT('',(144.73273687477,13.375,31.5));
#101048=CARTESIAN_POINT('',(144.73273687477,13.375,31.5));
#101049=CARTESIAN_POINT('',(144.73273687477,13.375,25.5));
#101050=CARTESIAN_POINT('Origin',(145.124004876606,14.45,25.5));
#101051=CARTESIAN_POINT('',(145.124004876606,14.45,25.5));
#101052=CARTESIAN_POINT('',(145.124004876606,14.45,25.5));
#101053=CARTESIAN_POINT('',(145.124004876606,14.45,31.5));
#101054=CARTESIAN_POINT('',(145.124004876606,14.45,31.5));
#101055=CARTESIAN_POINT('',(145.124004876606,14.45,25.5));
#101056=CARTESIAN_POINT('Origin',(145.561829829164,14.45,25.5));
#101057=CARTESIAN_POINT('',(145.561829829164,14.45,25.5));
#101058=CARTESIAN_POINT('',(145.561829829164,14.45,25.5));
#101059=CARTESIAN_POINT('',(145.561829829164,14.45,31.5));
#101060=CARTESIAN_POINT('',(145.561829829164,14.45,31.5));
#101061=CARTESIAN_POINT('',(145.561829829164,14.45,25.5));
#101062=CARTESIAN_POINT('Origin',(145.953097831,13.375,25.5));
#101063=CARTESIAN_POINT('',(145.953097831,13.375,25.5));
#101064=CARTESIAN_POINT('',(145.953097831,13.375,25.5));
#101065=CARTESIAN_POINT('',(145.953097831,13.375,31.5));
#101066=CARTESIAN_POINT('',(145.953097831,13.375,31.5));
#101067=CARTESIAN_POINT('',(145.953097831,13.375,25.5));
#101068=CARTESIAN_POINT('Origin',(146.303533201565,13.375,25.5));
#101069=CARTESIAN_POINT('',(146.303533201565,13.375,25.5));
#101070=CARTESIAN_POINT('',(146.303533201565,13.375,25.5));
#101071=CARTESIAN_POINT('',(146.303533201565,13.375,31.5));
#101072=CARTESIAN_POINT('',(146.303533201565,13.375,31.5));
#101073=CARTESIAN_POINT('',(146.303533201565,13.375,25.5));
#101074=CARTESIAN_POINT('Origin',(146.694801203401,14.45,25.5));
#101075=CARTESIAN_POINT('',(146.694801203401,14.45,25.5));
#101076=CARTESIAN_POINT('',(146.694801203401,14.45,25.5));
#101077=CARTESIAN_POINT('',(146.694801203401,14.45,31.5));
#101078=CARTESIAN_POINT('',(146.694801203401,14.45,31.5));
#101079=CARTESIAN_POINT('',(146.694801203401,14.45,25.5));
#101080=CARTESIAN_POINT('Origin',(147.132626155959,14.45,25.5));
#101081=CARTESIAN_POINT('',(147.132626155959,14.45,25.5));
#101082=CARTESIAN_POINT('',(147.132626155959,14.45,25.5));
#101083=CARTESIAN_POINT('',(147.132626155959,14.45,31.5));
#101084=CARTESIAN_POINT('',(147.132626155959,14.45,31.5));
#101085=CARTESIAN_POINT('',(147.132626155959,14.45,25.5));
#101086=CARTESIAN_POINT('Origin',(147.523894157795,13.375,25.5));
#101087=CARTESIAN_POINT('',(147.523894157795,13.375,25.5));
#101088=CARTESIAN_POINT('',(147.523894157795,13.375,25.5));
#101089=CARTESIAN_POINT('',(147.523894157795,13.375,31.5));
#101090=CARTESIAN_POINT('',(147.523894157795,13.375,31.5));
#101091=CARTESIAN_POINT('',(147.523894157795,13.375,25.5));
#101092=CARTESIAN_POINT('Origin',(147.87432952836,13.375,25.5));
#101093=CARTESIAN_POINT('',(147.87432952836,13.375,25.5));
#101094=CARTESIAN_POINT('',(147.87432952836,13.375,25.5));
#101095=CARTESIAN_POINT('',(147.87432952836,13.375,31.5));
#101096=CARTESIAN_POINT('',(147.87432952836,13.375,31.5));
#101097=CARTESIAN_POINT('',(147.87432952836,13.375,25.5));
#101098=CARTESIAN_POINT('Origin',(148.265597530196,14.45,25.5));
#101099=CARTESIAN_POINT('',(148.265597530196,14.45,25.5));
#101100=CARTESIAN_POINT('',(148.265597530196,14.45,25.5));
#101101=CARTESIAN_POINT('',(148.265597530196,14.45,31.5));
#101102=CARTESIAN_POINT('',(148.265597530196,14.45,31.5));
#101103=CARTESIAN_POINT('',(148.265597530196,14.45,25.5));
#101104=CARTESIAN_POINT('Origin',(148.703422482754,14.45,25.5));
#101105=CARTESIAN_POINT('',(148.703422482754,14.45,25.5));
#101106=CARTESIAN_POINT('',(148.703422482754,14.45,25.5));
#101107=CARTESIAN_POINT('',(148.703422482754,14.45,31.5));
#101108=CARTESIAN_POINT('',(148.703422482754,14.45,31.5));
#101109=CARTESIAN_POINT('',(148.703422482754,14.45,25.5));
#101110=CARTESIAN_POINT('Origin',(149.09469048459,13.375,25.5));
#101111=CARTESIAN_POINT('',(149.09469048459,13.375,25.5));
#101112=CARTESIAN_POINT('',(149.09469048459,13.375,25.5));
#101113=CARTESIAN_POINT('',(149.09469048459,13.375,31.5));
#101114=CARTESIAN_POINT('',(149.09469048459,13.375,31.5));
#101115=CARTESIAN_POINT('',(149.09469048459,13.375,25.5));
#101116=CARTESIAN_POINT('Origin',(149.445125855155,13.375,25.5));
#101117=CARTESIAN_POINT('',(149.445125855155,13.375,25.5));
#101118=CARTESIAN_POINT('',(149.445125855155,13.375,25.5));
#101119=CARTESIAN_POINT('',(149.445125855155,13.375,31.5));
#101120=CARTESIAN_POINT('',(149.445125855155,13.375,31.5));
#101121=CARTESIAN_POINT('',(149.445125855155,13.375,25.5));
#101122=CARTESIAN_POINT('Origin',(149.836393856991,14.45,25.5));
#101123=CARTESIAN_POINT('',(149.836393856991,14.45,25.5));
#101124=CARTESIAN_POINT('',(149.836393856991,14.45,25.5));
#101125=CARTESIAN_POINT('',(149.836393856991,14.45,31.5));
#101126=CARTESIAN_POINT('',(149.836393856991,14.45,31.5));
#101127=CARTESIAN_POINT('',(149.836393856991,14.45,25.5));
#101128=CARTESIAN_POINT('Origin',(150.274218809549,14.45,25.5));
#101129=CARTESIAN_POINT('',(150.274218809549,14.45,25.5));
#101130=CARTESIAN_POINT('',(150.274218809549,14.45,25.5));
#101131=CARTESIAN_POINT('',(150.274218809549,14.45,31.5));
#101132=CARTESIAN_POINT('',(150.274218809549,14.45,31.5));
#101133=CARTESIAN_POINT('',(150.274218809549,14.45,25.5));
#101134=CARTESIAN_POINT('Origin',(150.665486811385,13.375,25.5));
#101135=CARTESIAN_POINT('',(150.665486811385,13.375,25.5));
#101136=CARTESIAN_POINT('',(150.665486811385,13.375,25.5));
#101137=CARTESIAN_POINT('',(150.665486811385,13.375,31.5));
#101138=CARTESIAN_POINT('',(150.665486811385,13.375,31.5));
#101139=CARTESIAN_POINT('',(150.665486811385,13.375,25.5));
#101140=CARTESIAN_POINT('Origin',(151.01592218195,13.375,25.5));
#101141=CARTESIAN_POINT('',(151.01592218195,13.375,25.5));
#101142=CARTESIAN_POINT('',(151.01592218195,13.375,25.5));
#101143=CARTESIAN_POINT('',(151.01592218195,13.375,31.5));
#101144=CARTESIAN_POINT('',(151.01592218195,13.375,31.5));
#101145=CARTESIAN_POINT('',(151.01592218195,13.375,25.5));
#101146=CARTESIAN_POINT('Origin',(151.407190183786,14.45,25.5));
#101147=CARTESIAN_POINT('',(151.407190183786,14.45,25.5));
#101148=CARTESIAN_POINT('',(151.407190183786,14.45,25.5));
#101149=CARTESIAN_POINT('',(151.407190183786,14.45,31.5));
#101150=CARTESIAN_POINT('',(151.407190183786,14.45,31.5));
#101151=CARTESIAN_POINT('',(151.407190183786,14.45,25.5));
#101152=CARTESIAN_POINT('Origin',(151.845015136344,14.45,25.5));
#101153=CARTESIAN_POINT('',(151.845015136344,14.45,25.5));
#101154=CARTESIAN_POINT('',(151.845015136344,14.45,25.5));
#101155=CARTESIAN_POINT('',(151.845015136344,14.45,31.5));
#101156=CARTESIAN_POINT('',(151.845015136344,14.45,31.5));
#101157=CARTESIAN_POINT('',(151.845015136344,14.45,25.5));
#101158=CARTESIAN_POINT('Origin',(152.23628313818,13.375,25.5));
#101159=CARTESIAN_POINT('',(152.23628313818,13.375,25.5));
#101160=CARTESIAN_POINT('',(152.23628313818,13.375,25.5));
#101161=CARTESIAN_POINT('',(152.23628313818,13.375,31.5));
#101162=CARTESIAN_POINT('',(152.23628313818,13.375,31.5));
#101163=CARTESIAN_POINT('',(152.23628313818,13.375,25.5));
#101164=CARTESIAN_POINT('Origin',(152.586718508745,13.375,25.5));
#101165=CARTESIAN_POINT('',(152.586718508745,13.375,25.5));
#101166=CARTESIAN_POINT('',(152.586718508745,13.375,25.5));
#101167=CARTESIAN_POINT('',(152.586718508745,13.375,31.5));
#101168=CARTESIAN_POINT('',(152.586718508745,13.375,31.5));
#101169=CARTESIAN_POINT('',(152.586718508745,13.375,25.5));
#101170=CARTESIAN_POINT('Origin',(152.977986510581,14.45,25.5));
#101171=CARTESIAN_POINT('',(152.977986510581,14.45,25.5));
#101172=CARTESIAN_POINT('',(152.977986510581,14.45,25.5));
#101173=CARTESIAN_POINT('',(152.977986510581,14.45,31.5));
#101174=CARTESIAN_POINT('',(152.977986510581,14.45,31.5));
#101175=CARTESIAN_POINT('',(152.977986510581,14.45,25.5));
#101176=CARTESIAN_POINT('Origin',(153.415811463139,14.45,25.5));
#101177=CARTESIAN_POINT('',(153.415811463139,14.45,25.5));
#101178=CARTESIAN_POINT('',(153.415811463139,14.45,25.5));
#101179=CARTESIAN_POINT('',(153.415811463139,14.45,31.5));
#101180=CARTESIAN_POINT('',(153.415811463139,14.45,31.5));
#101181=CARTESIAN_POINT('',(153.415811463139,14.45,25.5));
#101182=CARTESIAN_POINT('Origin',(153.807079464975,13.375,25.5));
#101183=CARTESIAN_POINT('',(153.807079464975,13.375,25.5));
#101184=CARTESIAN_POINT('',(153.807079464975,13.375,25.5));
#101185=CARTESIAN_POINT('',(153.807079464975,13.375,31.5));
#101186=CARTESIAN_POINT('',(153.807079464975,13.375,31.5));
#101187=CARTESIAN_POINT('',(153.807079464975,13.375,25.5));
#101188=CARTESIAN_POINT('Origin',(154.157514835539,13.375,25.5));
#101189=CARTESIAN_POINT('',(154.157514835539,13.375,25.5));
#101190=CARTESIAN_POINT('',(154.157514835539,13.375,25.5));
#101191=CARTESIAN_POINT('',(154.157514835539,13.375,31.5));
#101192=CARTESIAN_POINT('',(154.157514835539,13.375,31.5));
#101193=CARTESIAN_POINT('',(154.157514835539,13.375,25.5));
#101194=CARTESIAN_POINT('Origin',(154.548782837376,14.45,25.5));
#101195=CARTESIAN_POINT('',(154.548782837376,14.45,25.5));
#101196=CARTESIAN_POINT('',(154.548782837376,14.45,25.5));
#101197=CARTESIAN_POINT('',(154.548782837376,14.45,31.5));
#101198=CARTESIAN_POINT('',(154.548782837376,14.45,31.5));
#101199=CARTESIAN_POINT('',(154.548782837376,14.45,25.5));
#101200=CARTESIAN_POINT('Origin',(154.986607789934,14.45,25.5));
#101201=CARTESIAN_POINT('',(154.986607789934,14.45,25.5));
#101202=CARTESIAN_POINT('',(154.986607789934,14.45,25.5));
#101203=CARTESIAN_POINT('',(154.986607789934,14.45,31.5));
#101204=CARTESIAN_POINT('',(154.986607789934,14.45,31.5));
#101205=CARTESIAN_POINT('',(154.986607789934,14.45,25.5));
#101206=CARTESIAN_POINT('Origin',(155.37787579177,13.375,25.5));
#101207=CARTESIAN_POINT('',(155.37787579177,13.375,25.5));
#101208=CARTESIAN_POINT('',(155.37787579177,13.375,25.5));
#101209=CARTESIAN_POINT('',(155.37787579177,13.375,31.5));
#101210=CARTESIAN_POINT('',(155.37787579177,13.375,31.5));
#101211=CARTESIAN_POINT('',(155.37787579177,13.375,25.5));
#101212=CARTESIAN_POINT('Origin',(155.728311162334,13.375,25.5));
#101213=CARTESIAN_POINT('',(155.728311162334,13.375,25.5));
#101214=CARTESIAN_POINT('',(155.728311162334,13.375,25.5));
#101215=CARTESIAN_POINT('',(155.728311162334,13.375,31.5));
#101216=CARTESIAN_POINT('',(155.728311162334,13.375,31.5));
#101217=CARTESIAN_POINT('',(155.728311162334,13.375,25.5));
#101218=CARTESIAN_POINT('Origin',(156.119579164171,14.45,25.5));
#101219=CARTESIAN_POINT('',(156.119579164171,14.45,25.5));
#101220=CARTESIAN_POINT('',(156.119579164171,14.45,25.5));
#101221=CARTESIAN_POINT('',(156.119579164171,14.45,31.5));
#101222=CARTESIAN_POINT('',(156.119579164171,14.45,31.5));
#101223=CARTESIAN_POINT('',(156.119579164171,14.45,25.5));
#101224=CARTESIAN_POINT('Origin',(156.557404116728,14.45,25.5));
#101225=CARTESIAN_POINT('',(156.557404116728,14.45,25.5));
#101226=CARTESIAN_POINT('',(156.557404116728,14.45,25.5));
#101227=CARTESIAN_POINT('',(156.557404116728,14.45,31.5));
#101228=CARTESIAN_POINT('',(156.557404116728,14.45,31.5));
#101229=CARTESIAN_POINT('',(156.557404116728,14.45,25.5));
#101230=CARTESIAN_POINT('Origin',(156.948672118565,13.375,25.5));
#101231=CARTESIAN_POINT('',(156.948672118565,13.375,25.5));
#101232=CARTESIAN_POINT('',(156.948672118565,13.375,25.5));
#101233=CARTESIAN_POINT('',(156.948672118565,13.375,31.5));
#101234=CARTESIAN_POINT('',(156.948672118565,13.375,31.5));
#101235=CARTESIAN_POINT('',(156.948672118565,13.375,25.5));
#101236=CARTESIAN_POINT('Origin',(157.299107489129,13.375,25.5));
#101237=CARTESIAN_POINT('',(157.299107489129,13.375,25.5));
#101238=CARTESIAN_POINT('',(157.299107489129,13.375,25.5));
#101239=CARTESIAN_POINT('',(157.299107489129,13.375,31.5));
#101240=CARTESIAN_POINT('',(157.299107489129,13.375,31.5));
#101241=CARTESIAN_POINT('',(157.299107489129,13.375,25.5));
#101242=CARTESIAN_POINT('Origin',(157.690375490965,14.45,25.5));
#101243=CARTESIAN_POINT('',(157.690375490965,14.45,25.5));
#101244=CARTESIAN_POINT('',(157.690375490965,14.45,25.5));
#101245=CARTESIAN_POINT('',(157.690375490965,14.45,31.5));
#101246=CARTESIAN_POINT('',(157.690375490965,14.45,31.5));
#101247=CARTESIAN_POINT('',(157.690375490965,14.45,25.5));
#101248=CARTESIAN_POINT('Origin',(158.128200443523,14.45,25.5));
#101249=CARTESIAN_POINT('',(158.128200443523,14.45,25.5));
#101250=CARTESIAN_POINT('',(158.128200443523,14.45,25.5));
#101251=CARTESIAN_POINT('',(158.128200443523,14.45,31.5));
#101252=CARTESIAN_POINT('',(158.128200443523,14.45,31.5));
#101253=CARTESIAN_POINT('',(158.128200443523,14.45,25.5));
#101254=CARTESIAN_POINT('Origin',(158.519468445359,13.375,25.5));
#101255=CARTESIAN_POINT('',(158.519468445359,13.375,25.5));
#101256=CARTESIAN_POINT('',(158.519468445359,13.375,25.5));
#101257=CARTESIAN_POINT('',(158.519468445359,13.375,31.5));
#101258=CARTESIAN_POINT('',(158.519468445359,13.375,31.5));
#101259=CARTESIAN_POINT('',(158.519468445359,13.375,25.5));
#101260=CARTESIAN_POINT('Origin',(158.869903815924,13.375,25.5));
#101261=CARTESIAN_POINT('',(158.869903815924,13.375,25.5));
#101262=CARTESIAN_POINT('',(158.869903815924,13.375,25.5));
#101263=CARTESIAN_POINT('',(158.869903815924,13.375,31.5));
#101264=CARTESIAN_POINT('',(158.869903815924,13.375,31.5));
#101265=CARTESIAN_POINT('',(158.869903815924,13.375,25.5));
#101266=CARTESIAN_POINT('Origin',(159.26117181776,14.45,25.5));
#101267=CARTESIAN_POINT('',(159.26117181776,14.45,25.5));
#101268=CARTESIAN_POINT('',(159.26117181776,14.45,25.5));
#101269=CARTESIAN_POINT('',(159.26117181776,14.45,31.5));
#101270=CARTESIAN_POINT('',(159.26117181776,14.45,31.5));
#101271=CARTESIAN_POINT('',(159.26117181776,14.45,25.5));
#101272=CARTESIAN_POINT('Origin',(159.698996770318,14.45,25.5));
#101273=CARTESIAN_POINT('',(159.698996770318,14.45,25.5));
#101274=CARTESIAN_POINT('',(159.698996770318,14.45,25.5));
#101275=CARTESIAN_POINT('',(159.698996770318,14.45,31.5));
#101276=CARTESIAN_POINT('',(159.698996770318,14.45,31.5));
#101277=CARTESIAN_POINT('',(159.698996770318,14.45,25.5));
#101278=CARTESIAN_POINT('Origin',(160.090264772154,13.375,25.5));
#101279=CARTESIAN_POINT('',(160.090264772154,13.375,25.5));
#101280=CARTESIAN_POINT('',(160.090264772154,13.375,25.5));
#101281=CARTESIAN_POINT('',(160.090264772154,13.375,31.5));
#101282=CARTESIAN_POINT('',(160.090264772154,13.375,31.5));
#101283=CARTESIAN_POINT('',(160.090264772154,13.375,25.5));
#101284=CARTESIAN_POINT('Origin',(160.440700142719,13.375,25.5));
#101285=CARTESIAN_POINT('',(160.440700142719,13.375,25.5));
#101286=CARTESIAN_POINT('',(160.440700142719,13.375,25.5));
#101287=CARTESIAN_POINT('',(160.440700142719,13.375,31.5));
#101288=CARTESIAN_POINT('',(160.440700142719,13.375,31.5));
#101289=CARTESIAN_POINT('',(160.440700142719,13.375,25.5));
#101290=CARTESIAN_POINT('Origin',(160.831968144555,14.45,25.5));
#101291=CARTESIAN_POINT('',(160.831968144555,14.45,25.5));
#101292=CARTESIAN_POINT('',(160.831968144555,14.45,25.5));
#101293=CARTESIAN_POINT('',(160.831968144555,14.45,31.5));
#101294=CARTESIAN_POINT('',(160.831968144555,14.45,31.5));
#101295=CARTESIAN_POINT('',(160.831968144555,14.45,25.5));
#101296=CARTESIAN_POINT('Origin',(161.269793097113,14.45,25.5));
#101297=CARTESIAN_POINT('',(161.269793097113,14.45,25.5));
#101298=CARTESIAN_POINT('',(161.269793097113,14.45,25.5));
#101299=CARTESIAN_POINT('',(161.269793097113,14.45,31.5));
#101300=CARTESIAN_POINT('',(161.269793097113,14.45,31.5));
#101301=CARTESIAN_POINT('',(161.269793097113,14.45,25.5));
#101302=CARTESIAN_POINT('Origin',(161.661061098949,13.375,25.5));
#101303=CARTESIAN_POINT('',(161.661061098949,13.375,25.5));
#101304=CARTESIAN_POINT('',(161.661061098949,13.375,25.5));
#101305=CARTESIAN_POINT('',(161.661061098949,13.375,31.5));
#101306=CARTESIAN_POINT('',(161.661061098949,13.375,31.5));
#101307=CARTESIAN_POINT('',(161.661061098949,13.375,25.5));
#101308=CARTESIAN_POINT('Origin',(162.011496469514,13.375,25.5));
#101309=CARTESIAN_POINT('',(162.011496469514,13.375,25.5));
#101310=CARTESIAN_POINT('',(162.011496469514,13.375,25.5));
#101311=CARTESIAN_POINT('',(162.011496469514,13.375,31.5));
#101312=CARTESIAN_POINT('',(162.011496469514,13.375,31.5));
#101313=CARTESIAN_POINT('',(162.011496469514,13.375,25.5));
#101314=CARTESIAN_POINT('Origin',(162.40276447135,14.45,25.5));
#101315=CARTESIAN_POINT('',(162.40276447135,14.45,25.5));
#101316=CARTESIAN_POINT('',(162.40276447135,14.45,25.5));
#101317=CARTESIAN_POINT('',(162.40276447135,14.45,31.5));
#101318=CARTESIAN_POINT('',(162.40276447135,14.45,31.5));
#101319=CARTESIAN_POINT('',(162.40276447135,14.45,25.5));
#101320=CARTESIAN_POINT('Origin',(162.840589423908,14.45,25.5));
#101321=CARTESIAN_POINT('',(162.840589423908,14.45,25.5));
#101322=CARTESIAN_POINT('',(162.840589423908,14.45,25.5));
#101323=CARTESIAN_POINT('',(162.840589423908,14.45,31.5));
#101324=CARTESIAN_POINT('',(162.840589423908,14.45,31.5));
#101325=CARTESIAN_POINT('',(162.840589423908,14.45,25.5));
#101326=CARTESIAN_POINT('Origin',(163.231857425744,13.375,25.5));
#101327=CARTESIAN_POINT('',(163.231857425744,13.375,25.5));
#101328=CARTESIAN_POINT('',(163.231857425744,13.375,25.5));
#101329=CARTESIAN_POINT('',(163.231857425744,13.375,31.5));
#101330=CARTESIAN_POINT('',(163.231857425744,13.375,31.5));
#101331=CARTESIAN_POINT('',(163.231857425744,13.375,25.5));
#101332=CARTESIAN_POINT('Origin',(163.582292796309,13.375,25.5));
#101333=CARTESIAN_POINT('',(163.582292796309,13.375,25.5));
#101334=CARTESIAN_POINT('',(163.582292796309,13.375,25.5));
#101335=CARTESIAN_POINT('',(163.582292796309,13.375,31.5));
#101336=CARTESIAN_POINT('',(163.582292796309,13.375,31.5));
#101337=CARTESIAN_POINT('',(163.582292796309,13.375,25.5));
#101338=CARTESIAN_POINT('Origin',(163.973560798145,14.45,25.5));
#101339=CARTESIAN_POINT('',(163.973560798145,14.45,25.5));
#101340=CARTESIAN_POINT('',(163.973560798145,14.45,25.5));
#101341=CARTESIAN_POINT('',(163.973560798145,14.45,31.5));
#101342=CARTESIAN_POINT('',(163.973560798145,14.45,31.5));
#101343=CARTESIAN_POINT('',(163.973560798145,14.45,25.5));
#101344=CARTESIAN_POINT('Origin',(164.411385750703,14.45,25.5));
#101345=CARTESIAN_POINT('',(164.411385750703,14.45,25.5));
#101346=CARTESIAN_POINT('',(164.411385750703,14.45,25.5));
#101347=CARTESIAN_POINT('',(164.411385750703,14.45,31.5));
#101348=CARTESIAN_POINT('',(164.411385750703,14.45,31.5));
#101349=CARTESIAN_POINT('',(164.411385750703,14.45,25.5));
#101350=CARTESIAN_POINT('Origin',(164.802653752539,13.375,25.5));
#101351=CARTESIAN_POINT('',(164.802653752539,13.375,25.5));
#101352=CARTESIAN_POINT('',(164.802653752539,13.375,25.5));
#101353=CARTESIAN_POINT('',(164.802653752539,13.375,31.5));
#101354=CARTESIAN_POINT('',(164.802653752539,13.375,31.5));
#101355=CARTESIAN_POINT('',(164.802653752539,13.375,25.5));
#101356=CARTESIAN_POINT('Origin',(165.153089123104,13.375,25.5));
#101357=CARTESIAN_POINT('',(165.153089123104,13.375,25.5));
#101358=CARTESIAN_POINT('',(165.153089123104,13.375,25.5));
#101359=CARTESIAN_POINT('',(165.153089123104,13.375,31.5));
#101360=CARTESIAN_POINT('',(165.153089123104,13.375,31.5));
#101361=CARTESIAN_POINT('',(165.153089123104,13.375,25.5));
#101362=CARTESIAN_POINT('Origin',(165.54435712494,14.45,25.5));
#101363=CARTESIAN_POINT('',(165.54435712494,14.45,25.5));
#101364=CARTESIAN_POINT('',(165.54435712494,14.45,25.5));
#101365=CARTESIAN_POINT('',(165.54435712494,14.45,31.5));
#101366=CARTESIAN_POINT('',(165.54435712494,14.45,31.5));
#101367=CARTESIAN_POINT('',(165.54435712494,14.45,25.5));
#101368=CARTESIAN_POINT('Origin',(165.982182077498,14.45,25.5));
#101369=CARTESIAN_POINT('',(165.982182077498,14.45,25.5));
#101370=CARTESIAN_POINT('',(165.982182077498,14.45,25.5));
#101371=CARTESIAN_POINT('',(165.982182077498,14.45,31.5));
#101372=CARTESIAN_POINT('',(165.982182077498,14.45,31.5));
#101373=CARTESIAN_POINT('',(165.982182077498,14.45,25.5));
#101374=CARTESIAN_POINT('Origin',(166.373450079334,13.375,25.5));
#101375=CARTESIAN_POINT('',(166.373450079334,13.375,25.5));
#101376=CARTESIAN_POINT('',(166.373450079334,13.375,25.5));
#101377=CARTESIAN_POINT('',(166.373450079334,13.375,31.5));
#101378=CARTESIAN_POINT('',(166.373450079334,13.375,31.5));
#101379=CARTESIAN_POINT('',(166.373450079334,13.375,25.5));
#101380=CARTESIAN_POINT('Origin',(166.723885449899,13.375,25.5));
#101381=CARTESIAN_POINT('',(166.723885449899,13.375,25.5));
#101382=CARTESIAN_POINT('',(166.723885449899,13.375,25.5));
#101383=CARTESIAN_POINT('',(166.723885449899,13.375,31.5));
#101384=CARTESIAN_POINT('',(166.723885449899,13.375,31.5));
#101385=CARTESIAN_POINT('',(166.723885449899,13.375,25.5));
#101386=CARTESIAN_POINT('Origin',(167.115153451735,14.45,25.5));
#101387=CARTESIAN_POINT('',(167.115153451735,14.45,25.5));
#101388=CARTESIAN_POINT('',(167.115153451735,14.45,25.5));
#101389=CARTESIAN_POINT('',(167.115153451735,14.45,31.5));
#101390=CARTESIAN_POINT('',(167.115153451735,14.45,31.5));
#101391=CARTESIAN_POINT('',(167.115153451735,14.45,25.5));
#101392=CARTESIAN_POINT('Origin',(167.552978404293,14.45,25.5));
#101393=CARTESIAN_POINT('',(167.552978404293,14.45,25.5));
#101394=CARTESIAN_POINT('',(167.552978404293,14.45,25.5));
#101395=CARTESIAN_POINT('',(167.552978404293,14.45,31.5));
#101396=CARTESIAN_POINT('',(167.552978404293,14.45,31.5));
#101397=CARTESIAN_POINT('',(167.552978404293,14.45,25.5));
#101398=CARTESIAN_POINT('Origin',(167.944246406129,13.375,25.5));
#101399=CARTESIAN_POINT('',(167.944246406129,13.375,25.5));
#101400=CARTESIAN_POINT('',(167.944246406129,13.375,25.5));
#101401=CARTESIAN_POINT('',(167.944246406129,13.375,31.5));
#101402=CARTESIAN_POINT('',(167.944246406129,13.375,31.5));
#101403=CARTESIAN_POINT('',(167.944246406129,13.375,25.5));
#101404=CARTESIAN_POINT('Origin',(168.294681776694,13.375,25.5));
#101405=CARTESIAN_POINT('',(168.294681776694,13.375,25.5));
#101406=CARTESIAN_POINT('',(168.294681776694,13.375,25.5));
#101407=CARTESIAN_POINT('',(168.294681776694,13.375,31.5));
#101408=CARTESIAN_POINT('',(168.294681776694,13.375,31.5));
#101409=CARTESIAN_POINT('',(168.294681776694,13.375,25.5));
#101410=CARTESIAN_POINT('Origin',(168.68594977853,14.45,25.5));
#101411=CARTESIAN_POINT('',(168.68594977853,14.45,25.5));
#101412=CARTESIAN_POINT('',(168.68594977853,14.45,25.5));
#101413=CARTESIAN_POINT('',(168.68594977853,14.45,31.5));
#101414=CARTESIAN_POINT('',(168.68594977853,14.45,31.5));
#101415=CARTESIAN_POINT('',(168.68594977853,14.45,25.5));
#101416=CARTESIAN_POINT('Origin',(169.123774731088,14.45,25.5));
#101417=CARTESIAN_POINT('',(169.123774731088,14.45,25.5));
#101418=CARTESIAN_POINT('',(169.123774731088,14.45,25.5));
#101419=CARTESIAN_POINT('',(169.123774731088,14.45,31.5));
#101420=CARTESIAN_POINT('',(169.123774731088,14.45,31.5));
#101421=CARTESIAN_POINT('',(169.123774731088,14.45,25.5));
#101422=CARTESIAN_POINT('Origin',(169.515042732924,13.375,25.5));
#101423=CARTESIAN_POINT('',(169.515042732924,13.375,25.5));
#101424=CARTESIAN_POINT('',(169.515042732924,13.375,25.5));
#101425=CARTESIAN_POINT('',(169.515042732924,13.375,31.5));
#101426=CARTESIAN_POINT('',(169.515042732924,13.375,31.5));
#101427=CARTESIAN_POINT('',(169.515042732924,13.375,25.5));
#101428=CARTESIAN_POINT('Origin',(169.865478103488,13.375,25.5));
#101429=CARTESIAN_POINT('',(169.865478103488,13.375,25.5));
#101430=CARTESIAN_POINT('',(169.865478103488,13.375,25.5));
#101431=CARTESIAN_POINT('',(169.865478103488,13.375,31.5));
#101432=CARTESIAN_POINT('',(169.865478103488,13.375,31.5));
#101433=CARTESIAN_POINT('',(169.865478103488,13.375,25.5));
#101434=CARTESIAN_POINT('Origin',(170.256746105325,14.45,25.5));
#101435=CARTESIAN_POINT('',(170.256746105325,14.45,25.5));
#101436=CARTESIAN_POINT('',(170.256746105325,14.45,25.5));
#101437=CARTESIAN_POINT('',(170.256746105325,14.45,31.5));
#101438=CARTESIAN_POINT('',(170.256746105325,14.45,31.5));
#101439=CARTESIAN_POINT('',(170.256746105325,14.45,25.5));
#101440=CARTESIAN_POINT('Origin',(170.694571057882,14.45,25.5));
#101441=CARTESIAN_POINT('',(170.694571057882,14.45,25.5));
#101442=CARTESIAN_POINT('',(170.694571057882,14.45,25.5));
#101443=CARTESIAN_POINT('',(170.694571057882,14.45,31.5));
#101444=CARTESIAN_POINT('',(170.694571057882,14.45,31.5));
#101445=CARTESIAN_POINT('',(170.694571057882,14.45,25.5));
#101446=CARTESIAN_POINT('Origin',(171.085839059719,13.375,25.5));
#101447=CARTESIAN_POINT('',(171.085839059719,13.375,25.5));
#101448=CARTESIAN_POINT('',(171.085839059719,13.375,25.5));
#101449=CARTESIAN_POINT('',(171.085839059719,13.375,31.5));
#101450=CARTESIAN_POINT('',(171.085839059719,13.375,31.5));
#101451=CARTESIAN_POINT('',(171.085839059719,13.375,25.5));
#101452=CARTESIAN_POINT('Origin',(171.436274430283,13.375,25.5));
#101453=CARTESIAN_POINT('',(171.436274430283,13.375,25.5));
#101454=CARTESIAN_POINT('',(171.436274430283,13.375,25.5));
#101455=CARTESIAN_POINT('',(171.436274430283,13.375,31.5));
#101456=CARTESIAN_POINT('',(171.436274430283,13.375,31.5));
#101457=CARTESIAN_POINT('',(171.436274430283,13.375,25.5));
#101458=CARTESIAN_POINT('Origin',(171.827542432119,14.45,25.5));
#101459=CARTESIAN_POINT('',(171.827542432119,14.45,25.5));
#101460=CARTESIAN_POINT('',(171.827542432119,14.45,25.5));
#101461=CARTESIAN_POINT('',(171.827542432119,14.45,31.5));
#101462=CARTESIAN_POINT('',(171.827542432119,14.45,31.5));
#101463=CARTESIAN_POINT('',(171.827542432119,14.45,25.5));
#101464=CARTESIAN_POINT('Origin',(172.265367384677,14.45,25.5));
#101465=CARTESIAN_POINT('',(172.265367384677,14.45,25.5));
#101466=CARTESIAN_POINT('',(172.265367384677,14.45,25.5));
#101467=CARTESIAN_POINT('',(172.265367384677,14.45,31.5));
#101468=CARTESIAN_POINT('',(172.265367384677,14.45,31.5));
#101469=CARTESIAN_POINT('',(172.265367384677,14.45,25.5));
#101470=CARTESIAN_POINT('Origin',(172.656635386514,13.375,25.5));
#101471=CARTESIAN_POINT('',(172.656635386514,13.375,25.5));
#101472=CARTESIAN_POINT('',(172.656635386514,13.375,25.5));
#101473=CARTESIAN_POINT('',(172.656635386514,13.375,31.5));
#101474=CARTESIAN_POINT('',(172.656635386514,13.375,31.5));
#101475=CARTESIAN_POINT('',(172.656635386514,13.375,25.5));
#101476=CARTESIAN_POINT('Origin',(173.007070757078,13.375,25.5));
#101477=CARTESIAN_POINT('',(173.007070757078,13.375,25.5));
#101478=CARTESIAN_POINT('',(173.007070757078,13.375,25.5));
#101479=CARTESIAN_POINT('',(173.007070757078,13.375,31.5));
#101480=CARTESIAN_POINT('',(173.007070757078,13.375,31.5));
#101481=CARTESIAN_POINT('',(173.007070757078,13.375,25.5));
#101482=CARTESIAN_POINT('Origin',(173.398338758914,14.45,25.5));
#101483=CARTESIAN_POINT('',(173.398338758914,14.45,25.5));
#101484=CARTESIAN_POINT('',(173.398338758914,14.45,25.5));
#101485=CARTESIAN_POINT('',(173.398338758914,14.45,31.5));
#101486=CARTESIAN_POINT('',(173.398338758914,14.45,31.5));
#101487=CARTESIAN_POINT('',(173.398338758914,14.45,25.5));
#101488=CARTESIAN_POINT('Origin',(173.836163711472,14.45,25.5));
#101489=CARTESIAN_POINT('',(173.836163711472,14.45,25.5));
#101490=CARTESIAN_POINT('',(173.836163711472,14.45,25.5));
#101491=CARTESIAN_POINT('',(173.836163711472,14.45,31.5));
#101492=CARTESIAN_POINT('',(173.836163711472,14.45,31.5));
#101493=CARTESIAN_POINT('',(173.836163711472,14.45,25.5));
#101494=CARTESIAN_POINT('Origin',(174.227431713308,13.375,25.5));
#101495=CARTESIAN_POINT('',(174.227431713308,13.375,25.5));
#101496=CARTESIAN_POINT('',(174.227431713308,13.375,25.5));
#101497=CARTESIAN_POINT('',(174.227431713308,13.375,31.5));
#101498=CARTESIAN_POINT('',(174.227431713308,13.375,31.5));
#101499=CARTESIAN_POINT('',(174.227431713308,13.375,25.5));
#101500=CARTESIAN_POINT('Origin',(174.577867083873,13.375,25.5));
#101501=CARTESIAN_POINT('',(174.577867083873,13.375,25.5));
#101502=CARTESIAN_POINT('',(174.577867083873,13.375,25.5));
#101503=CARTESIAN_POINT('',(174.577867083873,13.375,31.5));
#101504=CARTESIAN_POINT('',(174.577867083873,13.375,31.5));
#101505=CARTESIAN_POINT('',(174.577867083873,13.375,25.5));
#101506=CARTESIAN_POINT('Origin',(174.969135085709,14.45,25.5));
#101507=CARTESIAN_POINT('',(174.969135085709,14.45,25.5));
#101508=CARTESIAN_POINT('',(174.969135085709,14.45,25.5));
#101509=CARTESIAN_POINT('',(174.969135085709,14.45,31.5));
#101510=CARTESIAN_POINT('',(174.969135085709,14.45,31.5));
#101511=CARTESIAN_POINT('',(174.969135085709,14.45,25.5));
#101512=CARTESIAN_POINT('Origin',(175.406960038267,14.45,25.5));
#101513=CARTESIAN_POINT('',(175.406960038267,14.45,25.5));
#101514=CARTESIAN_POINT('',(175.406960038267,14.45,25.5));
#101515=CARTESIAN_POINT('',(175.406960038267,14.45,31.5));
#101516=CARTESIAN_POINT('',(175.406960038267,14.45,31.5));
#101517=CARTESIAN_POINT('',(175.406960038267,14.45,25.5));
#101518=CARTESIAN_POINT('Origin',(175.798228040103,13.375,25.5));
#101519=CARTESIAN_POINT('',(175.798228040103,13.375,25.5));
#101520=CARTESIAN_POINT('',(175.798228040103,13.375,25.5));
#101521=CARTESIAN_POINT('',(175.798228040103,13.375,31.5));
#101522=CARTESIAN_POINT('',(175.798228040103,13.375,31.5));
#101523=CARTESIAN_POINT('',(175.798228040103,13.375,25.5));
#101524=CARTESIAN_POINT('Origin',(176.148663410668,13.375,25.5));
#101525=CARTESIAN_POINT('',(176.148663410668,13.375,25.5));
#101526=CARTESIAN_POINT('',(176.148663410668,13.375,25.5));
#101527=CARTESIAN_POINT('',(176.148663410668,13.375,31.5));
#101528=CARTESIAN_POINT('',(176.148663410668,13.375,31.5));
#101529=CARTESIAN_POINT('',(176.148663410668,13.375,25.5));
#101530=CARTESIAN_POINT('Origin',(176.539931412504,14.45,25.5));
#101531=CARTESIAN_POINT('',(176.539931412504,14.45,25.5));
#101532=CARTESIAN_POINT('',(176.539931412504,14.45,25.5));
#101533=CARTESIAN_POINT('',(176.539931412504,14.45,31.5));
#101534=CARTESIAN_POINT('',(176.539931412504,14.45,31.5));
#101535=CARTESIAN_POINT('',(176.539931412504,14.45,25.5));
#101536=CARTESIAN_POINT('Origin',(176.977756365062,14.45,25.5));
#101537=CARTESIAN_POINT('',(176.977756365062,14.45,25.5));
#101538=CARTESIAN_POINT('',(176.977756365062,14.45,25.5));
#101539=CARTESIAN_POINT('',(176.977756365062,14.45,31.5));
#101540=CARTESIAN_POINT('',(176.977756365062,14.45,31.5));
#101541=CARTESIAN_POINT('',(176.977756365062,14.45,25.5));
#101542=CARTESIAN_POINT('Origin',(177.369024366898,13.375,25.5));
#101543=CARTESIAN_POINT('',(177.369024366898,13.375,25.5));
#101544=CARTESIAN_POINT('',(177.369024366898,13.375,25.5));
#101545=CARTESIAN_POINT('',(177.369024366898,13.375,31.5));
#101546=CARTESIAN_POINT('',(177.369024366898,13.375,31.5));
#101547=CARTESIAN_POINT('',(177.369024366898,13.375,25.5));
#101548=CARTESIAN_POINT('Origin',(177.719459737463,13.375,25.5));
#101549=CARTESIAN_POINT('',(177.719459737463,13.375,25.5));
#101550=CARTESIAN_POINT('',(177.719459737463,13.375,25.5));
#101551=CARTESIAN_POINT('',(177.719459737463,13.375,31.5));
#101552=CARTESIAN_POINT('',(177.719459737463,13.375,31.5));
#101553=CARTESIAN_POINT('',(177.719459737463,13.375,25.5));
#101554=CARTESIAN_POINT('Origin',(178.110727739299,14.45,25.5));
#101555=CARTESIAN_POINT('',(178.110727739299,14.45,25.5));
#101556=CARTESIAN_POINT('',(178.110727739299,14.45,25.5));
#101557=CARTESIAN_POINT('',(178.110727739299,14.45,31.5));
#101558=CARTESIAN_POINT('',(178.110727739299,14.45,31.5));
#101559=CARTESIAN_POINT('',(178.110727739299,14.45,25.5));
#101560=CARTESIAN_POINT('Origin',(178.548552691857,14.45,25.5));
#101561=CARTESIAN_POINT('',(178.548552691857,14.45,25.5));
#101562=CARTESIAN_POINT('',(178.548552691857,14.45,25.5));
#101563=CARTESIAN_POINT('',(178.548552691857,14.45,31.5));
#101564=CARTESIAN_POINT('',(178.548552691857,14.45,31.5));
#101565=CARTESIAN_POINT('',(178.548552691857,14.45,25.5));
#101566=CARTESIAN_POINT('Origin',(178.939820693693,13.375,25.5));
#101567=CARTESIAN_POINT('',(178.939820693693,13.375,25.5));
#101568=CARTESIAN_POINT('',(178.939820693693,13.375,25.5));
#101569=CARTESIAN_POINT('',(178.939820693693,13.375,31.5));
#101570=CARTESIAN_POINT('',(178.939820693693,13.375,31.5));
#101571=CARTESIAN_POINT('',(178.939820693693,13.375,25.5));
#101572=CARTESIAN_POINT('Origin',(179.290256064258,13.375,25.5));
#101573=CARTESIAN_POINT('',(179.290256064258,13.375,25.5));
#101574=CARTESIAN_POINT('',(179.290256064258,13.375,25.5));
#101575=CARTESIAN_POINT('',(179.290256064258,13.375,31.5));
#101576=CARTESIAN_POINT('',(179.290256064258,13.375,31.5));
#101577=CARTESIAN_POINT('',(179.290256064258,13.375,25.5));
#101578=CARTESIAN_POINT('Origin',(179.681524066094,14.45,25.5));
#101579=CARTESIAN_POINT('',(179.681524066094,14.45,25.5));
#101580=CARTESIAN_POINT('',(179.681524066094,14.45,25.5));
#101581=CARTESIAN_POINT('',(179.681524066094,14.45,31.5));
#101582=CARTESIAN_POINT('',(179.681524066094,14.45,31.5));
#101583=CARTESIAN_POINT('',(179.681524066094,14.45,25.5));
#101584=CARTESIAN_POINT('Origin',(180.119349018652,14.45,25.5));
#101585=CARTESIAN_POINT('',(180.119349018652,14.45,25.5));
#101586=CARTESIAN_POINT('',(180.119349018652,14.45,25.5));
#101587=CARTESIAN_POINT('',(180.119349018652,14.45,31.5));
#101588=CARTESIAN_POINT('',(180.119349018652,14.45,31.5));
#101589=CARTESIAN_POINT('',(180.119349018652,14.45,25.5));
#101590=CARTESIAN_POINT('Origin',(180.510617020488,13.375,25.5));
#101591=CARTESIAN_POINT('',(180.510617020488,13.375,25.5));
#101592=CARTESIAN_POINT('',(180.510617020488,13.375,25.5));
#101593=CARTESIAN_POINT('',(180.510617020488,13.375,31.5));
#101594=CARTESIAN_POINT('',(180.510617020488,13.375,31.5));
#101595=CARTESIAN_POINT('',(180.510617020488,13.375,25.5));
#101596=CARTESIAN_POINT('Origin',(180.861052391053,13.375,25.5));
#101597=CARTESIAN_POINT('',(180.861052391053,13.375,25.5));
#101598=CARTESIAN_POINT('',(180.861052391053,13.375,25.5));
#101599=CARTESIAN_POINT('',(180.861052391053,13.375,31.5));
#101600=CARTESIAN_POINT('',(180.861052391053,13.375,31.5));
#101601=CARTESIAN_POINT('',(180.861052391053,13.375,25.5));
#101602=CARTESIAN_POINT('Origin',(181.252320392889,14.45,25.5));
#101603=CARTESIAN_POINT('',(181.252320392889,14.45,25.5));
#101604=CARTESIAN_POINT('',(181.252320392889,14.45,25.5));
#101605=CARTESIAN_POINT('',(181.252320392889,14.45,31.5));
#101606=CARTESIAN_POINT('',(181.252320392889,14.45,31.5));
#101607=CARTESIAN_POINT('',(181.252320392889,14.45,25.5));
#101608=CARTESIAN_POINT('Origin',(181.690145345447,14.45,25.5));
#101609=CARTESIAN_POINT('',(181.690145345447,14.45,25.5));
#101610=CARTESIAN_POINT('',(181.690145345447,14.45,25.5));
#101611=CARTESIAN_POINT('',(181.690145345447,14.45,31.5));
#101612=CARTESIAN_POINT('',(181.690145345447,14.45,31.5));
#101613=CARTESIAN_POINT('',(181.690145345447,14.45,25.5));
#101614=CARTESIAN_POINT('Origin',(182.081413347283,13.375,25.5));
#101615=CARTESIAN_POINT('',(182.081413347283,13.375,25.5));
#101616=CARTESIAN_POINT('',(182.081413347283,13.375,25.5));
#101617=CARTESIAN_POINT('',(182.081413347283,13.375,31.5));
#101618=CARTESIAN_POINT('',(182.081413347283,13.375,31.5));
#101619=CARTESIAN_POINT('',(182.081413347283,13.375,25.5));
#101620=CARTESIAN_POINT('Origin',(182.431848717848,13.375,25.5));
#101621=CARTESIAN_POINT('',(182.431848717848,13.375,25.5));
#101622=CARTESIAN_POINT('',(182.431848717848,13.375,25.5));
#101623=CARTESIAN_POINT('',(182.431848717848,13.375,31.5));
#101624=CARTESIAN_POINT('',(182.431848717848,13.375,31.5));
#101625=CARTESIAN_POINT('',(182.431848717848,13.375,25.5));
#101626=CARTESIAN_POINT('Origin',(182.823116719684,14.45,25.5));
#101627=CARTESIAN_POINT('',(182.823116719684,14.45,25.5));
#101628=CARTESIAN_POINT('',(182.823116719684,14.45,25.5));
#101629=CARTESIAN_POINT('',(182.823116719684,14.45,31.5));
#101630=CARTESIAN_POINT('',(182.823116719684,14.45,31.5));
#101631=CARTESIAN_POINT('',(182.823116719684,14.45,25.5));
#101632=CARTESIAN_POINT('Origin',(183.260941672242,14.45,25.5));
#101633=CARTESIAN_POINT('',(183.260941672242,14.45,25.5));
#101634=CARTESIAN_POINT('',(183.260941672242,14.45,25.5));
#101635=CARTESIAN_POINT('',(183.260941672242,14.45,31.5));
#101636=CARTESIAN_POINT('',(183.260941672242,14.45,31.5));
#101637=CARTESIAN_POINT('',(183.260941672242,14.45,25.5));
#101638=CARTESIAN_POINT('Origin',(183.652209674078,13.375,25.5));
#101639=CARTESIAN_POINT('',(183.652209674078,13.375,25.5));
#101640=CARTESIAN_POINT('',(183.652209674078,13.375,25.5));
#101641=CARTESIAN_POINT('',(183.652209674078,13.375,31.5));
#101642=CARTESIAN_POINT('',(183.652209674078,13.375,31.5));
#101643=CARTESIAN_POINT('',(183.652209674078,13.375,25.5));
#101644=CARTESIAN_POINT('Origin',(184.002645044642,13.375,25.5));
#101645=CARTESIAN_POINT('',(184.002645044642,13.375,25.5));
#101646=CARTESIAN_POINT('',(184.002645044642,13.375,25.5));
#101647=CARTESIAN_POINT('',(184.002645044642,13.375,31.5));
#101648=CARTESIAN_POINT('',(184.002645044642,13.375,31.5));
#101649=CARTESIAN_POINT('',(184.002645044642,13.375,25.5));
#101650=CARTESIAN_POINT('Origin',(184.393913046479,14.45,25.5));
#101651=CARTESIAN_POINT('',(184.393913046479,14.45,25.5));
#101652=CARTESIAN_POINT('',(184.393913046479,14.45,25.5));
#101653=CARTESIAN_POINT('',(184.393913046479,14.45,31.5));
#101654=CARTESIAN_POINT('',(184.393913046479,14.45,31.5));
#101655=CARTESIAN_POINT('',(184.393913046479,14.45,25.5));
#101656=CARTESIAN_POINT('Origin',(184.831737999037,14.45,25.5));
#101657=CARTESIAN_POINT('',(184.831737999037,14.45,25.5));
#101658=CARTESIAN_POINT('',(184.831737999037,14.45,25.5));
#101659=CARTESIAN_POINT('',(184.831737999037,14.45,31.5));
#101660=CARTESIAN_POINT('',(184.831737999037,14.45,31.5));
#101661=CARTESIAN_POINT('',(184.831737999037,14.45,25.5));
#101662=CARTESIAN_POINT('Origin',(185.223006000873,13.375,25.5));
#101663=CARTESIAN_POINT('',(185.223006000873,13.375,25.5));
#101664=CARTESIAN_POINT('',(185.223006000873,13.375,25.5));
#101665=CARTESIAN_POINT('',(185.223006000873,13.375,31.5));
#101666=CARTESIAN_POINT('',(185.223006000873,13.375,31.5));
#101667=CARTESIAN_POINT('',(185.223006000873,13.375,25.5));
#101668=CARTESIAN_POINT('Origin',(185.573441371437,13.375,25.5));
#101669=CARTESIAN_POINT('',(185.573441371437,13.375,25.5));
#101670=CARTESIAN_POINT('',(185.573441371437,13.375,25.5));
#101671=CARTESIAN_POINT('',(185.573441371437,13.375,31.5));
#101672=CARTESIAN_POINT('',(185.573441371437,13.375,31.5));
#101673=CARTESIAN_POINT('',(185.573441371437,13.375,25.5));
#101674=CARTESIAN_POINT('Origin',(185.964709373274,14.45,25.5));
#101675=CARTESIAN_POINT('',(185.964709373274,14.45,25.5));
#101676=CARTESIAN_POINT('',(185.964709373274,14.45,25.5));
#101677=CARTESIAN_POINT('',(185.964709373274,14.45,31.5));
#101678=CARTESIAN_POINT('',(185.964709373274,14.45,31.5));
#101679=CARTESIAN_POINT('',(185.964709373274,14.45,25.5));
#101680=CARTESIAN_POINT('Origin',(186.402534325831,14.45,25.5));
#101681=CARTESIAN_POINT('',(186.402534325831,14.45,25.5));
#101682=CARTESIAN_POINT('',(186.402534325831,14.45,25.5));
#101683=CARTESIAN_POINT('',(186.402534325831,14.45,31.5));
#101684=CARTESIAN_POINT('',(186.402534325831,14.45,31.5));
#101685=CARTESIAN_POINT('',(186.402534325831,14.45,25.5));
#101686=CARTESIAN_POINT('Origin',(186.793802327668,13.375,25.5));
#101687=CARTESIAN_POINT('',(186.793802327668,13.375,25.5));
#101688=CARTESIAN_POINT('',(186.793802327668,13.375,25.5));
#101689=CARTESIAN_POINT('',(186.793802327668,13.375,31.5));
#101690=CARTESIAN_POINT('',(186.793802327668,13.375,31.5));
#101691=CARTESIAN_POINT('',(186.793802327668,13.375,25.5));
#101692=CARTESIAN_POINT('Origin',(187.144237698232,13.375,25.5));
#101693=CARTESIAN_POINT('',(187.144237698232,13.375,25.5));
#101694=CARTESIAN_POINT('',(187.144237698232,13.375,25.5));
#101695=CARTESIAN_POINT('',(187.144237698232,13.375,31.5));
#101696=CARTESIAN_POINT('',(187.144237698232,13.375,31.5));
#101697=CARTESIAN_POINT('',(187.144237698232,13.375,25.5));
#101698=CARTESIAN_POINT('Origin',(187.535505700068,14.45,25.5));
#101699=CARTESIAN_POINT('',(187.535505700068,14.45,25.5));
#101700=CARTESIAN_POINT('',(187.535505700068,14.45,25.5));
#101701=CARTESIAN_POINT('',(187.535505700068,14.45,31.5));
#101702=CARTESIAN_POINT('',(187.535505700068,14.45,31.5));
#101703=CARTESIAN_POINT('',(187.535505700068,14.45,25.5));
#101704=CARTESIAN_POINT('Origin',(187.973330652626,14.45,25.5));
#101705=CARTESIAN_POINT('',(187.973330652626,14.45,25.5));
#101706=CARTESIAN_POINT('',(187.973330652626,14.45,25.5));
#101707=CARTESIAN_POINT('',(187.973330652626,14.45,31.5));
#101708=CARTESIAN_POINT('',(187.973330652626,14.45,31.5));
#101709=CARTESIAN_POINT('',(187.973330652626,14.45,25.5));
#101710=CARTESIAN_POINT('Origin',(188.364598654462,13.375,25.5));
#101711=CARTESIAN_POINT('',(188.364598654462,13.375,25.5));
#101712=CARTESIAN_POINT('',(188.364598654462,13.375,25.5));
#101713=CARTESIAN_POINT('',(188.364598654462,13.375,31.5));
#101714=CARTESIAN_POINT('',(188.364598654462,13.375,31.5));
#101715=CARTESIAN_POINT('',(188.364598654462,13.375,25.5));
#101716=CARTESIAN_POINT('Origin',(188.715034025027,13.375,25.5));
#101717=CARTESIAN_POINT('',(188.715034025027,13.375,25.5));
#101718=CARTESIAN_POINT('',(188.715034025027,13.375,25.5));
#101719=CARTESIAN_POINT('',(188.715034025027,13.375,31.5));
#101720=CARTESIAN_POINT('',(188.715034025027,13.375,31.5));
#101721=CARTESIAN_POINT('',(188.715034025027,13.375,25.5));
#101722=CARTESIAN_POINT('Origin',(189.106302026863,14.45,25.5));
#101723=CARTESIAN_POINT('',(189.106302026863,14.45,25.5));
#101724=CARTESIAN_POINT('',(189.106302026863,14.45,25.5));
#101725=CARTESIAN_POINT('',(189.106302026863,14.45,31.5));
#101726=CARTESIAN_POINT('',(189.106302026863,14.45,31.5));
#101727=CARTESIAN_POINT('',(189.106302026863,14.45,25.5));
#101728=CARTESIAN_POINT('Origin',(189.544126979421,14.45,25.5));
#101729=CARTESIAN_POINT('',(189.544126979421,14.45,25.5));
#101730=CARTESIAN_POINT('',(189.544126979421,14.45,25.5));
#101731=CARTESIAN_POINT('',(189.544126979421,14.45,31.5));
#101732=CARTESIAN_POINT('',(189.544126979421,14.45,31.5));
#101733=CARTESIAN_POINT('',(189.544126979421,14.45,25.5));
#101734=CARTESIAN_POINT('Origin',(189.935394981257,13.375,25.5));
#101735=CARTESIAN_POINT('',(189.935394981257,13.375,25.5));
#101736=CARTESIAN_POINT('',(189.935394981257,13.375,25.5));
#101737=CARTESIAN_POINT('',(189.935394981257,13.375,31.5));
#101738=CARTESIAN_POINT('',(189.935394981257,13.375,31.5));
#101739=CARTESIAN_POINT('',(189.935394981257,13.375,25.5));
#101740=CARTESIAN_POINT('Origin',(190.285830351822,13.375,25.5));
#101741=CARTESIAN_POINT('',(190.285830351822,13.375,25.5));
#101742=CARTESIAN_POINT('',(190.285830351822,13.375,25.5));
#101743=CARTESIAN_POINT('',(190.285830351822,13.375,31.5));
#101744=CARTESIAN_POINT('',(190.285830351822,13.375,31.5));
#101745=CARTESIAN_POINT('',(190.285830351822,13.375,25.5));
#101746=CARTESIAN_POINT('Origin',(190.677098353658,14.45,25.5));
#101747=CARTESIAN_POINT('',(190.677098353658,14.45,25.5));
#101748=CARTESIAN_POINT('',(190.677098353658,14.45,25.5));
#101749=CARTESIAN_POINT('',(190.677098353658,14.45,31.5));
#101750=CARTESIAN_POINT('',(190.677098353658,14.45,31.5));
#101751=CARTESIAN_POINT('',(190.677098353658,14.45,25.5));
#101752=CARTESIAN_POINT('Origin',(191.114923306216,14.45,25.5));
#101753=CARTESIAN_POINT('',(191.114923306216,14.45,25.5));
#101754=CARTESIAN_POINT('',(191.114923306216,14.45,25.5));
#101755=CARTESIAN_POINT('',(191.114923306216,14.45,31.5));
#101756=CARTESIAN_POINT('',(191.114923306216,14.45,31.5));
#101757=CARTESIAN_POINT('',(191.114923306216,14.45,25.5));
#101758=CARTESIAN_POINT('Origin',(191.506191308052,13.375,25.5));
#101759=CARTESIAN_POINT('',(191.506191308052,13.375,25.5));
#101760=CARTESIAN_POINT('',(191.506191308052,13.375,25.5));
#101761=CARTESIAN_POINT('',(191.506191308052,13.375,31.5));
#101762=CARTESIAN_POINT('',(191.506191308052,13.375,31.5));
#101763=CARTESIAN_POINT('',(191.506191308052,13.375,25.5));
#101764=CARTESIAN_POINT('Origin',(191.856626678617,13.375,25.5));
#101765=CARTESIAN_POINT('',(191.856626678617,13.375,25.5));
#101766=CARTESIAN_POINT('',(191.856626678617,13.375,25.5));
#101767=CARTESIAN_POINT('',(191.856626678617,13.375,31.5));
#101768=CARTESIAN_POINT('',(191.856626678617,13.375,31.5));
#101769=CARTESIAN_POINT('',(191.856626678617,13.375,25.5));
#101770=CARTESIAN_POINT('Origin',(192.247894680453,14.45,25.5));
#101771=CARTESIAN_POINT('',(192.247894680453,14.45,25.5));
#101772=CARTESIAN_POINT('',(192.247894680453,14.45,25.5));
#101773=CARTESIAN_POINT('',(192.247894680453,14.45,31.5));
#101774=CARTESIAN_POINT('',(192.247894680453,14.45,31.5));
#101775=CARTESIAN_POINT('',(192.247894680453,14.45,25.5));
#101776=CARTESIAN_POINT('Origin',(192.685719633011,14.45,25.5));
#101777=CARTESIAN_POINT('',(192.685719633011,14.45,25.5));
#101778=CARTESIAN_POINT('',(192.685719633011,14.45,25.5));
#101779=CARTESIAN_POINT('',(192.685719633011,14.45,31.5));
#101780=CARTESIAN_POINT('',(192.685719633011,14.45,31.5));
#101781=CARTESIAN_POINT('',(192.685719633011,14.45,25.5));
#101782=CARTESIAN_POINT('Origin',(193.076987634847,13.375,25.5));
#101783=CARTESIAN_POINT('',(193.076987634847,13.375,25.5));
#101784=CARTESIAN_POINT('',(193.076987634847,13.375,25.5));
#101785=CARTESIAN_POINT('',(193.076987634847,13.375,31.5));
#101786=CARTESIAN_POINT('',(193.076987634847,13.375,31.5));
#101787=CARTESIAN_POINT('',(193.076987634847,13.375,25.5));
#101788=CARTESIAN_POINT('Origin',(193.427423005412,13.375,25.5));
#101789=CARTESIAN_POINT('',(193.427423005412,13.375,25.5));
#101790=CARTESIAN_POINT('',(193.427423005412,13.375,25.5));
#101791=CARTESIAN_POINT('',(193.427423005412,13.375,31.5));
#101792=CARTESIAN_POINT('',(193.427423005412,13.375,31.5));
#101793=CARTESIAN_POINT('',(193.427423005412,13.375,25.5));
#101794=CARTESIAN_POINT('Origin',(193.818691007248,14.45,25.5));
#101795=CARTESIAN_POINT('',(193.818691007248,14.45,25.5));
#101796=CARTESIAN_POINT('',(193.818691007248,14.45,25.5));
#101797=CARTESIAN_POINT('',(193.818691007248,14.45,31.5));
#101798=CARTESIAN_POINT('',(193.818691007248,14.45,31.5));
#101799=CARTESIAN_POINT('',(193.818691007248,14.45,25.5));
#101800=CARTESIAN_POINT('Origin',(194.256515959806,14.45,25.5));
#101801=CARTESIAN_POINT('',(194.256515959806,14.45,25.5));
#101802=CARTESIAN_POINT('',(194.256515959806,14.45,25.5));
#101803=CARTESIAN_POINT('',(194.256515959806,14.45,31.5));
#101804=CARTESIAN_POINT('',(194.256515959806,14.45,31.5));
#101805=CARTESIAN_POINT('',(194.256515959806,14.45,25.5));
#101806=CARTESIAN_POINT('Origin',(194.647783961642,13.375,25.5));
#101807=CARTESIAN_POINT('',(194.647783961642,13.375,25.5));
#101808=CARTESIAN_POINT('',(194.647783961642,13.375,25.5));
#101809=CARTESIAN_POINT('',(194.647783961642,13.375,31.5));
#101810=CARTESIAN_POINT('',(194.647783961642,13.375,31.5));
#101811=CARTESIAN_POINT('',(194.647783961642,13.375,25.5));
#101812=CARTESIAN_POINT('Origin',(194.998219332207,13.375,25.5));
#101813=CARTESIAN_POINT('',(194.998219332207,13.375,25.5));
#101814=CARTESIAN_POINT('',(194.998219332207,13.375,25.5));
#101815=CARTESIAN_POINT('',(194.998219332207,13.375,31.5));
#101816=CARTESIAN_POINT('',(194.998219332207,13.375,31.5));
#101817=CARTESIAN_POINT('',(194.998219332207,13.375,25.5));
#101818=CARTESIAN_POINT('Origin',(195.389487334043,14.45,25.5));
#101819=CARTESIAN_POINT('',(195.389487334043,14.45,25.5));
#101820=CARTESIAN_POINT('',(195.389487334043,14.45,25.5));
#101821=CARTESIAN_POINT('',(195.389487334043,14.45,31.5));
#101822=CARTESIAN_POINT('',(195.389487334043,14.45,31.5));
#101823=CARTESIAN_POINT('',(195.389487334043,14.45,25.5));
#101824=CARTESIAN_POINT('Origin',(195.827312286601,14.45,25.5));
#101825=CARTESIAN_POINT('',(195.827312286601,14.45,25.5));
#101826=CARTESIAN_POINT('',(195.827312286601,14.45,25.5));
#101827=CARTESIAN_POINT('',(195.827312286601,14.45,31.5));
#101828=CARTESIAN_POINT('',(195.827312286601,14.45,31.5));
#101829=CARTESIAN_POINT('',(195.827312286601,14.45,25.5));
#101830=CARTESIAN_POINT('Origin',(196.218580288437,13.375,25.5));
#101831=CARTESIAN_POINT('',(196.218580288437,13.375,25.5));
#101832=CARTESIAN_POINT('',(196.218580288437,13.375,25.5));
#101833=CARTESIAN_POINT('',(196.218580288437,13.375,31.5));
#101834=CARTESIAN_POINT('',(196.218580288437,13.375,31.5));
#101835=CARTESIAN_POINT('',(196.218580288437,13.375,25.5));
#101836=CARTESIAN_POINT('Origin',(196.569015659002,13.375,25.5));
#101837=CARTESIAN_POINT('',(196.569015659002,13.375,25.5));
#101838=CARTESIAN_POINT('',(196.569015659002,13.375,25.5));
#101839=CARTESIAN_POINT('',(196.569015659002,13.375,31.5));
#101840=CARTESIAN_POINT('',(196.569015659002,13.375,31.5));
#101841=CARTESIAN_POINT('',(196.569015659002,13.375,25.5));
#101842=CARTESIAN_POINT('Origin',(196.960283660838,14.45,25.5));
#101843=CARTESIAN_POINT('',(196.960283660838,14.45,25.5));
#101844=CARTESIAN_POINT('',(196.960283660838,14.45,25.5));
#101845=CARTESIAN_POINT('',(196.960283660838,14.45,31.5));
#101846=CARTESIAN_POINT('',(196.960283660838,14.45,31.5));
#101847=CARTESIAN_POINT('',(196.960283660838,14.45,25.5));
#101848=CARTESIAN_POINT('Origin',(197.398108613396,14.45,25.5));
#101849=CARTESIAN_POINT('',(197.398108613396,14.45,25.5));
#101850=CARTESIAN_POINT('',(197.398108613396,14.45,25.5));
#101851=CARTESIAN_POINT('',(197.398108613396,14.45,31.5));
#101852=CARTESIAN_POINT('',(197.398108613396,14.45,31.5));
#101853=CARTESIAN_POINT('',(197.398108613396,14.45,25.5));
#101854=CARTESIAN_POINT('Origin',(197.789376615232,13.375,25.5));
#101855=CARTESIAN_POINT('',(197.789376615232,13.375,25.5));
#101856=CARTESIAN_POINT('',(197.789376615232,13.375,25.5));
#101857=CARTESIAN_POINT('',(197.789376615232,13.375,31.5));
#101858=CARTESIAN_POINT('',(197.789376615232,13.375,31.5));
#101859=CARTESIAN_POINT('',(197.789376615232,13.375,25.5));
#101860=CARTESIAN_POINT('Origin',(198.139811985797,13.375,25.5));
#101861=CARTESIAN_POINT('',(198.139811985797,13.375,25.5));
#101862=CARTESIAN_POINT('',(198.139811985797,13.375,25.5));
#101863=CARTESIAN_POINT('',(198.139811985797,13.375,31.5));
#101864=CARTESIAN_POINT('',(198.139811985797,13.375,31.5));
#101865=CARTESIAN_POINT('',(198.139811985797,13.375,25.5));
#101866=CARTESIAN_POINT('Origin',(198.531079987633,14.45,25.5));
#101867=CARTESIAN_POINT('',(198.531079987633,14.45,25.5));
#101868=CARTESIAN_POINT('',(198.531079987633,14.45,25.5));
#101869=CARTESIAN_POINT('',(198.531079987633,14.45,31.5));
#101870=CARTESIAN_POINT('',(198.531079987633,14.45,31.5));
#101871=CARTESIAN_POINT('',(198.531079987633,14.45,25.5));
#101872=CARTESIAN_POINT('Origin',(198.968904940191,14.45,25.5));
#101873=CARTESIAN_POINT('',(198.968904940191,14.45,25.5));
#101874=CARTESIAN_POINT('',(198.968904940191,14.45,25.5));
#101875=CARTESIAN_POINT('',(198.968904940191,14.45,31.5));
#101876=CARTESIAN_POINT('',(198.968904940191,14.45,31.5));
#101877=CARTESIAN_POINT('',(198.968904940191,14.45,25.5));
#101878=CARTESIAN_POINT('Origin',(199.360172942027,13.375,25.5));
#101879=CARTESIAN_POINT('',(199.360172942027,13.375,25.5));
#101880=CARTESIAN_POINT('',(199.360172942027,13.375,25.5));
#101881=CARTESIAN_POINT('',(199.360172942027,13.375,31.5));
#101882=CARTESIAN_POINT('',(199.360172942027,13.375,31.5));
#101883=CARTESIAN_POINT('',(199.360172942027,13.375,25.5));
#101884=CARTESIAN_POINT('Origin',(199.710608312591,13.375,25.5));
#101885=CARTESIAN_POINT('',(199.710608312591,13.375,25.5));
#101886=CARTESIAN_POINT('',(199.710608312591,13.375,25.5));
#101887=CARTESIAN_POINT('',(199.710608312591,13.375,31.5));
#101888=CARTESIAN_POINT('',(199.710608312591,13.375,31.5));
#101889=CARTESIAN_POINT('',(199.710608312591,13.375,25.5));
#101890=CARTESIAN_POINT('Origin',(200.101876314428,14.45,25.5));
#101891=CARTESIAN_POINT('',(200.101876314428,14.45,25.5));
#101892=CARTESIAN_POINT('',(200.101876314428,14.45,25.5));
#101893=CARTESIAN_POINT('',(200.101876314428,14.45,31.5));
#101894=CARTESIAN_POINT('',(200.101876314428,14.45,31.5));
#101895=CARTESIAN_POINT('',(200.101876314428,14.45,25.5));
#101896=CARTESIAN_POINT('Origin',(200.539701266986,14.45,25.5));
#101897=CARTESIAN_POINT('',(200.539701266986,14.45,25.5));
#101898=CARTESIAN_POINT('',(200.539701266986,14.45,25.5));
#101899=CARTESIAN_POINT('',(200.539701266986,14.45,31.5));
#101900=CARTESIAN_POINT('',(200.539701266986,14.45,31.5));
#101901=CARTESIAN_POINT('',(200.539701266986,14.45,25.5));
#101902=CARTESIAN_POINT('Origin',(200.930969268822,13.375,25.5));
#101903=CARTESIAN_POINT('',(200.930969268822,13.375,25.5));
#101904=CARTESIAN_POINT('',(200.930969268822,13.375,25.5));
#101905=CARTESIAN_POINT('',(200.930969268822,13.375,31.5));
#101906=CARTESIAN_POINT('',(200.930969268822,13.375,31.5));
#101907=CARTESIAN_POINT('',(200.930969268822,13.375,25.5));
#101908=CARTESIAN_POINT('Origin',(201.281404639386,13.375,25.5));
#101909=CARTESIAN_POINT('',(201.281404639386,13.375,25.5));
#101910=CARTESIAN_POINT('',(201.281404639386,13.375,25.5));
#101911=CARTESIAN_POINT('',(201.281404639386,13.375,31.5));
#101912=CARTESIAN_POINT('',(201.281404639386,13.375,31.5));
#101913=CARTESIAN_POINT('',(201.281404639386,13.375,25.5));
#101914=CARTESIAN_POINT('Origin',(201.672672641223,14.45,25.5));
#101915=CARTESIAN_POINT('',(201.672672641223,14.45,25.5));
#101916=CARTESIAN_POINT('',(201.672672641223,14.45,25.5));
#101917=CARTESIAN_POINT('',(201.672672641223,14.45,31.5));
#101918=CARTESIAN_POINT('',(201.672672641223,14.45,31.5));
#101919=CARTESIAN_POINT('',(201.672672641223,14.45,25.5));
#101920=CARTESIAN_POINT('Origin',(202.11049759378,14.45,25.5));
#101921=CARTESIAN_POINT('',(202.11049759378,14.45,25.5));
#101922=CARTESIAN_POINT('',(202.11049759378,14.45,25.5));
#101923=CARTESIAN_POINT('',(202.11049759378,14.45,31.5));
#101924=CARTESIAN_POINT('',(202.11049759378,14.45,31.5));
#101925=CARTESIAN_POINT('',(202.11049759378,14.45,25.5));
#101926=CARTESIAN_POINT('Origin',(202.501765595617,13.375,25.5));
#101927=CARTESIAN_POINT('',(202.501765595617,13.375,25.5));
#101928=CARTESIAN_POINT('',(202.501765595617,13.375,25.5));
#101929=CARTESIAN_POINT('',(202.501765595617,13.375,31.5));
#101930=CARTESIAN_POINT('',(202.501765595617,13.375,31.5));
#101931=CARTESIAN_POINT('',(202.501765595617,13.375,25.5));
#101932=CARTESIAN_POINT('Origin',(202.852200966181,13.375,25.5));
#101933=CARTESIAN_POINT('',(202.852200966181,13.375,25.5));
#101934=CARTESIAN_POINT('',(202.852200966181,13.375,25.5));
#101935=CARTESIAN_POINT('',(202.852200966181,13.375,31.5));
#101936=CARTESIAN_POINT('',(202.852200966181,13.375,31.5));
#101937=CARTESIAN_POINT('',(202.852200966181,13.375,25.5));
#101938=CARTESIAN_POINT('Origin',(203.243468968017,14.45,25.5));
#101939=CARTESIAN_POINT('',(203.243468968017,14.45,25.5));
#101940=CARTESIAN_POINT('',(203.243468968017,14.45,25.5));
#101941=CARTESIAN_POINT('',(203.243468968017,14.45,31.5));
#101942=CARTESIAN_POINT('',(203.243468968017,14.45,31.5));
#101943=CARTESIAN_POINT('',(203.243468968017,14.45,25.5));
#101944=CARTESIAN_POINT('Origin',(203.681293920575,14.45,25.5));
#101945=CARTESIAN_POINT('',(203.681293920575,14.45,25.5));
#101946=CARTESIAN_POINT('',(203.681293920575,14.45,25.5));
#101947=CARTESIAN_POINT('',(203.681293920575,14.45,31.5));
#101948=CARTESIAN_POINT('',(203.681293920575,14.45,31.5));
#101949=CARTESIAN_POINT('',(203.681293920575,14.45,25.5));
#101950=CARTESIAN_POINT('Origin',(204.072561922411,13.375,25.5));
#101951=CARTESIAN_POINT('',(204.072561922411,13.375,25.5));
#101952=CARTESIAN_POINT('',(204.072561922411,13.375,25.5));
#101953=CARTESIAN_POINT('',(204.072561922411,13.375,31.5));
#101954=CARTESIAN_POINT('',(204.072561922411,13.375,31.5));
#101955=CARTESIAN_POINT('',(204.072561922411,13.375,25.5));
#101956=CARTESIAN_POINT('Origin',(204.422997292976,13.375,25.5));
#101957=CARTESIAN_POINT('',(204.422997292976,13.375,25.5));
#101958=CARTESIAN_POINT('',(204.422997292976,13.375,25.5));
#101959=CARTESIAN_POINT('',(204.422997292976,13.375,31.5));
#101960=CARTESIAN_POINT('',(204.422997292976,13.375,31.5));
#101961=CARTESIAN_POINT('',(204.422997292976,13.375,25.5));
#101962=CARTESIAN_POINT('Origin',(204.814265294812,14.45,25.5));
#101963=CARTESIAN_POINT('',(204.814265294812,14.45,25.5));
#101964=CARTESIAN_POINT('',(204.814265294812,14.45,25.5));
#101965=CARTESIAN_POINT('',(204.814265294812,14.45,31.5));
#101966=CARTESIAN_POINT('',(204.814265294812,14.45,31.5));
#101967=CARTESIAN_POINT('',(204.814265294812,14.45,25.5));
#101968=CARTESIAN_POINT('Origin',(205.25209024737,14.45,25.5));
#101969=CARTESIAN_POINT('',(205.25209024737,14.45,25.5));
#101970=CARTESIAN_POINT('',(205.25209024737,14.45,25.5));
#101971=CARTESIAN_POINT('',(205.25209024737,14.45,31.5));
#101972=CARTESIAN_POINT('',(205.25209024737,14.45,31.5));
#101973=CARTESIAN_POINT('',(205.25209024737,14.45,25.5));
#101974=CARTESIAN_POINT('Origin',(205.643358249206,13.375,25.5));
#101975=CARTESIAN_POINT('',(205.643358249206,13.375,25.5));
#101976=CARTESIAN_POINT('',(205.643358249206,13.375,25.5));
#101977=CARTESIAN_POINT('',(205.643358249206,13.375,31.5));
#101978=CARTESIAN_POINT('',(205.643358249206,13.375,31.5));
#101979=CARTESIAN_POINT('',(205.643358249206,13.375,25.5));
#101980=CARTESIAN_POINT('Origin',(205.993793619771,13.375,25.5));
#101981=CARTESIAN_POINT('',(205.993793619771,13.375,25.5));
#101982=CARTESIAN_POINT('',(205.993793619771,13.375,25.5));
#101983=CARTESIAN_POINT('',(205.993793619771,13.375,31.5));
#101984=CARTESIAN_POINT('',(205.993793619771,13.375,31.5));
#101985=CARTESIAN_POINT('',(205.993793619771,13.375,25.5));
#101986=CARTESIAN_POINT('Origin',(206.385061621607,14.45,25.5));
#101987=CARTESIAN_POINT('',(206.385061621607,14.45,25.5));
#101988=CARTESIAN_POINT('',(206.385061621607,14.45,25.5));
#101989=CARTESIAN_POINT('',(206.385061621607,14.45,31.5));
#101990=CARTESIAN_POINT('',(206.385061621607,14.45,31.5));
#101991=CARTESIAN_POINT('',(206.385061621607,14.45,25.5));
#101992=CARTESIAN_POINT('Origin',(206.822886574165,14.45,25.5));
#101993=CARTESIAN_POINT('',(206.822886574165,14.45,25.5));
#101994=CARTESIAN_POINT('',(206.822886574165,14.45,25.5));
#101995=CARTESIAN_POINT('',(206.822886574165,14.45,31.5));
#101996=CARTESIAN_POINT('',(206.822886574165,14.45,31.5));
#101997=CARTESIAN_POINT('',(206.822886574165,14.45,25.5));
#101998=CARTESIAN_POINT('Origin',(207.214154576001,13.375,25.5));
#101999=CARTESIAN_POINT('',(207.214154576001,13.375,25.5));
#102000=CARTESIAN_POINT('',(207.214154576001,13.375,25.5));
#102001=CARTESIAN_POINT('',(207.214154576001,13.375,31.5));
#102002=CARTESIAN_POINT('',(207.214154576001,13.375,31.5));
#102003=CARTESIAN_POINT('',(207.214154576001,13.375,25.5));
#102004=CARTESIAN_POINT('Origin',(207.564589946566,13.375,25.5));
#102005=CARTESIAN_POINT('',(207.564589946566,13.375,25.5));
#102006=CARTESIAN_POINT('',(207.564589946566,13.375,25.5));
#102007=CARTESIAN_POINT('',(207.564589946566,13.375,31.5));
#102008=CARTESIAN_POINT('',(207.564589946566,13.375,31.5));
#102009=CARTESIAN_POINT('',(207.564589946566,13.375,25.5));
#102010=CARTESIAN_POINT('Origin',(207.955857948402,14.45,25.5));
#102011=CARTESIAN_POINT('',(207.955857948402,14.45,25.5));
#102012=CARTESIAN_POINT('',(207.955857948402,14.45,31.5));
#102013=CARTESIAN_POINT('Origin',(2.,14.45,25.5));
#102014=CARTESIAN_POINT('',(2.,14.45,31.5));
#102015=CARTESIAN_POINT('',(2.,14.45,25.5));
#102016=CARTESIAN_POINT('Origin',(110.,11.975,31.5));
#102017=CARTESIAN_POINT('Origin',(110.,11.975,25.5));
#113953=UNCERTAINTY_MEASURE_WITH_UNIT(LENGTH_MEASURE(0.01),#113985,
'DISTANCE_ACCURACY_VALUE',
'Maximum model space distance between geometric entities at asserted c
onnectivities');
#113964=UNCERTAINTY_MEASURE_WITH_UNIT(LENGTH_MEASURE(0.01),#113985,
'DISTANCE_ACCURACY_VALUE',
'Maximum model space distance between geometric entities at asserted c
onnectivities');
#113973=(
GEOMETRIC_REPRESENTATION_CONTEXT(3)
GLOBAL_UNCERTAINTY_ASSIGNED_CONTEXT((#113953))
GLOBAL_UNIT_ASSIGNED_CONTEXT((#113985,#113987,#113988))
REPRESENTATION_CONTEXT('','3D')
);
#113984=(
GEOMETRIC_REPRESENTATION_CONTEXT(3)
GLOBAL_UNCERTAINTY_ASSIGNED_CONTEXT((#113964))
GLOBAL_UNIT_ASSIGNED_CONTEXT((#113985,#113987,#113988))
REPRESENTATION_CONTEXT('','3D')
);
#113985=(
LENGTH_UNIT()
NAMED_UNIT(*)
SI_UNIT(.MILLI.,.METRE.)
);
#113987=(
NAMED_UNIT(*)
PLANE_ANGLE_UNIT()
SI_UNIT($,.RADIAN.)
);
#113988=(
NAMED_UNIT(*)
SI_UNIT($,.STERADIAN.)
SOLID_ANGLE_UNIT()
);
#113997=SHAPE_DEFINITION_REPRESENTATION(#114016,#114059);
#114016=PRODUCT_DEFINITION_SHAPE('',$,#114079);
#114059=SHAPE_REPRESENTATION('',(#62396),#113973);
#114070=PRODUCT_DEFINITION_CONTEXT('part definition',#114129,'design');
#114079=PRODUCT_DEFINITION('2026-10-05-09-49-30-957',
'Carriage Drive Gear Rack m0.5 x 6 x 216',#114098,#114070);
#114098=PRODUCT_DEFINITION_FORMATION('',$,#114139);
#114129=APPLICATION_CONTEXT(
'Core Data for Automotive Mechanical Design Process');
#114130=PRODUCT_CONTEXT('part definition',#114129,'mechanical');
#114139=PRODUCT('2026-10-05-09-49-30-957',
'Carriage Drive Gear Rack m0.5 x 6 x 216',$,(#114130));
#114290=COLOUR_RGB('Light Blue',0.38,0.62,0.78);
#114291=FILL_AREA_STYLE_COLOUR('',#114290);
#114292=FILL_AREA_STYLE('',(#114291));
#114293=SURFACE_STYLE_FILL_AREA(#114292);
#114294=SURFACE_SIDE_STYLE('',(#114293));
#114295=SURFACE_STYLE_USAGE(.BOTH.,#114294);
#114296=PRESENTATION_STYLE_ASSIGNMENT((#114295));
ENDSEC;
END-ISO-10303-21;
